ISO-10303-21;
HEADER;
FILE_DESCRIPTION((''),'2;1');
FILE_NAME('Vertical_Knob.step','2026-10-09T11:34:15-07:00',(''),(''),'','','');
FILE_SCHEMA (('AUTOMOTIVE_DESIGN { 1 0 10303 214 3 1 1 }'));
ENDSEC;
DATA;
#10=MECHANICAL_DESIGN_GEOMETRIC_PRESENTATION_REPRESENTATION('',(#628),#117170);
#586=SHAPE_REPRESENTATION_RELATIONSHIP('SRR','None',#117241,#607) ;
#607=ADVANCED_BREP_SHAPE_REPRESENTATION('',(#649),#117149) ;
#628=STYLED_ITEM('',(#117355),#649) ;
#649=MANIFOLD_SOLID_BREP('Body1',#49057) ;
#670=FACE_BOUND('',#14042,.T.) ;
#773=CONICAL_SURFACE('',#49762,5.625,0.558599315343563) ;
#774=B_SPLINE_CURVE_WITH_KNOTS('',3,(#70344,#70345,#70346,#70347,#70348,
#70349,#70350,#70351,#70352,#70353,#70354,#70355,#70356,#70357,#70358,#70359,
#70360,#70361,#70362,#70363,#70364,#70365,#70366,#70367,#70368,#70369,#70370,
#70371,#70372,#70373,#70374,#70375,#70376,#70377,#70378,#70379,#70380,#70381,
#70382,#70383,#70384,#70385,#70386,#70387,#70388,#70389,#70390,#70391,#70392,
#70393,#70394,#70395,#70396,#70397,#70398,#70399,#70400,#70401,#70402,#70403,
#70404,#70405,#70406,#70407,#70408,#70409,#70410,#70411,#70412,#70413,#70414,
#70415,#70416,#70417,#70418,#70419,#70420,#70421,#70422,#70423,#70424,#70425,
#70426,#70427,#70428,#70429,#70430,#70431),.UNSPECIFIED.,.F.,.F.,(4,3,3,
3,3,3,3,3,3,3,3,3,3,3,3,3,3,3,3,3,3,3,3,3,3,3,3,3,3,4),(-0.886548021255927,
-0.866020543548015,-0.85169317239197,-0.845493065840103,-0.808981660034209,
-0.804435696364636,-0.793163090763113,-0.783892247515284,-0.778078363126709,
-0.774199582871934,-0.763350099380766,-0.757877841764194,-0.753807164984933,
-0.753076248451023,-0.744625414255735,-0.742798718670203,-0.736893863257229,
-0.732522509684251,-0.728117623171179,-0.724865268798491,-0.722246227513741,
-0.711109540545207,-0.704984345704586,-0.701711705949509,-0.681173329351425,
-0.671410018653926,-0.651499699186982,-0.640118813275259,-0.619305464345444,
-0.599057470751597),.UNSPECIFIED.) ;
#775=B_SPLINE_CURVE_WITH_KNOTS('',3,(#70432,#70433,#70434,#70435,#70436,
#70437,#70438,#70439,#70440,#70441,#70442,#70443,#70444,#70445,#70446,#70447,
#70448,#70449,#70450,#70451,#70452,#70453,#70454,#70455,#70456,#70457,#70458,
#70459,#70460,#70461,#70462,#70463,#70464,#70465,#70466,#70467,#70468,#70469,
#70470,#70471,#70472,#70473,#70474,#70475,#70476,#70477,#70478,#70479,#70480,
#70481,#70482,#70483,#70484,#70485,#70486,#70487,#70488,#70489,#70490,#70491,
#70492,#70493,#70494,#70495,#70496,#70497,#70498,#70499,#70500,#70501,#70502,
#70503,#70504,#70505,#70506,#70507,#70508,#70509,#70510,#70511,#70512,#70513,
#70514,#70515,#70516,#70517,#70518,#70519,#70520,#70521,#70522,#70523,#70524,
#70525,#70526,#70527,#70528,#70529,#70530,#70531,#70532,#70533,#70534),
 .UNSPECIFIED.,.F.,.F.,(4,3,3,3,3,3,3,3,3,3,3,3,3,3,3,3,3,3,3,3,3,3,3,3,
3,3,3,3,3,3,3,3,3,3,4),(0.599057470828701,0.615298120440717,0.630942941477274,
0.640127549392609,0.652806522977644,0.665132753910298,0.676916585880226,
0.681197628036496,0.691465147697467,0.700856798218276,0.701732667358439,
0.711232361509187,0.720303122206591,0.722267706680382,0.729879902279182,
0.732535226341353,0.738884690099024,0.742802746002325,0.74911482874544,
0.753070265663297,0.760745074540522,0.763337785324268,0.77242917331783,
0.781938963322013,0.783872824646211,0.793256044991626,0.803051435018297,
0.804407863968155,0.816263178412735,0.828482331000289,0.841197645853686,
0.845477942612041,0.861112429390543,0.877369654187312,0.886548021255484),
 .UNSPECIFIED.) ;
#776=B_SPLINE_CURVE_WITH_KNOTS('',3,(#70636,#70637,#70638,#70639,#70640,
#70641,#70642,#70643,#70644,#70645,#70646,#70647,#70648,#70649,#70650,#70651,
#70652,#70653,#70654,#70655,#70656,#70657,#70658,#70659,#70660,#70661,#70662,
#70663,#70664,#70665,#70666,#70667,#70668,#70669,#70670,#70671,#70672,#70673,
#70674,#70675,#70676,#70677,#70678,#70679,#70680,#70681,#70682,#70683,#70684,
#70685,#70686,#70687,#70688,#70689,#70690,#70691,#70692,#70693,#70694,#70695,
#70696,#70697,#70698,#70699,#70700,#70701,#70702,#70703,#70704,#70705,#70706,
#70707,#70708,#70709,#70710,#70711,#70712,#70713,#70714,#70715,#70716,#70717,
#70718,#70719,#70720,#70721,#70722,#70723,#70724,#70725,#70726,#70727,#70728,
#70729,#70730,#70731,#70732,#70733,#70734,#70735,#70736,#70737,#70738),
 .UNSPECIFIED.,.F.,.F.,(4,3,3,3,3,3,3,3,3,3,3,3,3,3,3,3,3,3,3,3,3,3,3,3,
3,3,3,3,3,3,3,3,3,3,4),(-0.886548021255908,-0.85656200124965,-0.850026819726932,
-0.84552111160629,-0.818797995447373,-0.814748789578144,-0.809615111606091,
-0.804479243671707,-0.803419323869529,-0.79434065594564,-0.786062741228933,
-0.777784826512226,-0.769788161614651,-0.763365298601152,-0.756898169483173,
-0.751589110728878,-0.748585034020594,-0.747944605577357,-0.743298812044044,
-0.742232977096382,-0.736337056382533,-0.729968012731944,-0.727476816747177,
-0.722258382596352,-0.714591862386322,-0.712000866477793,-0.704984345704397,
-0.701741062663608,-0.687720687939676,-0.681207485515591,-0.671410018653668,
-0.652269418497491,-0.640136959183649,-0.619305464345044,-0.599057470751579),
 .UNSPECIFIED.) ;
#777=B_SPLINE_CURVE_WITH_KNOTS('',3,(#70739,#70740,#70741,#70742,#70743,
#70744,#70745,#70746,#70747,#70748,#70749,#70750,#70751,#70752,#70753),
 .UNSPECIFIED.,.F.,.F.,(4,1,1,1,1,1,1,1,1,1,1,1,4),(0.599057470748727,0.64012754939261,
0.681197628036493,0.701732667358435,0.712000187019406,0.722267706680377,
0.747936505832804,0.76333778532426,0.804407863968143,0.809541623798628,
0.814675383629114,0.845477942612026,0.886548021255909),.UNSPECIFIED.) ;
#778=B_SPLINE_CURVE_WITH_KNOTS('',3,(#70855,#70856,#70857,#70858,#70859,
#70860,#70861,#70862,#70863,#70864,#70865,#70866,#70867,#70868,#70869),
 .UNSPECIFIED.,.F.,.F.,(4,1,1,1,1,1,1,1,1,1,1,1,4),(-1.15463223446652,-1.11356235392859,
-1.07249247339066,-1.0519575331217,-1.03142259285273,-1.02115512271825,
-1.01088765258376,-1.00062018244928,-0.990352712314799,-0.969817772045833,
-0.949282831776868,-0.908212951238937,-0.867143070701024),.UNSPECIFIED.) ;
#779=B_SPLINE_CURVE_WITH_KNOTS('',3,(#70870,#70871,#70872,#70873,#70874,
#70875,#70876,#70877,#70878,#70879,#70880,#70881,#70882,#70883,#70884,#70885,
#70886,#70887,#70888,#70889,#70890,#70891,#70892,#70893,#70894,#70895,#70896,
#70897,#70898,#70899,#70900,#70901,#70902,#70903,#70904,#70905,#70906,#70907,
#70908,#70909,#70910,#70911,#70912,#70913,#70914,#70915,#70916,#70917,#70918,
#70919,#70920,#70921,#70922,#70923,#70924,#70925,#70926,#70927,#70928,#70929,
#70930,#70931,#70932,#70933,#70934,#70935,#70936,#70937,#70938,#70939,#70940,
#70941,#70942,#70943,#70944,#70945,#70946,#70947,#70948,#70949,#70950,#70951,
#70952,#70953,#70954,#70955,#70956,#70957,#70958,#70959,#70960,#70961,#70962,
#70963,#70964,#70965,#70966,#70967,#70968,#70969,#70970,#70971,#70972),
 .UNSPECIFIED.,.F.,.F.,(4,3,3,3,3,3,3,3,3,3,3,3,3,3,3,3,3,3,3,3,3,3,3,3,
3,3,3,3,3,3,3,3,3,3,4),(0.867143070701496,0.88348027656878,0.899207678557921,
0.908212951238937,0.920868217474062,0.93317273149953,0.944935984179887,
0.949282831776868,0.95955030191135,0.968956555049588,0.969817772045833,
0.979310937859832,0.988375034212218,0.990352712314798,0.997960594090661,
1.00062018244928,1.00697043075183,1.01088765258376,1.01719943353249,1.02115512271825,
1.02883039234673,1.03142259285273,1.04051400153883,1.05002381110541,1.05195753312169,
1.06134071200587,1.07113605612072,1.07249247339066,1.08434800661934,1.09656739397206,
1.10928297177777,1.11356235392859,1.12919562860283,1.14545149693943,1.15463223446608),
 .UNSPECIFIED.) ;
#780=B_SPLINE_CURVE_WITH_KNOTS('',3,(#71075,#71076,#71077,#71078,#71079,
#71080,#71081,#71082,#71083),.UNSPECIFIED.,.F.,.F.,(4,1,1,1,1,1,4),(-0.411832935461353,
-0.370762950184382,-0.32969296490741,-0.309157972268924,-0.288622979630438,
-0.278355483311195,-0.268092192038243),.UNSPECIFIED.) ;
#781=B_SPLINE_CURVE_WITH_KNOTS('',3,(#71084,#71085,#71086,#71087,#71088,
#71089,#71090,#71091,#71092,#71093),.UNSPECIFIED.,.F.,.F.,(4,2,1,1,1,1,
4),(-0.268087986585571,-0.257816585743201,-0.247549389803151,-0.227014997923051,
-0.206480606042951,-0.165411822282751,-0.124343038522569),.UNSPECIFIED.) ;
#782=B_SPLINE_CURVE_WITH_KNOTS('',3,(#71094,#71095,#71096,#71097,#71098,
#71099,#71100,#71101,#71102,#71103,#71104,#71105,#71106,#71107,#71108,#71109,
#71110,#71111,#71112,#71113,#71114,#71115,#71116,#71117,#71118,#71119,#71120,
#71121,#71122,#71123,#71124,#71125,#71126,#71127,#71128,#71129,#71130,#71131,
#71132,#71133,#71134,#71135,#71136,#71137,#71138,#71139,#71140,#71141,#71142,
#71143,#71144,#71145,#71146,#71147,#71148,#71149,#71150,#71151,#71152,#71153,
#71154,#71155,#71156,#71157,#71158,#71159,#71160,#71161,#71162,#71163,#71164,
#71165,#71166,#71167,#71168,#71169,#71170,#71171,#71172,#71173,#71174,#71175,
#71176,#71177,#71178,#71179,#71180,#71181,#71182,#71183,#71184,#71185,#71186,
#71187,#71188,#71189,#71190,#71191,#71192,#71193,#71194,#71195,#71196),
 .UNSPECIFIED.,.F.,.F.,(4,3,3,3,3,3,3,3,3,3,3,3,3,3,3,3,3,3,3,3,3,3,3,3,
3,3,3,3,3,3,3,3,3,3,4),(0.124343038523051,0.140680308431655,0.156407764717396,
0.165413023799523,0.178068277230974,0.190372779140203,0.202136018930834,
0.206483009076495,0.216750505395738,0.226156738905456,0.227018001714981,
0.236511182380948,0.245575293706971,0.247552994353466,0.25516079885379,
0.257820490672709,0.264170716687648,0.268087986991952,0.274399785478541,
0.278355483311195,0.286030903500035,0.288622979630438,0.297714437508149,
0.307224296648561,0.309157972268924,0.318541007588984,0.328336197211916,
0.32969296490741,0.341549046953001,0.353769017763909,0.366485239447413,
0.370762950184382,0.386395556645212,0.402650777555412,0.411832935460906),
 .UNSPECIFIED.) ;
#783=B_SPLINE_CURVE_WITH_KNOTS('',3,(#71293,#71294,#71295,#71296,#71297,
#71298,#71299,#71300,#71301,#71302,#71303,#71304,#71305,#71306,#71307,#71308,
#71309,#71310,#71311,#71312,#71313,#71314,#71315,#71316,#71317,#71318,#71319,
#71320,#71321,#71322,#71323,#71324,#71325,#71326,#71327,#71328,#71329,#71330,
#71331,#71332,#71333,#71334,#71335,#71336,#71337,#71338,#71339,#71340,#71341,
#71342,#71343,#71344,#71345,#71346,#71347,#71348,#71349,#71350,#71351,#71352,
#71353,#71354,#71355,#71356,#71357,#71358,#71359,#71360,#71361,#71362,#71363,
#71364,#71365,#71366,#71367,#71368,#71369,#71370,#71371,#71372,#71373,#71374,
#71375,#71376,#71377,#71378,#71379,#71380,#71381,#71382,#71383,#71384,#71385,
#71386,#71387,#71388,#71389,#71390,#71391,#71392,#71393,#71394,#71395,#71396,
#71397,#71398,#71399,#71400,#71401,#71402,#71403,#71404,#71405,#71406,#71407,
#71408,#71409,#71410),.UNSPECIFIED.,.F.,.F.,(4,3,3,3,3,3,3,3,3,3,3,3,3,
3,3,3,3,3,3,3,3,3,3,3,3,3,3,3,3,3,3,3,3,3,3,3,3,3,3,4),(-0.477703831735214,
-0.454370643331098,-0.441181670393938,-0.436642153009234,-0.419200933510066,
-0.415005716588499,-0.398974103759707,-0.395554960231289,-0.394574174536507,
-0.380610876858235,-0.378136361334893,-0.375012123153041,-0.368939677179199,
-0.360083437747083,-0.354460833860627,-0.348053020150135,-0.340898396750089,
-0.339739884687549,-0.333958883265811,-0.329511911359018,-0.328177881844074,
-0.323681740140828,-0.319864746381499,-0.313388628374842,-0.305652785221246,
-0.303121846558283,-0.29897808935245,-0.292853793170735,-0.27960979488877,
-0.276868043426208,-0.273343591995159,-0.272324458736955,-0.256566521937693,
-0.251801543361572,-0.233103219355294,-0.229693343333032,-0.22673609613777,
-0.210005147820851,-0.192797532028038,-0.190214667974652),.UNSPECIFIED.) ;
#784=B_SPLINE_CURVE_WITH_KNOTS('',3,(#71411,#71412,#71413,#71414,#71415,
#71416,#71417,#71418,#71419,#71420,#71421,#71422,#71423,#71424),
 .UNSPECIFIED.,.F.,.F.,(4,1,1,1,1,1,1,1,1,1,1,4),(0.190214667974634,0.251819488780472,
0.272354429049085,0.292889369317698,0.303156839452004,0.313424309586311,
0.323691779720617,0.354494190123537,0.375029130392149,0.395564070660762,
0.436633951197988,0.477703831735214),.UNSPECIFIED.) ;
#785=B_SPLINE_CURVE_WITH_KNOTS('',3,(#71526,#71527,#71528,#71529,#71530,
#71531,#71532,#71533,#71534,#71535,#71536,#71537,#71538,#71539,#71540,#71541,
#71542,#71543,#71544,#71545,#71546,#71547,#71548,#71549,#71550,#71551,#71552,
#71553,#71554,#71555,#71556,#71557,#71558,#71559,#71560,#71561,#71562,#71563,
#71564,#71565,#71566,#71567,#71568,#71569,#71570,#71571,#71572,#71573,#71574,
#71575,#71576,#71577,#71578,#71579,#71580,#71581,#71582,#71583,#71584,#71585,
#71586,#71587,#71588,#71589,#71590,#71591,#71592,#71593,#71594,#71595,#71596,
#71597,#71598,#71599,#71600,#71601,#71602,#71603,#71604,#71605,#71606,#71607,
#71608,#71609,#71610,#71611,#71612,#71613,#71614,#71615,#71616,#71617,#71618,
#71619,#71620,#71621,#71622,#71623,#71624,#71625,#71626,#71627,#71628),
 .UNSPECIFIED.,.F.,.F.,(4,3,3,3,3,3,3,3,3,3,3,3,3,3,3,3,3,3,3,3,3,3,3,3,
3,3,3,3,3,3,3,3,3,3,4),(-0.88654802125593,-0.856559921133392,-0.850026819726776,
-0.845521107818283,-0.818795307853085,-0.814748784266003,-0.809615106409565,
-0.804479238719332,-0.803419323869451,-0.794340522423511,-0.786062674467852,
-0.777784826512192,-0.769787867667373,-0.763365294944202,-0.756898169483178,
-0.751589194764963,-0.748585034020606,-0.747944599813433,-0.743298958411371,
-0.742232977096391,-0.736337056382542,-0.729968873694819,-0.72747681674717,
-0.72225837506046,-0.714591851231898,-0.712000858187692,-0.704984345704301,
-0.70174105366968,-0.687720677804165,-0.681207476307132,-0.671410018653507,
-0.65226935125413,-0.640136953755786,-0.619305464344787,-0.599057470751606),
 .UNSPECIFIED.) ;
#786=B_SPLINE_CURVE_WITH_KNOTS('',3,(#71629,#71630,#71631,#71632,#71633,
#71634,#71635,#71636,#71637,#71638,#71639,#71640,#71641,#71642,#71643),
 .UNSPECIFIED.,.F.,.F.,(4,1,1,1,1,1,1,1,1,1,1,1,4),(0.599057470748751,0.640127549392634,
0.681197628036517,0.701732667358458,0.712000187019429,0.7222677066804,0.747936505832826,
0.763337785324282,0.804407863968165,0.80954162379865,0.814675383629136,
0.845477942612048,0.88654802125593),.UNSPECIFIED.) ;
#787=B_SPLINE_CURVE_WITH_KNOTS('',3,(#71745,#71746,#71747,#71748,#71749,
#71750,#71751,#71752,#71753,#71754,#71755,#71756,#71757,#71758,#71759,#71760,
#71761,#71762,#71763,#71764,#71765,#71766,#71767,#71768,#71769,#71770,#71771,
#71772,#71773,#71774,#71775,#71776,#71777,#71778,#71779,#71780,#71781,#71782,
#71783,#71784,#71785,#71786,#71787,#71788,#71789,#71790,#71791,#71792,#71793,
#71794,#71795,#71796,#71797,#71798,#71799,#71800,#71801,#71802,#71803,#71804,
#71805,#71806,#71807,#71808,#71809,#71810,#71811,#71812,#71813,#71814,#71815,
#71816,#71817,#71818,#71819,#71820,#71821,#71822,#71823,#71824,#71825,#71826,
#71827,#71828,#71829,#71830,#71831,#71832,#71833,#71834,#71835,#71836,#71837,
#71838,#71839,#71840,#71841,#71842,#71843,#71844,#71845,#71846,#71847),
 .UNSPECIFIED.,.F.,.F.,(4,3,3,3,3,3,3,3,3,3,3,3,3,3,3,3,3,3,3,3,3,3,3,3,
3,3,3,3,3,3,3,3,3,3,4),(-0.886548021255932,-0.856559926135766,-0.850026819726765,
-0.845521107827399,-0.818795314317799,-0.814748784278784,-0.809615106422069,
-0.804479238731248,-0.803419323869445,-0.794340522744604,-0.786062674628396,
-0.777784826512188,-0.769787868374517,-0.763365294952999,-0.756898169483175,
-0.751589194563149,-0.748585034020601,-0.747944599827302,-0.743298958059412,
-0.742232977096372,-0.736337056382513,-0.729968871625694,-0.727476816747115,
-0.72225837507861,-0.714591851258856,-0.712000858207665,-0.704984345704104,
-0.701741053691342,-0.687720677828186,-0.681207476329301,-0.671410018653206,
-0.652269351415935,-0.640136953768839,-0.619305464344328,-0.599057470751597),
 .UNSPECIFIED.) ;
#788=B_SPLINE_CURVE_WITH_KNOTS('',3,(#71848,#71849,#71850,#71851,#71852,
#71853,#71854,#71855,#71856,#71857,#71858,#71859,#71860,#71861,#71862),
 .UNSPECIFIED.,.F.,.F.,(4,1,1,1,1,1,1,1,1,1,1,1,4),(0.599057470748744,0.640127549392629,
0.681197628036513,0.701732667358455,0.712000187019426,0.722267706680398,
0.747936505832825,0.763337785324282,0.804407863968166,0.809541623798652,
0.814675383629137,0.84547794261205,0.886548021255935),.UNSPECIFIED.) ;
#789=B_SPLINE_CURVE_WITH_KNOTS('',3,(#71964,#71965,#71966,#71967,#71968,
#71969,#71970,#71971,#71972,#71973,#71974,#71975,#71976,#71977,#71978,#71979,
#71980,#71981,#71982,#71983,#71984,#71985,#71986,#71987,#71988,#71989,#71990,
#71991,#71992,#71993,#71994,#71995,#71996,#71997,#71998,#71999,#72000,#72001,
#72002,#72003,#72004,#72005,#72006,#72007,#72008,#72009,#72010,#72011,#72012,
#72013,#72014,#72015,#72016,#72017,#72018,#72019,#72020,#72021,#72022,#72023,
#72024,#72025,#72026,#72027,#72028,#72029,#72030,#72031,#72032,#72033,#72034,
#72035,#72036,#72037,#72038,#72039,#72040,#72041,#72042,#72043,#72044,#72045,
#72046,#72047,#72048,#72049,#72050,#72051,#72052,#72053,#72054),
 .UNSPECIFIED.,.F.,.F.,(4,3,3,3,3,3,3,3,3,3,3,3,3,3,3,3,3,3,3,3,3,3,3,3,
3,3,3,3,3,3,4),(-1.15463223446653,-1.1341178340239,-1.12022883800639,-1.11360343358128,
-1.07254719690285,-1.05532975113685,-1.05201126806733,-1.04611234292978,
-1.04174078600302,-1.03146911237729,-1.02733004480818,-1.02513884232791,
-1.0228904427285,-1.01804576856663,-1.01603397735204,-1.01032624264144,
-1.00510701775925,-0.998953323245803,-0.99679388229667,-0.990336102906064,
-0.982532688656496,-0.980075180629686,-0.975907225267637,-0.969811398153971,
-0.950272727910358,-0.949277530134206,-0.926594479609855,-0.908211294032182,
-0.903665232052998,-0.873530848284397,-0.867143070669774),.UNSPECIFIED.) ;
#790=B_SPLINE_CURVE_WITH_KNOTS('',3,(#72055,#72056,#72057,#72058,#72059,
#72060,#72061,#72062,#72063,#72064,#72065,#72066,#72067,#72068,#72069),
 .UNSPECIFIED.,.F.,.F.,(4,1,1,1,1,1,1,1,1,1,1,1,4),(0.867143070669756,0.908212951212153,
0.949282831754549,0.969817772025747,0.980085242161346,0.990352712296945,
1.01602138763594,1.03142259283934,1.04169006297494,1.05195753311054,1.07249247338174,
1.11356235392413,1.15463223446653),.UNSPECIFIED.) ;
#791=B_SPLINE_CURVE_WITH_KNOTS('',3,(#72171,#72172,#72173,#72174,#72175,
#72176,#72177,#72178,#72179,#72180,#72181,#72182,#72183,#72184,#72185),
 .UNSPECIFIED.,.F.,.F.,(4,1,1,1,1,1,1,1,1,1,1,1,4),(-0.411832935461242,
-0.370762950184276,-0.329692964907306,-0.309157972268821,-0.298890475949579,
-0.288622979630336,-0.273221735151472,-0.247552994353366,-0.237285498034123,
-0.227018001714881,-0.206483009076396,-0.165413023799426,-0.124343038522472),
 .UNSPECIFIED.) ;
#792=B_SPLINE_CURVE_WITH_KNOTS('',3,(#72186,#72187,#72188,#72189,#72190,
#72191,#72192,#72193,#72194,#72195,#72196,#72197,#72198,#72199,#72200),
 .UNSPECIFIED.,.F.,.F.,(4,1,1,1,1,1,1,1,1,1,1,1,4),(0.124343038522454,0.165413023799424,
0.206483009076393,0.227018001714878,0.23728549803412,0.247552994353363,
0.273221735151469,0.288622979630332,0.298890475949574,0.309157972268817,
0.329692964907302,0.370762950184271,0.41183293546124),.UNSPECIFIED.) ;
#793=B_SPLINE_CURVE_WITH_KNOTS('',3,(#72296,#72297,#72298,#72299,#72300,
#72301,#72302,#72303,#72304,#72305,#72306,#72307,#72308,#72309,#72310,#72311,
#72312,#72313,#72314,#72315,#72316,#72317,#72318,#72319,#72320,#72321,#72322,
#72323,#72324,#72325,#72326,#72327,#72328,#72329,#72330,#72331,#72332,#72333,
#72334,#72335,#72336,#72337,#72338,#72339,#72340,#72341,#72342,#72343,#72344,
#72345,#72346,#72347,#72348,#72349,#72350,#72351,#72352,#72353,#72354,#72355,
#72356,#72357,#72358,#72359,#72360,#72361,#72362,#72363,#72364,#72365,#72366,
#72367,#72368,#72369,#72370,#72371,#72372,#72373,#72374,#72375,#72376,#72377,
#72378,#72379,#72380,#72381,#72382,#72383),.UNSPECIFIED.,.F.,.F.,(4,3,3,
3,3,3,3,3,3,3,3,3,3,3,3,3,3,3,3,3,3,3,3,3,3,3,3,3,3,4),(-0.477703831735207,
-0.453614605110258,-0.443230345021846,-0.436675004882822,-0.395618787860206,
-0.378433001370195,-0.375082879002063,-0.364812392178865,-0.354540709068515,
-0.350401876328947,-0.348213627724221,-0.34440122597587,-0.339813935131242,
-0.339105559341817,-0.333397652452776,-0.328177881844085,-0.322023624791636,
-0.319864746381504,-0.313407649569444,-0.305604236787224,-0.303146716277064,
-0.298978089352453,-0.29288292803837,-0.273343591995163,-0.272349038216806,
-0.249678142342238,-0.231282783565101,-0.226736096137766,-0.196808788304168,
-0.190214667976269),.UNSPECIFIED.) ;
#794=B_SPLINE_CURVE_WITH_KNOTS('',3,(#72384,#72385,#72386,#72387,#72388,
#72389,#72390,#72391,#72392,#72393,#72394,#72395,#72396,#72397,#72398),
 .UNSPECIFIED.,.F.,.F.,(4,1,1,1,1,1,1,1,1,1,1,1,4),(0.19021466797625,0.231284548513244,
0.272354429050238,0.292889369318735,0.303156839452983,0.313424309587232,
0.339092984922853,0.354494190124226,0.364761660258474,0.375029130392723,
0.395564070661219,0.436633951198213,0.477703831735207),.UNSPECIFIED.) ;
#795=B_SPLINE_CURVE_WITH_KNOTS('',3,(#72404,#72405,#72406,#72407,#72408,
#72409,#72410,#72411,#72412,#72413,#72414,#72415,#72416,#72417),
 .UNSPECIFIED.,.F.,.F.,(4,2,2,2,2,2,4),(-0.000285103889769581,0.,0.00872930952732865,
0.0170606390707464,0.0258600808710477,0.0324403480688856,0.0341876342319972),
 .UNSPECIFIED.) ;
#796=B_SPLINE_CURVE_WITH_KNOTS('',3,(#72421,#72422,#72423,#72424,#72425,
#72426,#72427,#72428,#72429,#72430,#72431,#72432),.UNSPECIFIED.,.F.,.F.,
(4,2,2,2,2,4),(0.,0.00612475744370298,0.0140348469016774,0.0236318332037711,
0.0338613775546519,0.0341436529593686),.UNSPECIFIED.) ;
#797=B_SPLINE_CURVE_WITH_KNOTS('',3,(#72503,#72504,#72505,#72506,#72507,
#72508,#72509,#72510,#72511,#72512,#72513,#72514,#72515,#72516,#72517,#72518,
#72519,#72520,#72521,#72522,#72523,#72524,#72525,#72526,#72527,#72528,#72529,
#72530,#72531,#72532,#72533,#72534,#72535,#72536,#72537,#72538,#72539,#72540,
#72541,#72542,#72543,#72544,#72545,#72546,#72547,#72548,#72549,#72550,#72551,
#72552,#72553,#72554,#72555,#72556,#72557,#72558,#72559,#72560,#72561,#72562,
#72563,#72564,#72565,#72566,#72567,#72568,#72569,#72570,#72571,#72572,#72573,
#72574,#72575,#72576,#72577,#72578,#72579,#72580,#72581,#72582,#72583,#72584,
#72585,#72586,#72587,#72588,#72589,#72590,#72591,#72592,#72593,#72594,#72595,
#72596,#72597,#72598,#72599,#72600,#72601,#72602,#72603,#72604,#72605,#72606,
#72607,#72608,#72609,#72610,#72611,#72612,#72613,#72614),.UNSPECIFIED.,
 .F.,.F.,(4,3,3,3,3,3,3,3,3,3,3,3,3,3,3,3,3,3,3,3,3,3,3,3,3,3,3,3,3,3,3,
3,3,3,3,3,3,4),(-0.886548021255927,-0.863182140298643,-0.850026819726694,
-0.845485034834745,-0.828030597997826,-0.823995246256633,-0.807954076785211,
-0.804397382367369,-0.803419323869412,-0.789454447123549,-0.78719953786741,
-0.783854574530306,-0.777784826512168,-0.768895955447484,-0.763303798695202,
-0.756898169483172,-0.749793713751161,-0.748585034020601,-0.74223297709638,
-0.736710121550931,-0.736337056382528,-0.732525933237352,-0.727476816747137,
-0.722225326154133,-0.714703999684171,-0.7119635411798,-0.704984345704188,
-0.70169442338794,-0.687771632725246,-0.681167700475735,-0.671410018653332,
-0.660643601956556,-0.641874291222971,-0.639974533150539,-0.620382689790686,
-0.619305464344523,-0.602967164401198,-0.599057470751627),.UNSPECIFIED.) ;
#798=B_SPLINE_CURVE_WITH_KNOTS('',3,(#72615,#72616,#72617,#72618,#72619,
#72620,#72621,#72622,#72623,#72624,#72625,#72626,#72627,#72628),
 .UNSPECIFIED.,.F.,.F.,(4,1,1,1,1,1,1,1,1,1,1,4),(0.599057470748752,0.660662588714575,
0.681197628036517,0.701732667358458,0.712000187019428,0.722267706680399,
0.732535226341369,0.763337785324281,0.783872824646222,0.804407863968163,
0.845477942612046,0.886548021255928),.UNSPECIFIED.) ;
#799=B_SPLINE_CURVE_WITH_KNOTS('',3,(#72632,#72633,#72634,#72635,#72636,
#72637,#72638,#72639,#72640,#72641,#72642,#72643),.UNSPECIFIED.,.F.,.F.,
(4,2,2,2,2,4),(0.,0.00612475744371704,0.0140348469017579,0.0236318332042238,
0.0338613775553621,0.0341436529609325),.UNSPECIFIED.) ;
#800=B_SPLINE_CURVE_WITH_KNOTS('',3,(#72646,#72647,#72648,#72649,#72650,
#72651),.UNSPECIFIED.,.F.,.F.,(4,2,4),(0.027568167455487,0.0309707637796999,
0.0317834882745698),.UNSPECIFIED.) ;
#801=B_SPLINE_CURVE_WITH_KNOTS('',3,(#72654,#72655,#72656,#72657,#72658,
#72659),.UNSPECIFIED.,.F.,.F.,(4,2,4),(0.0987440670458636,0.10214723221737,
0.102957912597527),.UNSPECIFIED.) ;
#802=B_SPLINE_CURVE_WITH_KNOTS('',3,(#72663,#72664,#72665,#72666,#72667,
#72668,#72669,#72670,#72671,#72672,#72673,#72674,#72675,#72676),
 .UNSPECIFIED.,.F.,.F.,(4,2,2,2,2,2,4),(-0.000285103882378192,0.,0.00872930953448812,
0.0170606390834788,0.0258600808806183,0.0324403480767969,0.0341876342336229),
 .UNSPECIFIED.) ;
#803=B_SPLINE_CURVE_WITH_KNOTS('',3,(#72682,#72683,#72684,#72685,#72686,
#72687,#72688,#72689,#72690,#72691,#72692,#72693,#72694,#72695),
 .UNSPECIFIED.,.F.,.F.,(4,2,2,2,2,2,4),(-0.000285103883943185,2.27041150636931E-14,
0.00872930953329209,0.0170606390813087,0.0258600808790012,0.0324403480754976,
0.0341876342333561),.UNSPECIFIED.) ;
#804=B_SPLINE_CURVE_WITH_KNOTS('',3,(#72698,#72699,#72700,#72701,#72702,
#72703),.UNSPECIFIED.,.F.,.F.,(4,2,4),(0.0275681674553535,0.0309707637795716,
0.0317834882743947),.UNSPECIFIED.) ;
#805=B_SPLINE_CURVE_WITH_KNOTS('',3,(#72706,#72707,#72708,#72709,#72710,
#72711),.UNSPECIFIED.,.F.,.F.,(4,2,4),(0.0987440670452405,0.102147232216738,
0.102957912596903),.UNSPECIFIED.) ;
#806=B_SPLINE_CURVE_WITH_KNOTS('',3,(#72715,#72716,#72717,#72718,#72719,
#72720,#72721,#72722,#72723,#72724,#72725,#72726),.UNSPECIFIED.,.F.,.F.,
(4,2,2,2,2,4),(0.,0.00612475744371102,0.0140348469017037,0.0236318332038197,
0.0338613775547199,0.0341436529588805),.UNSPECIFIED.) ;
#807=B_SPLINE_CURVE_WITH_KNOTS('',3,(#72729,#72730,#72731,#72732,#72733,
#72734),.UNSPECIFIED.,.F.,.F.,(4,2,4),(0.0275681674555189,0.0309707637797563,
0.0317834882746156),.UNSPECIFIED.) ;
#808=B_SPLINE_CURVE_WITH_KNOTS('',3,(#72737,#72738,#72739,#72740,#72741,
#72742),.UNSPECIFIED.,.F.,.F.,(4,2,4),(0.0987440670463347,0.102147232217918,
0.102957912598071),.UNSPECIFIED.) ;
#809=B_SPLINE_CURVE_WITH_KNOTS('',3,(#72813,#72814,#72815,#72816,#72817,
#72818,#72819,#72820,#72821,#72822,#72823,#72824,#72825,#72826,#72827,#72828,
#72829,#72830,#72831,#72832,#72833,#72834,#72835,#72836,#72837,#72838,#72839,
#72840,#72841,#72842,#72843,#72844,#72845,#72846,#72847,#72848,#72849,#72850,
#72851,#72852,#72853,#72854,#72855,#72856,#72857,#72858,#72859,#72860,#72861,
#72862,#72863,#72864,#72865,#72866,#72867,#72868,#72869,#72870,#72871,#72872,
#72873,#72874,#72875,#72876,#72877,#72878,#72879,#72880,#72881,#72882,#72883,
#72884,#72885,#72886,#72887,#72888,#72889,#72890,#72891,#72892,#72893,#72894,
#72895,#72896,#72897,#72898,#72899,#72900,#72901,#72902,#72903,#72904,#72905,
#72906,#72907,#72908,#72909,#72910,#72911,#72912,#72913,#72914,#72915,#72916,
#72917,#72918,#72919,#72920,#72921,#72922,#72923,#72924),.UNSPECIFIED.,
 .F.,.F.,(4,3,3,3,3,3,3,3,3,3,3,3,3,3,3,3,3,3,3,3,3,3,3,3,3,3,3,3,3,3,3,
3,3,3,3,3,3,4),(-0.886548021255915,-0.863182183022991,-0.850026819726918,
-0.845485033904693,-0.828030709545769,-0.823993850862195,-0.807952761446644,
-0.804397379038152,-0.803419323869518,-0.789454453599431,-0.78719888115785,
-0.783854569044938,-0.777784826512226,-0.768895988020034,-0.763303790457395,
-0.756898169483171,-0.749793571369931,-0.748585034020596,-0.742232977096394,
-0.73671041200043,-0.736337056382546,-0.732525922194933,-0.727476816747194,
-0.722225315602094,-0.714704063959347,-0.711963531357458,-0.704984345704372,
-0.701694414342138,-0.687771578704614,-0.681167693161271,-0.671410018653635,
-0.66064359619164,-0.641874296603296,-0.639974530268315,-0.62038268997317,
-0.61930546434499,-0.602967220633359,-0.599057470751585),.UNSPECIFIED.) ;
#810=B_SPLINE_CURVE_WITH_KNOTS('',3,(#72925,#72926,#72927,#72928,#72929,
#72930,#72931,#72932,#72933,#72934,#72935,#72936,#72937,#72938),
 .UNSPECIFIED.,.F.,.F.,(4,1,1,1,1,1,1,1,1,1,1,4),(0.599057470748733,0.660662588714558,
0.681197628036499,0.701732667358441,0.712000187019412,0.722267706680383,
0.732535226341354,0.763337785324266,0.783872824646208,0.804407863968149,
0.845477942612033,0.886548021255916),.UNSPECIFIED.) ;
#811=B_SPLINE_CURVE_WITH_KNOTS('',3,(#72942,#72943,#72944,#72945,#72946,
#72947,#72948,#72949,#72950,#72951,#72952,#72953),.UNSPECIFIED.,.F.,.F.,
(4,2,2,2,2,4),(0.,0.00612475744370553,0.0140348469016906,0.0236318332038693,
0.0338613775548128,0.0341436529592063),.UNSPECIFIED.) ;
#812=B_SPLINE_CURVE_WITH_KNOTS('',3,(#72957,#72958,#72959,#72960,#72961,
#72962,#72963,#72964,#72965,#72966,#72967,#72968,#72969,#72970),
 .UNSPECIFIED.,.F.,.F.,(4,2,2,2,2,2,4),(-0.000285103891090118,0.,0.00872930952749538,
0.0170606390711773,0.0258600808714152,0.0324403480692667,0.0341876342322289),
 .UNSPECIFIED.) ;
#813=B_SPLINE_CURVE_WITH_KNOTS('',3,(#72976,#72977,#72978,#72979,#72980,
#72981,#72982,#72983,#72984,#72985,#72986,#72987,#72988,#72989),
 .UNSPECIFIED.,.F.,.F.,(4,2,2,2,2,2,4),(-0.000285103883294333,0.,0.00872930953430471,
0.0170606390832003,0.0258600808804658,0.0324403480767586,0.0341876342335693),
 .UNSPECIFIED.) ;
#814=B_SPLINE_CURVE_WITH_KNOTS('',3,(#72992,#72993,#72994,#72995,#72996,
#72997),.UNSPECIFIED.,.F.,.F.,(4,2,4),(0.0275681674553505,0.030970763779561,
0.0317834882744106),.UNSPECIFIED.) ;
#815=B_SPLINE_CURVE_WITH_KNOTS('',3,(#73000,#73001,#73002,#73003,#73004,
#73005),.UNSPECIFIED.,.F.,.F.,(4,2,4),(0.0987440670468542,0.102147232218389,
0.102957912598554),.UNSPECIFIED.) ;
#816=B_SPLINE_CURVE_WITH_KNOTS('',3,(#73009,#73010,#73011,#73012,#73013,
#73014,#73015,#73016,#73017,#73018,#73019,#73020),.UNSPECIFIED.,.F.,.F.,
(4,2,2,2,2,4),(0.,0.0061247574437008,0.0140348469016623,0.0236318332037904,
0.0338613775546856,0.0341436529591702),.UNSPECIFIED.) ;
#817=B_SPLINE_CURVE_WITH_KNOTS('',3,(#73023,#73024,#73025,#73026,#73027,
#73028),.UNSPECIFIED.,.F.,.F.,(4,2,4),(0.0275681674553572,0.0309707637795828,
0.0317834882744022),.UNSPECIFIED.) ;
#818=B_SPLINE_CURVE_WITH_KNOTS('',3,(#73031,#73032,#73033,#73034,#73035,
#73036),.UNSPECIFIED.,.F.,.F.,(4,2,4),(0.0987440670462714,0.102147232217851,
0.102957912597979),.UNSPECIFIED.) ;
#819=B_SPLINE_CURVE_WITH_KNOTS('',3,(#73112,#73113,#73114,#73115,#73116,
#73117,#73118,#73119,#73120,#73121,#73122,#73123,#73124,#73125,#73126),
 .UNSPECIFIED.,.F.,.F.,(4,1,1,1,1,1,1,1,1,1,1,1,4),(-1.1546322344665,-1.11356235393268,
-1.07249247339886,-1.05195753313195,-1.03142259286504,-1.02115512273159,
-1.01088765259813,-1.00062018246467,-0.99035271233122,-0.969817772064309,
-0.949282831797399,-0.908212951263578,-0.867143070729775),.UNSPECIFIED.) ;
#820=B_SPLINE_CURVE_WITH_KNOTS('',3,(#73127,#73128,#73129,#73130,#73131,
#73132,#73133,#73134,#73135,#73136,#73137,#73138,#73139,#73140,#73141,#73142,
#73143,#73144,#73145,#73146,#73147,#73148,#73149,#73150,#73151,#73152,#73153,
#73154,#73155,#73156,#73157,#73158,#73159,#73160,#73161,#73162,#73163,#73164,
#73165,#73166,#73167,#73168,#73169,#73170,#73171,#73172,#73173,#73174,#73175,
#73176,#73177,#73178,#73179,#73180,#73181,#73182,#73183,#73184,#73185,#73186,
#73187,#73188,#73189,#73190,#73191,#73192,#73193,#73194,#73195,#73196,#73197,
#73198,#73199,#73200,#73201,#73202,#73203,#73204,#73205,#73206,#73207,#73208,
#73209,#73210,#73211,#73212,#73213,#73214,#73215,#73216,#73217,#73218,#73219,
#73220,#73221,#73222,#73223,#73224,#73225,#73226,#73227,#73228,#73229),
 .UNSPECIFIED.,.F.,.F.,(4,3,3,3,3,3,3,3,3,3,3,3,3,3,3,3,3,3,3,3,3,3,3,3,
3,3,3,3,3,3,3,3,3,3,4),(0.86714307073025,0.883480214507125,0.899207563799762,
0.908212951263578,0.920868221979847,0.933172739853617,0.944935995976013,
0.949282831797399,0.959550301930854,0.968956551813585,0.969817772064309,
0.979310938211651,0.988375034947783,0.99035271233122,0.997960594527763,
1.00062018246467,1.0069704296549,1.01088765259813,1.01719943327265,1.02115512273159,
1.02883039102215,1.03142259286504,1.04051400057577,1.05002380913911,1.05195753313195,
1.06134071109721,1.07113605430996,1.07249247339886,1.08434800851963,1.09656739803681,
1.10928297864463,1.11356235393268,1.12919557822945,1.14545138845601,1.15463223446606),
 .UNSPECIFIED.) ;
#821=B_SPLINE_CURVE_WITH_KNOTS('',3,(#73233,#73234,#73235,#73236,#73237,
#73238,#73239,#73240,#73241,#73242,#73243,#73244),.UNSPECIFIED.,.F.,.F.,
(4,2,2,2,2,4),(0.,0.00612475744371958,0.0140348469017581,0.0236318332039418,
0.0338613775548876,0.034143652959597),.UNSPECIFIED.) ;
#822=B_SPLINE_CURVE_WITH_KNOTS('',3,(#73248,#73249,#73250,#73251,#73252,
#73253,#73254,#73255,#73256,#73257,#73258,#73259,#73260,#73261),
 .UNSPECIFIED.,.F.,.F.,(4,2,2,2,2,2,4),(-0.000285103884839838,0.,0.00872930953208846,
0.0170606390791463,0.0258600808772505,0.0324403480739367,0.0341876342326163),
 .UNSPECIFIED.) ;
#823=B_SPLINE_CURVE_WITH_KNOTS('',3,(#73267,#73268,#73269,#73270,#73271,
#73272,#73273,#73274,#73275,#73276,#73277,#73278,#73279,#73280),
 .UNSPECIFIED.,.F.,.F.,(4,2,2,2,2,2,4),(-0.000285103882893919,6.72676974886044E-15,
0.00872930953393735,0.017060639082469,0.0258600808798638,0.032440348076175,
0.0341876342333578),.UNSPECIFIED.) ;
#824=B_SPLINE_CURVE_WITH_KNOTS('',3,(#73283,#73284,#73285,#73286,#73287,
#73288),.UNSPECIFIED.,.F.,.F.,(4,2,4),(0.0275681674553702,0.0309707637796163,
0.0317834882744124),.UNSPECIFIED.) ;
#825=B_SPLINE_CURVE_WITH_KNOTS('',3,(#73291,#73292,#73293,#73294,#73295,
#73296),.UNSPECIFIED.,.F.,.F.,(4,2,4),(0.0987440670462461,0.102147232217778,
0.102957912597939),.UNSPECIFIED.) ;
#826=B_SPLINE_CURVE_WITH_KNOTS('',3,(#73300,#73301,#73302,#73303,#73304,
#73305,#73306,#73307,#73308,#73309,#73310,#73311),.UNSPECIFIED.,.F.,.F.,
(4,2,2,2,2,4),(0.,0.00612475744372758,0.0140348469017917,0.0236318332039519,
0.0338613775547788,0.0341436529598709),.UNSPECIFIED.) ;
#827=B_SPLINE_CURVE_WITH_KNOTS('',3,(#73314,#73315,#73316,#73317,#73318,
#73319),.UNSPECIFIED.,.F.,.F.,(4,2,4),(0.0275681674553604,0.0309707637795872,
0.0317834882744037),.UNSPECIFIED.) ;
#828=B_SPLINE_CURVE_WITH_KNOTS('',3,(#73322,#73323,#73324,#73325,#73326,
#73327),.UNSPECIFIED.,.F.,.F.,(4,2,4),(0.0987440670453332,0.102147232216817,
0.102957912596973),.UNSPECIFIED.) ;
#829=B_SPLINE_CURVE_WITH_KNOTS('',3,(#73403,#73404,#73405,#73406,#73407,
#73408,#73409,#73410,#73411,#73412,#73413,#73414,#73415,#73416,#73417),
 .UNSPECIFIED.,.F.,.F.,(4,1,1,1,1,1,1,1,1,1,1,1,4),(-0.411832935461112,
-0.37076295018414,-0.329692964907169,-0.309157972268683,-0.298890475949441,
-0.288622979630198,-0.262954238832091,-0.247552994353227,-0.237285498033984,
-0.227018001714741,-0.206483009076255,-0.165413023799284,-0.124343038522328),
 .UNSPECIFIED.) ;
#830=B_SPLINE_CURVE_WITH_KNOTS('',3,(#73418,#73419,#73420,#73421,#73422,
#73423,#73424,#73425,#73426,#73427,#73428,#73429,#73430,#73431,#73432),
 .UNSPECIFIED.,.F.,.F.,(4,1,1,1,1,1,1,1,1,1,1,1,4),(0.124343038522312,0.165413023799283,
0.206483009076254,0.22701800171474,0.237285498033983,0.247552994353225,
0.26295423883209,0.288622979630197,0.29889047594944,0.309157972268682,0.329692964907168,
0.370762950184139,0.411832935461111),.UNSPECIFIED.) ;
#831=B_SPLINE_CURVE_WITH_KNOTS('',3,(#73436,#73437,#73438,#73439,#73440,
#73441,#73442,#73443,#73444,#73445,#73446,#73447),.UNSPECIFIED.,.F.,.F.,
(4,2,2,2,2,4),(0.,0.00612475744370097,0.0140348469016502,0.0236318332037224,
0.0338613775545817,0.0341436529591511),.UNSPECIFIED.) ;
#832=B_SPLINE_CURVE_WITH_KNOTS('',3,(#73451,#73452,#73453,#73454,#73455,
#73456,#73457,#73458,#73459,#73460,#73461,#73462,#73463,#73464),
 .UNSPECIFIED.,.F.,.F.,(4,2,2,2,2,2,4),(-0.00028510389012683,2.52045563239878E-14,
0.00872930952634134,0.0170606390690788,0.0258600808700429,0.0324403480682151,
0.0341876342326173),.UNSPECIFIED.) ;
#833=B_SPLINE_CURVE_WITH_KNOTS('',3,(#73470,#73471,#73472,#73473,#73474,
#73475,#73476,#73477,#73478,#73479,#73480,#73481,#73482,#73483),
 .UNSPECIFIED.,.F.,.F.,(4,2,2,2,2,2,4),(-0.000285103881470846,0.,0.00872930953485893,
0.0170606390840687,0.0258600808810181,0.032440348077114,0.0341876342334867),
 .UNSPECIFIED.) ;
#834=B_SPLINE_CURVE_WITH_KNOTS('',3,(#73486,#73487,#73488,#73489,#73490,
#73491),.UNSPECIFIED.,.F.,.F.,(4,2,4),(0.0275681674553353,0.030970763779553,
0.0317834882743904),.UNSPECIFIED.) ;
#835=B_SPLINE_CURVE_WITH_KNOTS('',3,(#73494,#73495,#73496,#73497,#73498,
#73499),.UNSPECIFIED.,.F.,.F.,(4,2,4),(0.0987440670457375,0.10214723221726,
0.102957912597412),.UNSPECIFIED.) ;
#836=B_SPLINE_CURVE_WITH_KNOTS('',3,(#73503,#73504,#73505,#73506,#73507,
#73508,#73509,#73510,#73511,#73512,#73513,#73514),.UNSPECIFIED.,.F.,.F.,
(4,2,2,2,2,4),(0.,0.00612475744369581,0.014034846901649,0.0236318332038529,
0.0338613775546785,0.0341436529596609),.UNSPECIFIED.) ;
#837=B_SPLINE_CURVE_WITH_KNOTS('',3,(#73517,#73518,#73519,#73520,#73521,
#73522),.UNSPECIFIED.,.F.,.F.,(4,2,4),(0.0275681674554589,0.0309707637797025,
0.0317834882745042),.UNSPECIFIED.) ;
#838=B_SPLINE_CURVE_WITH_KNOTS('',3,(#73525,#73526,#73527,#73528,#73529,
#73530),.UNSPECIFIED.,.F.,.F.,(4,2,4),(0.098744067045831,0.102147232217366,
0.102957912597521),.UNSPECIFIED.) ;
#839=B_SPLINE_CURVE_WITH_KNOTS('',3,(#73606,#73607,#73608,#73609,#73610,
#73611,#73612,#73613,#73614,#73615,#73616,#73617,#73618,#73619,#73620,#73621,
#73622,#73623,#73624,#73625,#73626,#73627,#73628,#73629,#73630,#73631,#73632,
#73633,#73634,#73635,#73636,#73637,#73638,#73639,#73640,#73641,#73642,#73643,
#73644,#73645,#73646,#73647,#73648,#73649,#73650,#73651,#73652,#73653,#73654,
#73655,#73656,#73657,#73658,#73659,#73660,#73661,#73662,#73663,#73664,#73665,
#73666,#73667,#73668,#73669,#73670,#73671,#73672,#73673,#73674,#73675,#73676,
#73677,#73678,#73679,#73680,#73681,#73682,#73683,#73684,#73685,#73686,#73687,
#73688,#73689,#73690,#73691,#73692,#73693),.UNSPECIFIED.,.F.,.F.,(4,3,3,
3,3,3,3,3,3,3,3,3,3,3,3,3,3,3,3,3,3,3,3,3,3,3,3,3,3,4),(-0.477703831735363,
-0.45718942947788,-0.443230571702975,-0.436675027220398,-0.395618819134948,
-0.378433420479109,-0.375082910242375,-0.364812420917539,-0.354540733105092,
-0.350401894405927,-0.348213670695578,-0.345961980835223,-0.341117222395463,
-0.339105573036344,-0.333397647574564,-0.328177881844221,-0.322023234625397,
-0.319864746381625,-0.31340764305829,-0.30560393863315,-0.303146705918973,
-0.298978089352453,-0.292882915418747,-0.273343591995043,-0.272349024384765,
-0.249678001030715,-0.231282775402659,-0.226736096137401,-0.196809892828657,
-0.190214667987186),.UNSPECIFIED.) ;
#840=B_SPLINE_CURVE_WITH_KNOTS('',3,(#73694,#73695,#73696,#73697,#73698,
#73699,#73700,#73701,#73702,#73703,#73704,#73705,#73706,#73707,#73708),
 .UNSPECIFIED.,.F.,.F.,(4,1,1,1,1,1,1,1,1,1,1,1,4),(0.19021466798717,0.231284548522626,
0.272354429058083,0.292889369325811,0.303156839459675,0.313424309593539,
0.339092984928199,0.354494190128995,0.364761660262859,0.375029130396723,
0.395564070664451,0.436633951199908,0.477703831735364),.UNSPECIFIED.) ;
#841=B_SPLINE_CURVE_WITH_KNOTS('',3,(#73712,#73713,#73714,#73715,#73716,
#73717,#73718,#73719,#73720,#73721,#73722,#73723),.UNSPECIFIED.,.F.,.F.,
(4,2,2,2,2,4),(0.,0.0061247574437173,0.0140348469017339,0.0236318332039063,
0.0338613775548282,0.0341436529591761),.UNSPECIFIED.) ;
#842=B_SPLINE_CURVE_WITH_KNOTS('',3,(#73727,#73728,#73729,#73730,#73731,
#73732,#73733,#73734,#73735,#73736,#73737,#73738,#73739,#73740),
 .UNSPECIFIED.,.F.,.F.,(4,2,2,2,2,2,4),(-0.000285103881352186,0.,0.00872930953547832,
0.0170606390851658,0.0258600808817554,0.0324403480776579,0.0341876342332736),
 .UNSPECIFIED.) ;
#843=B_SPLINE_CURVE_WITH_KNOTS('',3,(#73746,#73747,#73748,#73749,#73750,
#73751,#73752,#73753,#73754,#73755,#73756,#73757,#73758,#73759),
 .UNSPECIFIED.,.F.,.F.,(4,2,2,2,2,2,4),(-0.000285103880786882,0.,0.00872930953571026,
0.0170606390855883,0.025860080882109,0.0324403480779487,0.034187634233573),
 .UNSPECIFIED.) ;
#844=B_SPLINE_CURVE_WITH_KNOTS('',3,(#73762,#73763,#73764,#73765,#73766,
#73767),.UNSPECIFIED.,.F.,.F.,(4,2,4),(0.0275681674553793,0.0309707637795965,
0.0317834882744089),.UNSPECIFIED.) ;
#845=B_SPLINE_CURVE_WITH_KNOTS('',3,(#73770,#73771,#73772,#73773,#73774,
#73775),.UNSPECIFIED.,.F.,.F.,(4,2,4),(0.0987440670459561,0.102147232217522,
0.102957912597634),.UNSPECIFIED.) ;
#846=B_SPLINE_CURVE_WITH_KNOTS('',3,(#73779,#73780,#73781,#73782,#73783,
#73784,#73785,#73786,#73787,#73788,#73789,#73790),.UNSPECIFIED.,.F.,.F.,
(4,2,2,2,2,4),(0.,0.00612475744370604,0.0140348469017081,0.0236318332039229,
0.0338613775549312,0.0341436529594248),.UNSPECIFIED.) ;
#847=B_SPLINE_CURVE_WITH_KNOTS('',3,(#73793,#73794,#73795,#73796,#73797,
#73798),.UNSPECIFIED.,.F.,.F.,(4,2,4),(0.0275681674554173,0.0309707637796397,
0.0317834882744546),.UNSPECIFIED.) ;
#848=B_SPLINE_CURVE_WITH_KNOTS('',3,(#73801,#73802,#73803,#73804,#73805,
#73806),.UNSPECIFIED.,.F.,.F.,(4,2,4),(0.0987440670461074,0.102147232217608,
0.10295791259778),.UNSPECIFIED.) ;
#849=B_SPLINE_CURVE_WITH_KNOTS('',3,(#73882,#73883,#73884,#73885,#73886,
#73887,#73888,#73889,#73890,#73891,#73892,#73893,#73894,#73895,#73896,#73897,
#73898,#73899,#73900,#73901,#73902,#73903,#73904,#73905,#73906,#73907,#73908,
#73909,#73910,#73911,#73912,#73913,#73914,#73915,#73916,#73917,#73918,#73919,
#73920,#73921,#73922,#73923,#73924,#73925,#73926,#73927,#73928,#73929,#73930,
#73931,#73932,#73933,#73934,#73935,#73936,#73937,#73938,#73939,#73940,#73941,
#73942,#73943,#73944,#73945,#73946,#73947,#73948,#73949,#73950,#73951,#73952,
#73953,#73954,#73955,#73956,#73957,#73958,#73959,#73960,#73961,#73962,#73963,
#73964,#73965,#73966,#73967,#73968,#73969,#73970,#73971,#73972,#73973,#73974,
#73975,#73976,#73977,#73978,#73979,#73980,#73981,#73982,#73983,#73984),
 .UNSPECIFIED.,.F.,.F.,(4,3,3,3,3,3,3,3,3,3,3,3,3,3,3,3,3,3,3,3,3,3,3,3,
3,3,3,3,3,3,3,3,3,3,4),(-0.886548021255922,-0.855653870250158,-0.85002681972678,
-0.845470505946487,-0.822368676399289,-0.804396442083867,-0.803419323869455,
-0.783862639207905,-0.777784826512195,-0.773600413563503,-0.765740334199066,
-0.763343542875113,-0.756898169483182,-0.750967673087341,-0.748585034020608,
-0.742943881897718,-0.742232977096396,-0.737660156503543,-0.73633705638255,
-0.730852789241292,-0.727476816747186,-0.722234803402179,-0.714862413628147,
-0.70697932438281,-0.704984345704348,-0.69423844792319,-0.682180041289652,
-0.681161690517635,-0.676013453381874,-0.67141001865358,-0.670871987902952,
-0.64753741444397,-0.64008354109392,-0.619305464344901,-0.599057470751608),
 .UNSPECIFIED.) ;
#850=B_SPLINE_CURVE_WITH_KNOTS('',3,(#73985,#73986,#73987,#73988,#73989,
#73990,#73991,#73992,#73993,#73994,#73995,#73996,#73997,#73998,#73999),
 .UNSPECIFIED.,.F.,.F.,(4,1,1,1,1,1,1,1,1,1,1,1,4),(0.599057470748756,0.640127549392637,
0.670930108375547,0.676063868206032,0.681197628036518,0.722267706680398,
0.737668986171854,0.763337785324279,0.77360530498525,0.78387282464622,0.80440786396816,
0.845477942612041,0.886548021255922),.UNSPECIFIED.) ;
#851=B_SPLINE_CURVE_WITH_KNOTS('',3,(#74003,#74004,#74005,#74006,#74007,
#74008,#74009,#74010,#74011,#74012,#74013,#74014),.UNSPECIFIED.,.F.,.F.,
(4,2,2,2,2,4),(0.,0.00612475744371223,0.0140348469017155,0.0236318332039426,
0.0338613775549202,0.0341436529594837),.UNSPECIFIED.) ;
#852=B_SPLINE_CURVE_WITH_KNOTS('',3,(#74018,#74019,#74020,#74021,#74022,
#74023,#74024,#74025,#74026,#74027,#74028,#74029,#74030,#74031),
 .UNSPECIFIED.,.F.,.F.,(4,2,2,2,2,2,4),(-0.000285103883765505,0.,0.00872930953291526,
0.0170606390807207,0.0258600808785664,0.0324403480751399,0.0341876342333296),
 .UNSPECIFIED.) ;
#853=B_SPLINE_CURVE_WITH_KNOTS('',3,(#74037,#74038,#74039,#74040,#74041,
#74042,#74043,#74044,#74045,#74046,#74047,#74048,#74049,#74050),
 .UNSPECIFIED.,.F.,.F.,(4,2,2,2,2,2,4),(-0.000285103876031147,0.,0.00872930954136664,
0.0170606390955509,0.0258600808893367,0.0324403480837712,0.0341876342338359),
 .UNSPECIFIED.) ;
#854=B_SPLINE_CURVE_WITH_KNOTS('',3,(#74053,#74054,#74055,#74056,#74057,
#74058),.UNSPECIFIED.,.F.,.F.,(4,2,4),(0.0275681674554096,0.0309707637796443,
0.0317834882744809),.UNSPECIFIED.) ;
#855=B_SPLINE_CURVE_WITH_KNOTS('',3,(#74061,#74062,#74063,#74064,#74065,
#74066),.UNSPECIFIED.,.F.,.F.,(4,2,4),(0.0987440670458425,0.102147232217394,
0.102957912597541),.UNSPECIFIED.) ;
#856=B_SPLINE_CURVE_WITH_KNOTS('',3,(#74070,#74071,#74072,#74073,#74074,
#74075,#74076,#74077,#74078,#74079,#74080,#74081),.UNSPECIFIED.,.F.,.F.,
(4,2,2,2,2,4),(0.,0.00612475744370653,0.014034846901692,0.0236318332038886,
0.0338613775548516,0.0341436529594063),.UNSPECIFIED.) ;
#857=B_SPLINE_CURVE_WITH_KNOTS('',3,(#74084,#74085,#74086,#74087,#74088,
#74089),.UNSPECIFIED.,.F.,.F.,(4,2,4),(0.0275681674553618,0.0309707637795795,
0.0317834882744105),.UNSPECIFIED.) ;
#858=B_SPLINE_CURVE_WITH_KNOTS('',3,(#74092,#74093,#74094,#74095,#74096,
#74097),.UNSPECIFIED.,.F.,.F.,(4,2,4),(0.0987440670458198,0.102147232217339,
0.102957912597487),.UNSPECIFIED.) ;
#859=B_SPLINE_CURVE_WITH_KNOTS('',3,(#74168,#74169,#74170,#74171,#74172,
#74173,#74174,#74175,#74176,#74177,#74178,#74179,#74180,#74181,#74182,#74183,
#74184,#74185,#74186,#74187,#74188,#74189,#74190,#74191,#74192,#74193,#74194,
#74195,#74196,#74197,#74198,#74199,#74200,#74201,#74202,#74203,#74204,#74205,
#74206,#74207,#74208,#74209,#74210,#74211,#74212,#74213,#74214,#74215,#74216,
#74217,#74218,#74219,#74220,#74221,#74222,#74223,#74224,#74225,#74226,#74227,
#74228,#74229,#74230,#74231,#74232,#74233,#74234,#74235,#74236,#74237,#74238,
#74239,#74240,#74241,#74242,#74243,#74244,#74245,#74246,#74247,#74248,#74249,
#74250,#74251,#74252,#74253,#74254,#74255,#74256,#74257,#74258,#74259,#74260,
#74261,#74262,#74263,#74264,#74265,#74266,#74267,#74268,#74269,#74270,#74271,
#74272,#74273,#74274,#74275,#74276,#74277,#74278,#74279),.UNSPECIFIED.,
 .F.,.F.,(4,3,3,3,3,3,3,3,3,3,3,3,3,3,3,3,3,3,3,3,3,3,3,3,3,3,3,3,3,3,3,
3,3,3,3,3,3,4),(-0.886548021255907,-0.863182318004303,-0.850026819727067,
-0.845485030967072,-0.828031061920953,-0.823989441594979,-0.807948605086144,
-0.804397368521845,-0.803419323869594,-0.789454474081531,-0.787196805980162,
-0.783854551717749,-0.777784826512269,-0.768896090894216,-0.763303764436096,
-0.75689816948318,-0.749793121745379,-0.748585034020595,-0.742232977096377,
-0.736711329196858,-0.736337056382526,-0.732525887314632,-0.727476816747158,
-0.722225282270684,-0.714704266959016,-0.711963500330866,-0.704984345704295,
-0.701694385768342,-0.687771408069272,-0.681167670056181,-0.671410018653506,
-0.660643577981008,-0.641874313618654,-0.639974521162902,-0.620382690534388,
-0.619305464344796,-0.602967398208329,-0.599057470751573),.UNSPECIFIED.) ;
#860=B_SPLINE_CURVE_WITH_KNOTS('',3,(#74280,#74281,#74282,#74283,#74284,
#74285,#74286,#74287,#74288,#74289,#74290,#74291,#74292,#74293),
 .UNSPECIFIED.,.F.,.F.,(4,1,1,1,1,1,1,1,1,1,1,4),(0.59905747074872,0.660662588714547,
0.681197628036489,0.701732667358431,0.712000187019402,0.722267706680373,
0.732535226341344,0.763337785324257,0.783872824646199,0.804407863968141,
0.845477942612025,0.886548021255909),.UNSPECIFIED.) ;
#861=B_SPLINE_CURVE_WITH_KNOTS('',3,(#74297,#74298,#74299,#74300,#74301,
#74302,#74303,#74304,#74305,#74306,#74307,#74308),.UNSPECIFIED.,.F.,.F.,
(4,2,2,2,2,4),(0.,0.00612475744372648,0.0140348469017703,0.0236318332038679,
0.0338613775547147,0.0341436529599871),.UNSPECIFIED.) ;
#862=B_SPLINE_CURVE_WITH_KNOTS('',3,(#74312,#74313,#74314,#74315,#74316,
#74317,#74318,#74319,#74320,#74321,#74322,#74323,#74324,#74325),
 .UNSPECIFIED.,.F.,.F.,(4,2,2,2,2,2,4),(-0.000285103885038181,0.,0.00872930953219139,
0.0170606390794635,0.0258600808776587,0.0324403480744031,0.0341876342331678),
 .UNSPECIFIED.) ;
#863=B_SPLINE_CURVE_WITH_KNOTS('',3,(#74331,#74332,#74333,#74334,#74335,
#74336,#74337,#74338,#74339,#74340,#74341,#74342,#74343,#74344),
 .UNSPECIFIED.,.F.,.F.,(4,2,2,2,2,2,4),(-0.000285103884159099,0.,0.00872930953339573,
0.0170606390816542,0.0258600808793018,0.0324403480757735,0.0341876342333799),
 .UNSPECIFIED.) ;
#864=B_SPLINE_CURVE_WITH_KNOTS('',3,(#74347,#74348,#74349,#74350,#74351,
#74352),.UNSPECIFIED.,.F.,.F.,(4,2,4),(0.0275681674553244,0.0309707637795474,
0.0317834882743744),.UNSPECIFIED.) ;
#865=B_SPLINE_CURVE_WITH_KNOTS('',3,(#74355,#74356,#74357,#74358,#74359,
#74360),.UNSPECIFIED.,.F.,.F.,(4,2,4),(0.0987440670455209,0.10214723221702,
0.102957912597177),.UNSPECIFIED.) ;
#866=B_SPLINE_CURVE_WITH_KNOTS('',3,(#74364,#74365,#74366,#74367,#74368,
#74369,#74370,#74371,#74372,#74373,#74374,#74375),.UNSPECIFIED.,.F.,.F.,
(4,2,2,2,2,4),(0.,0.00612475744370874,0.0140348469017083,0.0236318332038301,
0.0338613775547143,0.0341436529591838),.UNSPECIFIED.) ;
#867=B_SPLINE_CURVE_WITH_KNOTS('',3,(#74378,#74379,#74380,#74381,#74382,
#74383),.UNSPECIFIED.,.F.,.F.,(4,2,4),(0.0275681674553622,0.0309707637796043,
0.0317834882744653),.UNSPECIFIED.) ;
#868=B_SPLINE_CURVE_WITH_KNOTS('',3,(#74386,#74387,#74388,#74389,#74390,
#74391),.UNSPECIFIED.,.F.,.F.,(4,2,4),(0.0987440670462907,0.102147232217805,
0.102957912597974),.UNSPECIFIED.) ;
#869=B_SPLINE_CURVE_WITH_KNOTS('',3,(#74467,#74468,#74469,#74470,#74471,
#74472,#74473,#74474,#74475,#74476,#74477,#74478,#74479,#74480,#74481,#74482,
#74483,#74484,#74485,#74486,#74487,#74488,#74489,#74490,#74491,#74492,#74493,
#74494,#74495,#74496,#74497,#74498,#74499,#74500,#74501,#74502,#74503,#74504,
#74505,#74506,#74507,#74508,#74509,#74510,#74511,#74512,#74513,#74514,#74515,
#74516,#74517,#74518,#74519,#74520,#74521,#74522,#74523,#74524,#74525,#74526,
#74527,#74528,#74529,#74530,#74531,#74532,#74533,#74534,#74535,#74536,#74537,
#74538,#74539,#74540,#74541,#74542,#74543,#74544,#74545,#74546,#74547,#74548,
#74549,#74550,#74551,#74552,#74553,#74554),.UNSPECIFIED.,.F.,.F.,(4,3,3,
3,3,3,3,3,3,3,3,3,3,3,3,3,3,3,3,3,3,3,3,3,3,3,3,3,3,4),(-1.15463223446657,
-1.13411784956101,-1.12022914538744,-1.11360346465544,-1.07254724042576,
-1.05201131155961,-1.04611218888535,-1.04174082602754,-1.03146914587479,
-1.02708078581791,-1.02476147151778,-1.02289044034752,-1.01804574952196,
-1.01603399648863,-1.01032623594513,-1.00510701775931,-0.998952781220051,
-0.996793882296726,-0.990336093963219,-0.982532274474594,-0.980075166341655,
-0.975907225267658,-0.969811380724416,-0.950272727910345,-0.949277511016964,
-0.926594285022028,-0.908211282780506,-0.903665232052903,-0.873532453171296,
-0.867143070761121),.UNSPECIFIED.) ;
#870=B_SPLINE_CURVE_WITH_KNOTS('',3,(#74555,#74556,#74557,#74558,#74559,
#74560,#74561,#74562,#74563,#74564,#74565,#74566,#74567,#74568,#74569),
 .UNSPECIFIED.,.F.,.F.,(4,1,1,1,1,1,1,1,1,1,1,1,4),(0.867143070761104,0.908212951290456,
0.949282831819809,0.969817772084486,0.980085242216824,0.990352712349162,
1.01602138768001,1.03142259287851,1.04169006301085,1.05195753314319,1.07249247340787,
1.11356235393722,1.15463223446657),.UNSPECIFIED.) ;
#871=B_SPLINE_CURVE_WITH_KNOTS('',3,(#74573,#74574,#74575,#74576,#74577,
#74578,#74579,#74580,#74581,#74582,#74583,#74584),.UNSPECIFIED.,.F.,.F.,
(4,2,2,2,2,4),(0.,0.0061247574437176,0.0140348469017413,0.02363183320368,
0.0338613775544456,0.0341436529587641),.UNSPECIFIED.) ;
#872=B_SPLINE_CURVE_WITH_KNOTS('',3,(#74588,#74589,#74590,#74591,#74592,
#74593,#74594,#74595,#74596,#74597,#74598,#74599,#74600,#74601),
 .UNSPECIFIED.,.F.,.F.,(4,2,2,2,2,2,4),(-0.000285103884421192,0.,0.00872930953257869,
0.0170606390801584,0.0258600808781175,0.0324403480747261,0.0341876342330866),
 .UNSPECIFIED.) ;
#873=B_SPLINE_CURVE_WITH_KNOTS('',3,(#74607,#74608,#74609,#74610,#74611,
#74612,#74613,#74614,#74615,#74616,#74617,#74618,#74619,#74620),
 .UNSPECIFIED.,.F.,.F.,(4,2,2,2,2,2,4),(-0.000285103889744773,0.,0.00872930952671932,
0.0170606390697499,0.0258600808702053,0.0324403480681302,0.0341876342317),
 .UNSPECIFIED.) ;
#874=B_SPLINE_CURVE_WITH_KNOTS('',3,(#74623,#74624,#74625,#74626,#74627,
#74628),.UNSPECIFIED.,.F.,.F.,(4,2,4),(0.0275681674553669,0.0309707637795839,
0.0317834882744089),.UNSPECIFIED.) ;
#875=B_SPLINE_CURVE_WITH_KNOTS('',3,(#74631,#74632,#74633,#74634,#74635,
#74636),.UNSPECIFIED.,.F.,.F.,(4,2,4),(0.0987440670462967,0.102147232217882,
0.102957912598016),.UNSPECIFIED.) ;
#876=B_SPLINE_CURVE_WITH_KNOTS('',3,(#74640,#74641,#74642,#74643,#74644,
#74645,#74646,#74647,#74648,#74649,#74650,#74651),.UNSPECIFIED.,.F.,.F.,
(4,2,2,2,2,4),(0.,0.00612475744371255,0.0140348469017152,0.0236318332037933,
0.0338613775546911,0.0341436529587335),.UNSPECIFIED.) ;
#877=B_SPLINE_CURVE_WITH_KNOTS('',3,(#74654,#74655,#74656,#74657,#74658,
#74659),.UNSPECIFIED.,.F.,.F.,(4,2,4),(0.0275681674553678,0.0309707637795747,
0.031783488274427),.UNSPECIFIED.) ;
#878=B_SPLINE_CURVE_WITH_KNOTS('',3,(#74662,#74663,#74664,#74665,#74666,
#74667),.UNSPECIFIED.,.F.,.F.,(4,2,4),(0.0987440670465932,0.102147232218164,
0.102957912598333),.UNSPECIFIED.) ;
#879=B_SPLINE_CURVE_WITH_KNOTS('',3,(#74743,#74744,#74745,#74746,#74747,
#74748,#74749,#74750,#74751,#74752,#74753,#74754,#74755,#74756,#74757),
 .UNSPECIFIED.,.F.,.F.,(4,1,1,1,1,1,1,1,1,1,1,1,4),(-0.411832935461185,
-0.37076295018422,-0.32969296490725,-0.309157972268765,-0.298890475949523,
-0.28862297963028,-0.273221735151417,-0.247552994353311,-0.237285498034068,
-0.227018001714826,-0.206483009076341,-0.165413023799371,-0.124343038522417),
 .UNSPECIFIED.) ;
#880=B_SPLINE_CURVE_WITH_KNOTS('',3,(#74758,#74759,#74760,#74761,#74762,
#74763,#74764,#74765,#74766,#74767,#74768,#74769,#74770,#74771,#74772),
 .UNSPECIFIED.,.F.,.F.,(4,1,1,1,1,1,1,1,1,1,1,1,4),(0.1243430385224,0.165413023799369,
0.206483009076339,0.227018001714824,0.237285498034067,0.247552994353309,
0.273221735151415,0.288622979630279,0.298890475949521,0.309157972268764,
0.329692964907249,0.370762950184219,0.411832935461188),.UNSPECIFIED.) ;
#881=B_SPLINE_CURVE_WITH_KNOTS('',3,(#74776,#74777,#74778,#74779,#74780,
#74781,#74782,#74783,#74784,#74785,#74786,#74787),.UNSPECIFIED.,.F.,.F.,
(4,2,2,2,2,4),(0.,0.00612475744369689,0.0140348469016405,0.0236318332037292,
0.0338613775545991,0.0341436529587365),.UNSPECIFIED.) ;
#882=B_SPLINE_CURVE_WITH_KNOTS('',3,(#74791,#74792,#74793,#74794,#74795,
#74796,#74797,#74798,#74799,#74800,#74801,#74802,#74803,#74804),
 .UNSPECIFIED.,.F.,.F.,(4,2,2,2,2,2,4),(-0.000285103884298923,0.,0.00872930953326711,
0.0170606390812955,0.0258600808788128,0.0324403480752013,0.0341876342326143),
 .UNSPECIFIED.) ;
#883=B_SPLINE_CURVE_WITH_KNOTS('',3,(#74810,#74811,#74812,#74813,#74814,
#74815,#74816,#74817,#74818,#74819,#74820,#74821,#74822,#74823),
 .UNSPECIFIED.,.F.,.F.,(4,2,2,2,2,2,4),(-0.000285103883452685,0.,0.00872930953447474,
0.0170606390835385,0.0258600808807064,0.0324403480769824,0.0341876342336455),
 .UNSPECIFIED.) ;
#884=B_SPLINE_CURVE_WITH_KNOTS('',3,(#74826,#74827,#74828,#74829,#74830,
#74831),.UNSPECIFIED.,.F.,.F.,(4,2,4),(0.027568167455528,0.0309707637797636,
0.0317834882746252),.UNSPECIFIED.) ;
#885=B_SPLINE_CURVE_WITH_KNOTS('',3,(#74834,#74835,#74836,#74837,#74838,
#74839),.UNSPECIFIED.,.F.,.F.,(4,2,4),(0.0987440670463977,0.10214723221798,
0.102957912598135),.UNSPECIFIED.) ;
#886=B_SPLINE_CURVE_WITH_KNOTS('',3,(#74843,#74844,#74845,#74846,#74847,
#74848,#74849,#74850,#74851,#74852,#74853,#74854),.UNSPECIFIED.,.F.,.F.,
(4,2,2,2,2,4),(0.,0.00612475744370791,0.0140348469017071,0.0236318332038692,
0.0338613775547471,0.0341436529596501),.UNSPECIFIED.) ;
#887=B_SPLINE_CURVE_WITH_KNOTS('',3,(#74857,#74858,#74859,#74860,#74861,
#74862),.UNSPECIFIED.,.F.,.F.,(4,2,4),(0.0275681674553135,0.0309707637795262,
0.0317834882743389),.UNSPECIFIED.) ;
#888=B_SPLINE_CURVE_WITH_KNOTS('',3,(#74865,#74866,#74867,#74868,#74869,
#74870),.UNSPECIFIED.,.F.,.F.,(4,2,4),(0.0987440670454317,0.102147232216938,
0.102957912597103),.UNSPECIFIED.) ;
#889=B_SPLINE_CURVE_WITH_KNOTS('',3,(#74946,#74947,#74948,#74949,#74950,
#74951,#74952,#74953,#74954,#74955,#74956,#74957,#74958,#74959,#74960,#74961,
#74962,#74963,#74964,#74965,#74966,#74967,#74968,#74969,#74970,#74971,#74972,
#74973,#74974,#74975,#74976,#74977,#74978,#74979,#74980,#74981,#74982,#74983,
#74984,#74985,#74986,#74987,#74988,#74989,#74990,#74991,#74992,#74993,#74994,
#74995,#74996,#74997,#74998,#74999,#75000,#75001,#75002,#75003,#75004,#75005,
#75006,#75007,#75008,#75009,#75010,#75011,#75012,#75013,#75014,#75015,#75016,
#75017,#75018,#75019,#75020,#75021,#75022,#75023,#75024,#75025,#75026,#75027,
#75028,#75029,#75030,#75031,#75032,#75033,#75034,#75035,#75036),
 .UNSPECIFIED.,.F.,.F.,(4,3,3,3,3,3,3,3,3,3,3,3,3,3,3,3,3,3,3,3,3,3,3,3,
3,3,3,3,3,3,4),(-0.477703831735242,-0.457189426261555,-0.443230506420269,
-0.436675020787869,-0.395618810128837,-0.378433299612694,-0.375082901246212,
-0.369185298823285,-0.364812412641861,-0.354540726183523,-0.350401889199105,
-0.348213658304538,-0.345961981360179,-0.341117226356061,-0.339105569093216,
-0.333397648976201,-0.328177881844107,-0.322023347030127,-0.319864746381521,
-0.313407644934347,-0.305604024516391,-0.30314670890323,-0.29897808935244,
-0.292882919054629,-0.273343591995118,-0.272349028370288,-0.249678041716392,
-0.231282777755435,-0.22673609613766,-0.196809574226464,-0.190214667985449),
 .UNSPECIFIED.) ;
#890=B_SPLINE_CURVE_WITH_KNOTS('',3,(#75037,#75038,#75039,#75040,#75041,
#75042,#75043,#75044,#75045,#75046,#75047,#75048,#75049,#75050,#75051),
 .UNSPECIFIED.,.F.,.F.,(4,1,1,1,1,1,1,1,1,1,1,1,4),(0.190214667985433,0.23128454852112,
0.272354429056807,0.29288936932465,0.303156839458572,0.313424309592494,
0.339092984927298,0.354494190128181,0.364761660262103,0.375029130396024,
0.395564070663868,0.436633951199555,0.477703831735242),.UNSPECIFIED.) ;
#891=B_SPLINE_CURVE_WITH_KNOTS('',3,(#75055,#75056,#75057,#75058,#75059,
#75060,#75061,#75062,#75063,#75064,#75065,#75066),.UNSPECIFIED.,.F.,.F.,
(4,2,2,2,2,4),(0.,0.00612475744370239,0.0140348469016695,0.0236318332040214,
0.0338613775551618,0.0341436529601212),.UNSPECIFIED.) ;
#892=B_SPLINE_CURVE_WITH_KNOTS('',3,(#75070,#75071,#75072,#75073,#75074,
#75075,#75076,#75077,#75078,#75079,#75080,#75081,#75082,#75083),
 .UNSPECIFIED.,.F.,.F.,(4,2,2,2,2,2,4),(-0.000285103889775932,0.,0.00872930952735993,
0.0170606390708911,0.0258600808712746,0.0324403480691489,0.0341876342324684),
 .UNSPECIFIED.) ;
#893=B_SPLINE_CURVE_WITH_KNOTS('',3,(#75086,#75087,#75088,#75089,#75090,
#75091),.UNSPECIFIED.,.F.,.F.,(4,2,4),(0.0275681674554672,0.0309707637796864,
0.031783488274549),.UNSPECIFIED.) ;
#894=B_SPLINE_CURVE_WITH_KNOTS('',3,(#75094,#75095,#75096,#75097,#75098,
#75099),.UNSPECIFIED.,.F.,.F.,(4,2,4),(0.0987440670467281,0.102147232218267,
0.102957912598433),.UNSPECIFIED.) ;
#1769=B_SPLINE_SURFACE_WITH_KNOTS('',3,3,((#70269,#70270,#70271,#70272,
#70273,#70274,#70275,#70276,#70277,#70278,#70279,#70280,#70281,#70282,#70283),
(#70284,#70285,#70286,#70287,#70288,#70289,#70290,#70291,#70292,#70293,
#70294,#70295,#70296,#70297,#70298),(#70299,#70300,#70301,#70302,#70303,
#70304,#70305,#70306,#70307,#70308,#70309,#70310,#70311,#70312,#70313),
(#70314,#70315,#70316,#70317,#70318,#70319,#70320,#70321,#70322,#70323,
#70324,#70325,#70326,#70327,#70328),(#70329,#70330,#70331,#70332,#70333,
#70334,#70335,#70336,#70337,#70338,#70339,#70340,#70341,#70342,#70343)),
 .UNSPECIFIED.,.F.,.F.,.F.,(4,1,4),(4,1,1,1,1,1,1,1,1,1,1,1,4),(-0.000196888981062193,
0.571428571428571,1.),(0.598860581847638,0.640127549392609,0.681197628036496,
0.701732667358439,0.722267706680382,0.732535226341353,0.742802746002325,
0.753070265663297,0.763337785324268,0.783872824646211,0.804407863968155,
0.845477942612041,0.886744910236546),.UNSPECIFIED.) ;
#1770=B_SPLINE_SURFACE_WITH_KNOTS('',3,3,((#70561,#70562,#70563,#70564,
#70565,#70566,#70567,#70568,#70569,#70570,#70571,#70572,#70573,#70574,#70575),
(#70576,#70577,#70578,#70579,#70580,#70581,#70582,#70583,#70584,#70585,
#70586,#70587,#70588,#70589,#70590),(#70591,#70592,#70593,#70594,#70595,
#70596,#70597,#70598,#70599,#70600,#70601,#70602,#70603,#70604,#70605),
(#70606,#70607,#70608,#70609,#70610,#70611,#70612,#70613,#70614,#70615,
#70616,#70617,#70618,#70619,#70620),(#70621,#70622,#70623,#70624,#70625,
#70626,#70627,#70628,#70629,#70630,#70631,#70632,#70633,#70634,#70635)),
 .UNSPECIFIED.,.F.,.F.,.F.,(4,1,4),(4,1,1,1,1,1,1,1,1,1,1,1,4),(0.,0.571428571428571,
1.),(0.599057470748727,0.64012754939261,0.681197628036493,0.701732667358435,
0.712000187019406,0.722267706680377,0.747936505832804,0.76333778532426,
0.804407863968143,0.809541623798628,0.814675383629114,0.845477942612026,
0.886548021255909),.UNSPECIFIED.) ;
#1771=B_SPLINE_SURFACE_WITH_KNOTS('',3,3,((#70780,#70781,#70782,#70783,
#70784,#70785,#70786,#70787,#70788,#70789,#70790,#70791,#70792,#70793,#70794),
(#70795,#70796,#70797,#70798,#70799,#70800,#70801,#70802,#70803,#70804,
#70805,#70806,#70807,#70808,#70809),(#70810,#70811,#70812,#70813,#70814,
#70815,#70816,#70817,#70818,#70819,#70820,#70821,#70822,#70823,#70824),
(#70825,#70826,#70827,#70828,#70829,#70830,#70831,#70832,#70833,#70834,
#70835,#70836,#70837,#70838,#70839),(#70840,#70841,#70842,#70843,#70844,
#70845,#70846,#70847,#70848,#70849,#70850,#70851,#70852,#70853,#70854)),
 .UNSPECIFIED.,.F.,.F.,.F.,(4,1,4),(4,1,1,1,1,1,1,1,1,1,1,1,4),(-0.000196404178126319,
0.571428571428571,1.),(0.866946666522881,0.908212951238937,0.949282831776868,
0.969817772045833,0.990352712314798,1.00062018244928,1.01088765258376,1.02115512271825,
1.03142259285273,1.05195753312169,1.07249247339066,1.11356235392859,1.15482863864465),
 .UNSPECIFIED.) ;
#1772=B_SPLINE_SURFACE_WITH_KNOTS('',3,3,((#70999,#71000,#71001,#71002,
#71003,#71004,#71005,#71006,#71007,#71008,#71009,#71010,#71011,#71012,#71013),
(#71014,#71015,#71016,#71017,#71018,#71019,#71020,#71021,#71022,#71023,
#71024,#71025,#71026,#71027,#71028),(#71029,#71030,#71031,#71032,#71033,
#71034,#71035,#71036,#71037,#71038,#71039,#71040,#71041,#71042,#71043),
(#71044,#71045,#71046,#71047,#71048,#71049,#71050,#71051,#71052,#71053,
#71054,#71055,#71056,#71057,#71058),(#71059,#71060,#71061,#71062,#71063,
#71064,#71065,#71066,#71067,#71068,#71069,#71070,#71071,#71072,#71073)),
 .UNSPECIFIED.,.F.,.F.,.F.,(4,1,4),(4,1,1,1,1,1,1,1,1,1,1,1,4),(-0.000196418998065374,
0.571428571428571,1.),(0.124146619524486,0.165413023799523,0.206483009076495,
0.227018001714981,0.247552994353466,0.257820490672709,0.268087986991952,
0.278355483311195,0.288622979630438,0.309157972268924,0.32969296490741,
0.370762950184382,0.412029354459418),.UNSPECIFIED.) ;
#1773=B_SPLINE_SURFACE_WITH_KNOTS('',3,3,((#71223,#71224,#71225,#71226,
#71227,#71228,#71229,#71230,#71231,#71232,#71233,#71234,#71235,#71236),
(#71237,#71238,#71239,#71240,#71241,#71242,#71243,#71244,#71245,#71246,
#71247,#71248,#71249,#71250),(#71251,#71252,#71253,#71254,#71255,#71256,
#71257,#71258,#71259,#71260,#71261,#71262,#71263,#71264),(#71265,#71266,
#71267,#71268,#71269,#71270,#71271,#71272,#71273,#71274,#71275,#71276,#71277,
#71278),(#71279,#71280,#71281,#71282,#71283,#71284,#71285,#71286,#71287,
#71288,#71289,#71290,#71291,#71292)),.UNSPECIFIED.,.F.,.F.,.F.,(4,1,4),
(4,1,1,1,1,1,1,1,1,1,1,4),(0.,0.571428571428571,1.),(0.190214667974634,
0.251819488780472,0.272354429049085,0.292889369317698,0.303156839452004,
0.313424309586311,0.323691779720617,0.354494190123537,0.375029130392149,
0.395564070660762,0.436633951197988,0.477703831735214),.UNSPECIFIED.) ;
#1774=B_SPLINE_SURFACE_WITH_KNOTS('',3,3,((#71451,#71452,#71453,#71454,
#71455,#71456,#71457,#71458,#71459,#71460,#71461,#71462,#71463,#71464,#71465),
(#71466,#71467,#71468,#71469,#71470,#71471,#71472,#71473,#71474,#71475,
#71476,#71477,#71478,#71479,#71480),(#71481,#71482,#71483,#71484,#71485,
#71486,#71487,#71488,#71489,#71490,#71491,#71492,#71493,#71494,#71495),
(#71496,#71497,#71498,#71499,#71500,#71501,#71502,#71503,#71504,#71505,
#71506,#71507,#71508,#71509,#71510),(#71511,#71512,#71513,#71514,#71515,
#71516,#71517,#71518,#71519,#71520,#71521,#71522,#71523,#71524,#71525)),
 .UNSPECIFIED.,.F.,.F.,.F.,(4,1,4),(4,1,1,1,1,1,1,1,1,1,1,1,4),(0.,0.571428571428571,
1.),(0.599057470748751,0.640127549392634,0.681197628036517,0.701732667358458,
0.712000187019429,0.7222677066804,0.747936505832826,0.763337785324282,0.804407863968165,
0.80954162379865,0.814675383629136,0.845477942612048,0.88654802125593),
 .UNSPECIFIED.) ;
#1775=B_SPLINE_SURFACE_WITH_KNOTS('',3,3,((#71670,#71671,#71672,#71673,
#71674,#71675,#71676,#71677,#71678,#71679,#71680,#71681,#71682,#71683,#71684),
(#71685,#71686,#71687,#71688,#71689,#71690,#71691,#71692,#71693,#71694,
#71695,#71696,#71697,#71698,#71699),(#71700,#71701,#71702,#71703,#71704,
#71705,#71706,#71707,#71708,#71709,#71710,#71711,#71712,#71713,#71714),
(#71715,#71716,#71717,#71718,#71719,#71720,#71721,#71722,#71723,#71724,
#71725,#71726,#71727,#71728,#71729),(#71730,#71731,#71732,#71733,#71734,
#71735,#71736,#71737,#71738,#71739,#71740,#71741,#71742,#71743,#71744)),
 .UNSPECIFIED.,.F.,.F.,.F.,(4,1,4),(4,1,1,1,1,1,1,1,1,1,1,1,4),(0.,0.571428571428571,
1.),(0.599057470748744,0.640127549392629,0.681197628036513,0.701732667358455,
0.712000187019426,0.722267706680398,0.747936505832825,0.763337785324282,
0.804407863968166,0.809541623798652,0.814675383629137,0.84547794261205,
0.886548021255935),.UNSPECIFIED.) ;
#1776=B_SPLINE_SURFACE_WITH_KNOTS('',3,3,((#71889,#71890,#71891,#71892,
#71893,#71894,#71895,#71896,#71897,#71898,#71899,#71900,#71901,#71902,#71903),
(#71904,#71905,#71906,#71907,#71908,#71909,#71910,#71911,#71912,#71913,
#71914,#71915,#71916,#71917,#71918),(#71919,#71920,#71921,#71922,#71923,
#71924,#71925,#71926,#71927,#71928,#71929,#71930,#71931,#71932,#71933),
(#71934,#71935,#71936,#71937,#71938,#71939,#71940,#71941,#71942,#71943,
#71944,#71945,#71946,#71947,#71948),(#71949,#71950,#71951,#71952,#71953,
#71954,#71955,#71956,#71957,#71958,#71959,#71960,#71961,#71962,#71963)),
 .UNSPECIFIED.,.F.,.F.,.F.,(4,1,4),(4,1,1,1,1,1,1,1,1,1,1,1,4),(0.,0.571428571428571,
1.),(0.867143070669756,0.908212951212153,0.949282831754549,0.969817772025747,
0.980085242161346,0.990352712296945,1.01602138763594,1.03142259283934,1.04169006297494,
1.05195753311054,1.07249247338174,1.11356235392413,1.15463223446653),
 .UNSPECIFIED.) ;
#1777=B_SPLINE_SURFACE_WITH_KNOTS('',3,3,((#72096,#72097,#72098,#72099,
#72100,#72101,#72102,#72103,#72104,#72105,#72106,#72107,#72108,#72109,#72110),
(#72111,#72112,#72113,#72114,#72115,#72116,#72117,#72118,#72119,#72120,
#72121,#72122,#72123,#72124,#72125),(#72126,#72127,#72128,#72129,#72130,
#72131,#72132,#72133,#72134,#72135,#72136,#72137,#72138,#72139,#72140),
(#72141,#72142,#72143,#72144,#72145,#72146,#72147,#72148,#72149,#72150,
#72151,#72152,#72153,#72154,#72155),(#72156,#72157,#72158,#72159,#72160,
#72161,#72162,#72163,#72164,#72165,#72166,#72167,#72168,#72169,#72170)),
 .UNSPECIFIED.,.F.,.F.,.F.,(4,1,4),(4,1,1,1,1,1,1,1,1,1,1,1,4),(0.,0.571428571428571,
1.),(0.124343038522454,0.165413023799424,0.206483009076393,0.227018001714878,
0.23728549803412,0.247552994353363,0.273221735151469,0.288622979630332,
0.298890475949574,0.309157972268817,0.329692964907302,0.370762950184271,
0.41183293546124),.UNSPECIFIED.) ;
#1778=B_SPLINE_SURFACE_WITH_KNOTS('',3,3,((#72221,#72222,#72223,#72224,
#72225,#72226,#72227,#72228,#72229,#72230,#72231,#72232,#72233,#72234,#72235),
(#72236,#72237,#72238,#72239,#72240,#72241,#72242,#72243,#72244,#72245,
#72246,#72247,#72248,#72249,#72250),(#72251,#72252,#72253,#72254,#72255,
#72256,#72257,#72258,#72259,#72260,#72261,#72262,#72263,#72264,#72265),
(#72266,#72267,#72268,#72269,#72270,#72271,#72272,#72273,#72274,#72275,
#72276,#72277,#72278,#72279,#72280),(#72281,#72282,#72283,#72284,#72285,
#72286,#72287,#72288,#72289,#72290,#72291,#72292,#72293,#72294,#72295)),
 .UNSPECIFIED.,.F.,.F.,.F.,(4,1,4),(4,1,1,1,1,1,1,1,1,1,1,1,4),(0.,0.571428571428571,
1.),(0.19021466797625,0.231284548513244,0.272354429050238,0.292889369318735,
0.303156839452983,0.313424309587232,0.339092984922853,0.354494190124226,
0.364761660258474,0.375029130392723,0.395564070661219,0.436633951198213,
0.477703831735207),.UNSPECIFIED.) ;
#1779=B_SPLINE_SURFACE_WITH_KNOTS('',3,3,((#72433,#72434,#72435,#72436,
#72437,#72438,#72439,#72440,#72441,#72442,#72443,#72444,#72445,#72446),
(#72447,#72448,#72449,#72450,#72451,#72452,#72453,#72454,#72455,#72456,
#72457,#72458,#72459,#72460),(#72461,#72462,#72463,#72464,#72465,#72466,
#72467,#72468,#72469,#72470,#72471,#72472,#72473,#72474),(#72475,#72476,
#72477,#72478,#72479,#72480,#72481,#72482,#72483,#72484,#72485,#72486,#72487,
#72488),(#72489,#72490,#72491,#72492,#72493,#72494,#72495,#72496,#72497,
#72498,#72499,#72500,#72501,#72502)),.UNSPECIFIED.,.F.,.F.,.F.,(4,1,4),
(4,1,1,1,1,1,1,1,1,1,1,4),(0.,0.571428571428571,1.),(0.599057470748752,
0.660662588714575,0.681197628036517,0.701732667358458,0.712000187019428,
0.722267706680399,0.732535226341369,0.763337785324281,0.783872824646222,
0.804407863968163,0.845477942612046,0.886548021255928),.UNSPECIFIED.) ;
#1780=B_SPLINE_SURFACE_WITH_KNOTS('',3,3,((#72743,#72744,#72745,#72746,
#72747,#72748,#72749,#72750,#72751,#72752,#72753,#72754,#72755,#72756),
(#72757,#72758,#72759,#72760,#72761,#72762,#72763,#72764,#72765,#72766,
#72767,#72768,#72769,#72770),(#72771,#72772,#72773,#72774,#72775,#72776,
#72777,#72778,#72779,#72780,#72781,#72782,#72783,#72784),(#72785,#72786,
#72787,#72788,#72789,#72790,#72791,#72792,#72793,#72794,#72795,#72796,#72797,
#72798),(#72799,#72800,#72801,#72802,#72803,#72804,#72805,#72806,#72807,
#72808,#72809,#72810,#72811,#72812)),.UNSPECIFIED.,.F.,.F.,.F.,(4,1,4),
(4,1,1,1,1,1,1,1,1,1,1,4),(0.,0.571428571428571,1.),(0.599057470748733,
0.660662588714558,0.681197628036499,0.701732667358441,0.712000187019412,
0.722267706680383,0.732535226341354,0.763337785324266,0.783872824646208,
0.804407863968149,0.845477942612033,0.886548021255916),.UNSPECIFIED.) ;
#1781=B_SPLINE_SURFACE_WITH_KNOTS('',3,3,((#73037,#73038,#73039,#73040,
#73041,#73042,#73043,#73044,#73045,#73046,#73047,#73048,#73049,#73050,#73051),
(#73052,#73053,#73054,#73055,#73056,#73057,#73058,#73059,#73060,#73061,
#73062,#73063,#73064,#73065,#73066),(#73067,#73068,#73069,#73070,#73071,
#73072,#73073,#73074,#73075,#73076,#73077,#73078,#73079,#73080,#73081),
(#73082,#73083,#73084,#73085,#73086,#73087,#73088,#73089,#73090,#73091,
#73092,#73093,#73094,#73095,#73096),(#73097,#73098,#73099,#73100,#73101,
#73102,#73103,#73104,#73105,#73106,#73107,#73108,#73109,#73110,#73111)),
 .UNSPECIFIED.,.F.,.F.,.F.,(4,1,4),(4,1,1,1,1,1,1,1,1,1,1,1,4),(-0.000196399328153213,
0.571428571428571,1.),(0.866946671401604,0.908212951263578,0.949282831797399,
0.969817772064309,0.99035271233122,1.00062018246467,1.01088765259813,1.02115512273159,
1.03142259286504,1.05195753313195,1.07249247339886,1.11356235393268,1.15482863379465),
 .UNSPECIFIED.) ;
#1782=B_SPLINE_SURFACE_WITH_KNOTS('',3,3,((#73328,#73329,#73330,#73331,
#73332,#73333,#73334,#73335,#73336,#73337,#73338,#73339,#73340,#73341,#73342),
(#73343,#73344,#73345,#73346,#73347,#73348,#73349,#73350,#73351,#73352,
#73353,#73354,#73355,#73356,#73357),(#73358,#73359,#73360,#73361,#73362,
#73363,#73364,#73365,#73366,#73367,#73368,#73369,#73370,#73371,#73372),
(#73373,#73374,#73375,#73376,#73377,#73378,#73379,#73380,#73381,#73382,
#73383,#73384,#73385,#73386,#73387),(#73388,#73389,#73390,#73391,#73392,
#73393,#73394,#73395,#73396,#73397,#73398,#73399,#73400,#73401,#73402)),
 .UNSPECIFIED.,.F.,.F.,.F.,(4,1,4),(4,1,1,1,1,1,1,1,1,1,1,1,4),(0.,0.571428571428571,
1.),(0.124343038522312,0.165413023799283,0.206483009076254,0.22701800171474,
0.237285498033983,0.247552994353225,0.26295423883209,0.288622979630197,
0.29889047594944,0.309157972268682,0.329692964907168,0.370762950184139,
0.411832935461111),.UNSPECIFIED.) ;
#1783=B_SPLINE_SURFACE_WITH_KNOTS('',3,3,((#73531,#73532,#73533,#73534,
#73535,#73536,#73537,#73538,#73539,#73540,#73541,#73542,#73543,#73544,#73545),
(#73546,#73547,#73548,#73549,#73550,#73551,#73552,#73553,#73554,#73555,
#73556,#73557,#73558,#73559,#73560),(#73561,#73562,#73563,#73564,#73565,
#73566,#73567,#73568,#73569,#73570,#73571,#73572,#73573,#73574,#73575),
(#73576,#73577,#73578,#73579,#73580,#73581,#73582,#73583,#73584,#73585,
#73586,#73587,#73588,#73589,#73590),(#73591,#73592,#73593,#73594,#73595,
#73596,#73597,#73598,#73599,#73600,#73601,#73602,#73603,#73604,#73605)),
 .UNSPECIFIED.,.F.,.F.,.F.,(4,1,4),(4,1,1,1,1,1,1,1,1,1,1,1,4),(0.,0.571428571428571,
1.),(0.19021466798717,0.231284548522626,0.272354429058083,0.292889369325811,
0.303156839459675,0.313424309593539,0.339092984928199,0.354494190128995,
0.364761660262859,0.375029130396723,0.395564070664451,0.436633951199908,
0.477703831735364),.UNSPECIFIED.) ;
#1784=B_SPLINE_SURFACE_WITH_KNOTS('',3,3,((#73807,#73808,#73809,#73810,
#73811,#73812,#73813,#73814,#73815,#73816,#73817,#73818,#73819,#73820,#73821),
(#73822,#73823,#73824,#73825,#73826,#73827,#73828,#73829,#73830,#73831,
#73832,#73833,#73834,#73835,#73836),(#73837,#73838,#73839,#73840,#73841,
#73842,#73843,#73844,#73845,#73846,#73847,#73848,#73849,#73850,#73851),
(#73852,#73853,#73854,#73855,#73856,#73857,#73858,#73859,#73860,#73861,
#73862,#73863,#73864,#73865,#73866),(#73867,#73868,#73869,#73870,#73871,
#73872,#73873,#73874,#73875,#73876,#73877,#73878,#73879,#73880,#73881)),
 .UNSPECIFIED.,.F.,.F.,.F.,(4,1,4),(4,1,1,1,1,1,1,1,1,1,1,1,4),(0.,0.571428571428571,
1.),(0.599057470748756,0.640127549392637,0.670930108375547,0.676063868206032,
0.681197628036518,0.722267706680398,0.737668986171854,0.763337785324279,
0.77360530498525,0.78387282464622,0.80440786396816,0.845477942612041,0.886548021255922),
 .UNSPECIFIED.) ;
#1785=B_SPLINE_SURFACE_WITH_KNOTS('',3,3,((#74098,#74099,#74100,#74101,
#74102,#74103,#74104,#74105,#74106,#74107,#74108,#74109,#74110,#74111),
(#74112,#74113,#74114,#74115,#74116,#74117,#74118,#74119,#74120,#74121,
#74122,#74123,#74124,#74125),(#74126,#74127,#74128,#74129,#74130,#74131,
#74132,#74133,#74134,#74135,#74136,#74137,#74138,#74139),(#74140,#74141,
#74142,#74143,#74144,#74145,#74146,#74147,#74148,#74149,#74150,#74151,#74152,
#74153),(#74154,#74155,#74156,#74157,#74158,#74159,#74160,#74161,#74162,
#74163,#74164,#74165,#74166,#74167)),.UNSPECIFIED.,.F.,.F.,.F.,(4,1,4),
(4,1,1,1,1,1,1,1,1,1,1,4),(0.,0.571428571428571,1.),(0.59905747074872,0.660662588714547,
0.681197628036489,0.701732667358431,0.712000187019402,0.722267706680373,
0.732535226341344,0.763337785324257,0.783872824646199,0.804407863968141,
0.845477942612025,0.886548021255909),.UNSPECIFIED.) ;
#1786=B_SPLINE_SURFACE_WITH_KNOTS('',3,3,((#74392,#74393,#74394,#74395,
#74396,#74397,#74398,#74399,#74400,#74401,#74402,#74403,#74404,#74405,#74406),
(#74407,#74408,#74409,#74410,#74411,#74412,#74413,#74414,#74415,#74416,
#74417,#74418,#74419,#74420,#74421),(#74422,#74423,#74424,#74425,#74426,
#74427,#74428,#74429,#74430,#74431,#74432,#74433,#74434,#74435,#74436),
(#74437,#74438,#74439,#74440,#74441,#74442,#74443,#74444,#74445,#74446,
#74447,#74448,#74449,#74450,#74451),(#74452,#74453,#74454,#74455,#74456,
#74457,#74458,#74459,#74460,#74461,#74462,#74463,#74464,#74465,#74466)),
 .UNSPECIFIED.,.F.,.F.,.F.,(4,1,4),(4,1,1,1,1,1,1,1,1,1,1,1,4),(0.,0.571428571428571,
1.),(0.867143070761104,0.908212951290456,0.949282831819809,0.969817772084486,
0.980085242216824,0.990352712349162,1.01602138768001,1.03142259287851,1.04169006301085,
1.05195753314319,1.07249247340787,1.11356235393722,1.15463223446657),
 .UNSPECIFIED.) ;
#1787=B_SPLINE_SURFACE_WITH_KNOTS('',3,3,((#74668,#74669,#74670,#74671,
#74672,#74673,#74674,#74675,#74676,#74677,#74678,#74679,#74680,#74681,#74682),
(#74683,#74684,#74685,#74686,#74687,#74688,#74689,#74690,#74691,#74692,
#74693,#74694,#74695,#74696,#74697),(#74698,#74699,#74700,#74701,#74702,
#74703,#74704,#74705,#74706,#74707,#74708,#74709,#74710,#74711,#74712),
(#74713,#74714,#74715,#74716,#74717,#74718,#74719,#74720,#74721,#74722,
#74723,#74724,#74725,#74726,#74727),(#74728,#74729,#74730,#74731,#74732,
#74733,#74734,#74735,#74736,#74737,#74738,#74739,#74740,#74741,#74742)),
 .UNSPECIFIED.,.F.,.F.,.F.,(4,1,4),(4,1,1,1,1,1,1,1,1,1,1,1,4),(0.,0.571428571428571,
1.),(0.1243430385224,0.165413023799369,0.206483009076339,0.227018001714824,
0.237285498034067,0.247552994353309,0.273221735151415,0.288622979630279,
0.298890475949521,0.309157972268764,0.329692964907249,0.370762950184219,
0.411832935461188),.UNSPECIFIED.) ;
#1788=B_SPLINE_SURFACE_WITH_KNOTS('',3,3,((#74871,#74872,#74873,#74874,
#74875,#74876,#74877,#74878,#74879,#74880,#74881,#74882,#74883,#74884,#74885),
(#74886,#74887,#74888,#74889,#74890,#74891,#74892,#74893,#74894,#74895,
#74896,#74897,#74898,#74899,#74900),(#74901,#74902,#74903,#74904,#74905,
#74906,#74907,#74908,#74909,#74910,#74911,#74912,#74913,#74914,#74915),
(#74916,#74917,#74918,#74919,#74920,#74921,#74922,#74923,#74924,#74925,
#74926,#74927,#74928,#74929,#74930),(#74931,#74932,#74933,#74934,#74935,
#74936,#74937,#74938,#74939,#74940,#74941,#74942,#74943,#74944,#74945)),
 .UNSPECIFIED.,.F.,.F.,.F.,(4,1,4),(4,1,1,1,1,1,1,1,1,1,1,1,4),(0.,0.571428571428571,
1.),(0.190214667985433,0.23128454852112,0.272354429056807,0.29288936932465,
0.303156839458572,0.313424309592494,0.339092984927298,0.354494190128181,
0.364761660262103,0.375029130396024,0.395564070663868,0.436633951199555,
0.477703831735242),.UNSPECIFIED.) ;
#2119=SPHERICAL_SURFACE('',#49407,0.2) ;
#2120=SPHERICAL_SURFACE('',#49409,0.2) ;
#2121=SPHERICAL_SURFACE('',#49411,0.2) ;
#2122=SPHERICAL_SURFACE('',#49413,0.2) ;
#2123=SPHERICAL_SURFACE('',#49415,0.2) ;
#2124=SPHERICAL_SURFACE('',#49417,0.2) ;
#2125=SPHERICAL_SURFACE('',#49419,0.2) ;
#2126=SPHERICAL_SURFACE('',#49421,0.2) ;
#2127=SPHERICAL_SURFACE('',#49442,0.199999999999992) ;
#2128=SPHERICAL_SURFACE('',#49446,0.199999999999996) ;
#2129=SPHERICAL_SURFACE('',#49450,0.199999999999982) ;
#2130=SPHERICAL_SURFACE('',#49456,0.19999999999999) ;
#2131=SPHERICAL_SURFACE('',#49460,0.199999999999987) ;
#2132=SPHERICAL_SURFACE('',#49464,0.199999999999985) ;
#2133=SPHERICAL_SURFACE('',#49468,0.199999999999991) ;
#2134=SPHERICAL_SURFACE('',#49474,0.199999999999996) ;
#2135=SPHERICAL_SURFACE('',#49478,0.199999999999987) ;
#2136=SPHERICAL_SURFACE('',#49482,0.200000000000018) ;
#2137=SPHERICAL_SURFACE('',#49486,0.200000000000018) ;
#2138=SPHERICAL_SURFACE('',#49492,0.200000000000001) ;
#2139=SPHERICAL_SURFACE('',#49496,0.199999999999999) ;
#2140=SPHERICAL_SURFACE('',#49500,0.200000000000007) ;
#2141=SPHERICAL_SURFACE('',#49504,0.200000000000012) ;
#2142=SPHERICAL_SURFACE('',#49510,0.200000000000011) ;
#2143=SPHERICAL_SURFACE('',#49514,0.199999999999993) ;
#2144=SPHERICAL_SURFACE('',#49518,0.200000000000016) ;
#2145=SPHERICAL_SURFACE('',#49522,0.200000000000006) ;
#2146=SPHERICAL_SURFACE('',#49528,0.199999999999982) ;
#2147=SPHERICAL_SURFACE('',#49532,0.199999999999997) ;
#2148=SPHERICAL_SURFACE('',#49536,0.199999999999999) ;
#2149=SPHERICAL_SURFACE('',#49540,0.200000000000023) ;
#2150=SPHERICAL_SURFACE('',#49546,0.199999999999992) ;
#2151=SPHERICAL_SURFACE('',#49550,0.199999999999988) ;
#2152=SPHERICAL_SURFACE('',#49554,0.199999999999997) ;
#2153=SPHERICAL_SURFACE('',#49558,0.200000000000027) ;
#2154=SPHERICAL_SURFACE('',#49564,0.199999999999997) ;
#2155=SPHERICAL_SURFACE('',#49568,0.199999999999974) ;
#2156=SPHERICAL_SURFACE('',#49572,0.200000000000024) ;
#2157=SPHERICAL_SURFACE('',#49576,0.199999999999994) ;
#2158=SPHERICAL_SURFACE('',#49582,0.199999999999997) ;
#2159=SPHERICAL_SURFACE('',#49586,0.199999999999995) ;
#2160=SPHERICAL_SURFACE('',#49590,0.200000000000031) ;
#2161=SPHERICAL_SURFACE('',#49594,0.199999999999985) ;
#2162=SPHERICAL_SURFACE('',#49600,0.199999999999994) ;
#2163=SPHERICAL_SURFACE('',#49604,0.199999999999995) ;
#2164=SPHERICAL_SURFACE('',#49608,0.199999999999986) ;
#2165=SPHERICAL_SURFACE('',#49612,0.199999999999968) ;
#2166=SPHERICAL_SURFACE('',#49618,0.199999999999996) ;
#2216=PLANE('',#49358) ;
#2217=PLANE('',#49423) ;
#2218=PLANE('',#49426) ;
#2219=PLANE('',#49429) ;
#2220=PLANE('',#49432) ;
#2221=PLANE('',#49435) ;
#2222=PLANE('',#49438) ;
#2223=PLANE('',#49441) ;
#2224=PLANE('',#49768) ;
#2225=PLANE('',#49783) ;
#2226=PLANE('',#49796) ;
#2227=PLANE('',#49842) ;
#2228=PLANE('',#49843) ;
#2229=PLANE('',#49844) ;
#2230=PLANE('',#49845) ;
#2231=PLANE('',#49846) ;
#2232=PLANE('',#49847) ;
#2233=PLANE('',#49848) ;
#2234=PLANE('',#49849) ;
#2235=PLANE('',#49850) ;
#2236=PLANE('',#49851) ;
#2237=PLANE('',#49852) ;
#2238=PLANE('',#49853) ;
#2239=PLANE('',#49854) ;
#2240=PLANE('',#49855) ;
#2241=PLANE('',#49856) ;
#2242=PLANE('',#49857) ;
#2243=PLANE('',#49858) ;
#2244=PLANE('',#49859) ;
#2245=PLANE('',#49860) ;
#2246=PLANE('',#49861) ;
#2247=PLANE('',#49862) ;
#2248=PLANE('',#49863) ;
#2249=PLANE('',#49864) ;
#2250=PLANE('',#49865) ;
#3032=LINE('',#69895,#6246) ;
#3033=LINE('',#69899,#6247) ;
#3034=LINE('',#69903,#6248) ;
#3035=LINE('',#69907,#6249) ;
#3036=LINE('',#69911,#6250) ;
#3037=LINE('',#69915,#6251) ;
#3038=LINE('',#69919,#6252) ;
#3039=LINE('',#69923,#6253) ;
#3040=LINE('',#69927,#6254) ;
#3041=LINE('',#69931,#6255) ;
#3042=LINE('',#69935,#6256) ;
#3043=LINE('',#69939,#6257) ;
#3044=LINE('',#69943,#6258) ;
#3045=LINE('',#69947,#6259) ;
#3046=LINE('',#69951,#6260) ;
#3047=LINE('',#69955,#6261) ;
#3048=LINE('',#69959,#6262) ;
#3049=LINE('',#69963,#6263) ;
#3050=LINE('',#69967,#6264) ;
#3051=LINE('',#69971,#6265) ;
#3052=LINE('',#69975,#6266) ;
#3053=LINE('',#69979,#6267) ;
#3054=LINE('',#69983,#6268) ;
#3055=LINE('',#69987,#6269) ;
#3056=LINE('',#69991,#6270) ;
#3057=LINE('',#69995,#6271) ;
#3058=LINE('',#69999,#6272) ;
#3059=LINE('',#70003,#6273) ;
#3060=LINE('',#70007,#6274) ;
#3061=LINE('',#70011,#6275) ;
#3062=LINE('',#70015,#6276) ;
#3063=LINE('',#70019,#6277) ;
#3064=LINE('',#70023,#6278) ;
#3065=LINE('',#70027,#6279) ;
#3066=LINE('',#70031,#6280) ;
#3067=LINE('',#70035,#6281) ;
#3068=LINE('',#70039,#6282) ;
#3069=LINE('',#70043,#6283) ;
#3070=LINE('',#70047,#6284) ;
#3071=LINE('',#70051,#6285) ;
#3072=LINE('',#70055,#6286) ;
#3073=LINE('',#70063,#6287) ;
#3074=LINE('',#70066,#6288) ;
#3075=LINE('',#70072,#6289) ;
#3076=LINE('',#70075,#6290) ;
#3077=LINE('',#70085,#6291) ;
#3078=LINE('',#70086,#6292) ;
#3079=LINE('',#70091,#6293) ;
#3080=LINE('',#70094,#6294) ;
#3081=LINE('',#70100,#6295) ;
#3082=LINE('',#70103,#6296) ;
#3083=LINE('',#70113,#6297) ;
#3084=LINE('',#70114,#6298) ;
#3085=LINE('',#70119,#6299) ;
#3086=LINE('',#70122,#6300) ;
#3087=LINE('',#70128,#6301) ;
#3088=LINE('',#70131,#6302) ;
#3089=LINE('',#70141,#6303) ;
#3090=LINE('',#70142,#6304) ;
#3091=LINE('',#70147,#6305) ;
#3092=LINE('',#70150,#6306) ;
#3093=LINE('',#70163,#6307) ;
#3094=LINE('',#70164,#6308) ;
#3095=LINE('',#70168,#6309) ;
#3096=LINE('',#70169,#6310) ;
#3097=LINE('',#70188,#6311) ;
#3098=LINE('',#70190,#6312) ;
#3099=LINE('',#70191,#6313) ;
#3100=LINE('',#70194,#6314) ;
#3101=LINE('',#70198,#6315) ;
#3102=LINE('',#70199,#6316) ;
#3103=LINE('',#70202,#6317) ;
#3104=LINE('',#70206,#6318) ;
#3105=LINE('',#70207,#6319) ;
#3106=LINE('',#70210,#6320) ;
#3107=LINE('',#70214,#6321) ;
#3108=LINE('',#70215,#6322) ;
#3109=LINE('',#70218,#6323) ;
#3110=LINE('',#70222,#6324) ;
#3111=LINE('',#70223,#6325) ;
#3112=LINE('',#70226,#6326) ;
#3113=LINE('',#70230,#6327) ;
#3114=LINE('',#70231,#6328) ;
#3115=LINE('',#70234,#6329) ;
#3116=LINE('',#72403,#6330) ;
#3117=LINE('',#72420,#6331) ;
#3118=LINE('',#72631,#6332) ;
#3119=LINE('',#72662,#6333) ;
#3120=LINE('',#72681,#6334) ;
#3121=LINE('',#72714,#6335) ;
#3122=LINE('',#72941,#6336) ;
#3123=LINE('',#72956,#6337) ;
#3124=LINE('',#72975,#6338) ;
#3125=LINE('',#73008,#6339) ;
#3126=LINE('',#73232,#6340) ;
#3127=LINE('',#73247,#6341) ;
#3128=LINE('',#73266,#6342) ;
#3129=LINE('',#73299,#6343) ;
#3130=LINE('',#73435,#6344) ;
#3131=LINE('',#73450,#6345) ;
#3132=LINE('',#73469,#6346) ;
#3133=LINE('',#73502,#6347) ;
#3134=LINE('',#73711,#6348) ;
#3135=LINE('',#73726,#6349) ;
#3136=LINE('',#73745,#6350) ;
#3137=LINE('',#73778,#6351) ;
#3138=LINE('',#74002,#6352) ;
#3139=LINE('',#74017,#6353) ;
#3140=LINE('',#74036,#6354) ;
#3141=LINE('',#74069,#6355) ;
#3142=LINE('',#74296,#6356) ;
#3143=LINE('',#74311,#6357) ;
#3144=LINE('',#74330,#6358) ;
#3145=LINE('',#74363,#6359) ;
#3146=LINE('',#74572,#6360) ;
#3147=LINE('',#74587,#6361) ;
#3148=LINE('',#74606,#6362) ;
#3149=LINE('',#74639,#6363) ;
#3150=LINE('',#74775,#6364) ;
#3151=LINE('',#74790,#6365) ;
#3152=LINE('',#74809,#6366) ;
#3153=LINE('',#74842,#6367) ;
#3154=LINE('',#75054,#6368) ;
#3155=LINE('',#75069,#6369) ;
#3156=LINE('',#75142,#6370) ;
#3157=LINE('',#75154,#6371) ;
#3158=LINE('',#75158,#6372) ;
#3159=LINE('',#75162,#6373) ;
#3160=LINE('',#75166,#6374) ;
#3161=LINE('',#75170,#6375) ;
#3162=LINE('',#75174,#6376) ;
#3163=LINE('',#75178,#6377) ;
#3164=LINE('',#75182,#6378) ;
#3165=LINE('',#75186,#6379) ;
#3166=LINE('',#75190,#6380) ;
#3167=LINE('',#75194,#6381) ;
#3168=LINE('',#75197,#6382) ;
#3169=LINE('',#75200,#6383) ;
#3170=LINE('',#75203,#6384) ;
#3171=LINE('',#75216,#6385) ;
#3172=LINE('',#75217,#6386) ;
#3173=LINE('',#75220,#6387) ;
#3174=LINE('',#75223,#6388) ;
#3175=LINE('',#75230,#6389) ;
#3176=LINE('',#75253,#6390) ;
#3177=LINE('',#75261,#6391) ;
#3178=LINE('',#75263,#6392) ;
#3179=LINE('',#75264,#6393) ;
#3180=LINE('',#75272,#6394) ;
#3181=LINE('',#75278,#6395) ;
#3182=LINE('',#75280,#6396) ;
#3183=LINE('',#75282,#6397) ;
#3184=LINE('',#75283,#6398) ;
#3185=LINE('',#75285,#6399) ;
#6246=VECTOR('',#55111,6.) ;
#6247=VECTOR('',#55114,10.) ;
#6248=VECTOR('',#55117,10.) ;
#6249=VECTOR('',#55120,10.) ;
#6250=VECTOR('',#55123,10.) ;
#6251=VECTOR('',#55126,10.) ;
#6252=VECTOR('',#55129,10.) ;
#6253=VECTOR('',#55132,10.) ;
#6254=VECTOR('',#55135,10.) ;
#6255=VECTOR('',#55138,10.) ;
#6256=VECTOR('',#55141,10.) ;
#6257=VECTOR('',#55144,10.) ;
#6258=VECTOR('',#55147,10.) ;
#6259=VECTOR('',#55150,10.) ;
#6260=VECTOR('',#55153,10.) ;
#6261=VECTOR('',#55156,10.) ;
#6262=VECTOR('',#55159,10.) ;
#6263=VECTOR('',#55162,10.) ;
#6264=VECTOR('',#55165,10.) ;
#6265=VECTOR('',#55168,10.) ;
#6266=VECTOR('',#55171,10.) ;
#6267=VECTOR('',#55174,10.) ;
#6268=VECTOR('',#55177,10.) ;
#6269=VECTOR('',#55180,10.) ;
#6270=VECTOR('',#55183,10.) ;
#6271=VECTOR('',#55186,10.) ;
#6272=VECTOR('',#55189,10.) ;
#6273=VECTOR('',#55192,10.) ;
#6274=VECTOR('',#55195,10.) ;
#6275=VECTOR('',#55198,10.) ;
#6276=VECTOR('',#55201,10.) ;
#6277=VECTOR('',#55204,10.) ;
#6278=VECTOR('',#55207,10.) ;
#6279=VECTOR('',#55210,10.) ;
#6280=VECTOR('',#55213,10.) ;
#6281=VECTOR('',#55216,10.) ;
#6282=VECTOR('',#55219,10.) ;
#6283=VECTOR('',#55222,10.) ;
#6284=VECTOR('',#55225,10.) ;
#6285=VECTOR('',#55228,10.) ;
#6286=VECTOR('',#55231,10.) ;
#6287=VECTOR('',#55240,10.) ;
#6288=VECTOR('',#55243,10.) ;
#6289=VECTOR('',#55248,10.) ;
#6290=VECTOR('',#55251,10.) ;
#6291=VECTOR('',#55264,10.) ;
#6292=VECTOR('',#55265,10.) ;
#6293=VECTOR('',#55270,10.) ;
#6294=VECTOR('',#55273,10.) ;
#6295=VECTOR('',#55278,10.) ;
#6296=VECTOR('',#55281,10.) ;
#6297=VECTOR('',#55294,10.) ;
#6298=VECTOR('',#55295,10.) ;
#6299=VECTOR('',#55300,10.) ;
#6300=VECTOR('',#55303,10.) ;
#6301=VECTOR('',#55308,10.) ;
#6302=VECTOR('',#55311,10.) ;
#6303=VECTOR('',#55324,10.) ;
#6304=VECTOR('',#55325,10.) ;
#6305=VECTOR('',#55330,10.) ;
#6306=VECTOR('',#55333,10.) ;
#6307=VECTOR('',#55348,10.) ;
#6308=VECTOR('',#55349,10.) ;
#6309=VECTOR('',#55354,10.) ;
#6310=VECTOR('',#55355,10.) ;
#6311=VECTOR('',#55390,10.) ;
#6312=VECTOR('',#55391,10.) ;
#6313=VECTOR('',#55392,10.) ;
#6314=VECTOR('',#55395,10.) ;
#6315=VECTOR('',#55400,10.) ;
#6316=VECTOR('',#55401,10.) ;
#6317=VECTOR('',#55404,10.) ;
#6318=VECTOR('',#55409,10.) ;
#6319=VECTOR('',#55410,10.) ;
#6320=VECTOR('',#55413,10.) ;
#6321=VECTOR('',#55418,10.) ;
#6322=VECTOR('',#55419,10.) ;
#6323=VECTOR('',#55422,10.) ;
#6324=VECTOR('',#55427,10.) ;
#6325=VECTOR('',#55428,10.) ;
#6326=VECTOR('',#55431,10.) ;
#6327=VECTOR('',#55436,10.) ;
#6328=VECTOR('',#55437,10.) ;
#6329=VECTOR('',#55440,10.) ;
#6330=VECTOR('',#55811,10.) ;
#6331=VECTOR('',#55814,10.) ;
#6332=VECTOR('',#55817,10.) ;
#6333=VECTOR('',#55824,10.) ;
#6334=VECTOR('',#55831,10.) ;
#6335=VECTOR('',#55838,10.) ;
#6336=VECTOR('',#55845,10.) ;
#6337=VECTOR('',#55848,10.) ;
#6338=VECTOR('',#55855,10.) ;
#6339=VECTOR('',#55862,10.) ;
#6340=VECTOR('',#55869,10.) ;
#6341=VECTOR('',#55872,10.) ;
#6342=VECTOR('',#55879,10.) ;
#6343=VECTOR('',#55886,10.) ;
#6344=VECTOR('',#55893,10.) ;
#6345=VECTOR('',#55896,10.) ;
#6346=VECTOR('',#55903,10.) ;
#6347=VECTOR('',#55910,10.) ;
#6348=VECTOR('',#55917,10.) ;
#6349=VECTOR('',#55920,10.) ;
#6350=VECTOR('',#55927,10.) ;
#6351=VECTOR('',#55934,10.) ;
#6352=VECTOR('',#55941,10.) ;
#6353=VECTOR('',#55944,10.) ;
#6354=VECTOR('',#55951,10.) ;
#6355=VECTOR('',#55958,10.) ;
#6356=VECTOR('',#55965,10.) ;
#6357=VECTOR('',#55968,10.) ;
#6358=VECTOR('',#55975,10.) ;
#6359=VECTOR('',#55982,10.) ;
#6360=VECTOR('',#55989,10.) ;
#6361=VECTOR('',#55992,10.) ;
#6362=VECTOR('',#55999,10.) ;
#6363=VECTOR('',#56006,10.) ;
#6364=VECTOR('',#56013,10.) ;
#6365=VECTOR('',#56016,10.) ;
#6366=VECTOR('',#56023,10.) ;
#6367=VECTOR('',#56030,10.) ;
#6368=VECTOR('',#56037,10.) ;
#6369=VECTOR('',#56040,10.) ;
#6370=VECTOR('',#56127,5.625) ;
#6371=VECTOR('',#56142,10.) ;
#6372=VECTOR('',#56145,10.) ;
#6373=VECTOR('',#56148,10.) ;
#6374=VECTOR('',#56151,10.) ;
#6375=VECTOR('',#56154,10.) ;
#6376=VECTOR('',#56157,10.) ;
#6377=VECTOR('',#56160,10.) ;
#6378=VECTOR('',#56163,10.) ;
#6379=VECTOR('',#56166,10.) ;
#6380=VECTOR('',#56169,10.) ;
#6381=VECTOR('',#56172,10.) ;
#6382=VECTOR('',#56175,10.) ;
#6383=VECTOR('',#56178,10.) ;
#6384=VECTOR('',#56183,10.) ;
#6385=VECTOR('',#56204,10.) ;
#6386=VECTOR('',#56205,10.) ;
#6387=VECTOR('',#56208,10.) ;
#6388=VECTOR('',#56213,10.) ;
#6389=VECTOR('',#56224,10.) ;
#6390=VECTOR('',#56267,10.) ;
#6391=VECTOR('',#56278,10.) ;
#6392=VECTOR('',#56281,10.) ;
#6393=VECTOR('',#56282,10.) ;
#6394=VECTOR('',#56293,10.) ;
#6395=VECTOR('',#56302,10.) ;
#6396=VECTOR('',#56305,10.) ;
#6397=VECTOR('',#56308,10.) ;
#6398=VECTOR('',#56309,10.) ;
#6399=VECTOR('',#56312,10.) ;
#9460=CYLINDRICAL_SURFACE('',#49316,6.) ;
#9461=CYLINDRICAL_SURFACE('',#49359,0.2) ;
#9462=CYLINDRICAL_SURFACE('',#49362,0.2) ;
#9463=CYLINDRICAL_SURFACE('',#49369,0.2) ;
#9464=CYLINDRICAL_SURFACE('',#49371,0.2) ;
#9465=CYLINDRICAL_SURFACE('',#49374,0.2) ;
#9466=CYLINDRICAL_SURFACE('',#49381,0.2) ;
#9467=CYLINDRICAL_SURFACE('',#49383,0.2) ;
#9468=CYLINDRICAL_SURFACE('',#49386,0.2) ;
#9469=CYLINDRICAL_SURFACE('',#49393,0.2) ;
#9470=CYLINDRICAL_SURFACE('',#49395,0.2) ;
#9471=CYLINDRICAL_SURFACE('',#49403,0.2) ;
#9472=CYLINDRICAL_SURFACE('',#49405,0.2) ;
#9473=CYLINDRICAL_SURFACE('',#49424,0.2) ;
#9474=CYLINDRICAL_SURFACE('',#49427,0.2) ;
#9475=CYLINDRICAL_SURFACE('',#49430,0.95) ;
#9476=CYLINDRICAL_SURFACE('',#49433,0.2) ;
#9477=CYLINDRICAL_SURFACE('',#49436,0.2) ;
#9478=CYLINDRICAL_SURFACE('',#49439,0.95) ;
#9479=CYLINDRICAL_SURFACE('',#49624,0.2) ;
#9480=CYLINDRICAL_SURFACE('',#49625,0.2) ;
#9481=CYLINDRICAL_SURFACE('',#49626,0.2) ;
#9482=CYLINDRICAL_SURFACE('',#49629,0.2) ;
#9483=CYLINDRICAL_SURFACE('',#49632,0.2) ;
#9484=CYLINDRICAL_SURFACE('',#49635,0.2) ;
#9485=CYLINDRICAL_SURFACE('',#49638,0.2) ;
#9486=CYLINDRICAL_SURFACE('',#49639,0.2) ;
#9487=CYLINDRICAL_SURFACE('',#49642,0.2) ;
#9488=CYLINDRICAL_SURFACE('',#49645,0.2) ;
#9489=CYLINDRICAL_SURFACE('',#49648,0.2) ;
#9490=CYLINDRICAL_SURFACE('',#49649,0.2) ;
#9491=CYLINDRICAL_SURFACE('',#49652,0.2) ;
#9492=CYLINDRICAL_SURFACE('',#49655,0.2) ;
#9493=CYLINDRICAL_SURFACE('',#49658,0.2) ;
#9494=CYLINDRICAL_SURFACE('',#49659,0.2) ;
#9495=CYLINDRICAL_SURFACE('',#49662,0.2) ;
#9496=CYLINDRICAL_SURFACE('',#49665,0.2) ;
#9497=CYLINDRICAL_SURFACE('',#49668,0.2) ;
#9498=CYLINDRICAL_SURFACE('',#49669,0.2) ;
#9499=CYLINDRICAL_SURFACE('',#49672,0.2) ;
#9500=CYLINDRICAL_SURFACE('',#49675,0.2) ;
#9501=CYLINDRICAL_SURFACE('',#49678,0.2) ;
#9502=CYLINDRICAL_SURFACE('',#49679,0.2) ;
#9503=CYLINDRICAL_SURFACE('',#49682,0.2) ;
#9504=CYLINDRICAL_SURFACE('',#49685,0.2) ;
#9505=CYLINDRICAL_SURFACE('',#49688,0.2) ;
#9506=CYLINDRICAL_SURFACE('',#49689,0.2) ;
#9507=CYLINDRICAL_SURFACE('',#49692,0.2) ;
#9508=CYLINDRICAL_SURFACE('',#49695,0.2) ;
#9509=CYLINDRICAL_SURFACE('',#49698,0.2) ;
#9510=CYLINDRICAL_SURFACE('',#49699,0.2) ;
#9511=CYLINDRICAL_SURFACE('',#49702,0.2) ;
#9512=CYLINDRICAL_SURFACE('',#49705,0.2) ;
#9513=CYLINDRICAL_SURFACE('',#49708,0.2) ;
#9514=CYLINDRICAL_SURFACE('',#49709,0.2) ;
#9515=CYLINDRICAL_SURFACE('',#49712,0.2) ;
#9516=CYLINDRICAL_SURFACE('',#49715,0.2) ;
#9517=CYLINDRICAL_SURFACE('',#49718,0.2) ;
#9518=CYLINDRICAL_SURFACE('',#49719,0.2) ;
#9519=CYLINDRICAL_SURFACE('',#49722,0.599999999999996) ;
#9520=CYLINDRICAL_SURFACE('',#49724,0.599999999999996) ;
#9521=CYLINDRICAL_SURFACE('',#49726,0.599999999999996) ;
#9522=CYLINDRICAL_SURFACE('',#49728,0.599999999999996) ;
#9523=CYLINDRICAL_SURFACE('',#49730,0.599999999999996) ;
#9524=CYLINDRICAL_SURFACE('',#49732,0.599999999999996) ;
#9525=CYLINDRICAL_SURFACE('',#49734,0.599999999999996) ;
#9526=CYLINDRICAL_SURFACE('',#49736,0.599999999999996) ;
#9527=CYLINDRICAL_SURFACE('',#49738,0.599999999999996) ;
#9528=CYLINDRICAL_SURFACE('',#49740,0.599999999999996) ;
#9529=CYLINDRICAL_SURFACE('',#49742,0.599999999999996) ;
#9530=CYLINDRICAL_SURFACE('',#49744,0.599999999999996) ;
#9531=CYLINDRICAL_SURFACE('',#49746,0.599999999999996) ;
#9532=CYLINDRICAL_SURFACE('',#49748,0.599999999999996) ;
#9533=CYLINDRICAL_SURFACE('',#49750,0.599999999999996) ;
#9534=CYLINDRICAL_SURFACE('',#49752,0.599999999999996) ;
#9535=CYLINDRICAL_SURFACE('',#49754,0.599999999999996) ;
#9536=CYLINDRICAL_SURFACE('',#49756,0.599999999999996) ;
#9537=CYLINDRICAL_SURFACE('',#49758,0.599999999999996) ;
#9538=CYLINDRICAL_SURFACE('',#49760,0.599999999999996) ;
#9539=CYLINDRICAL_SURFACE('',#49781,0.2) ;
#9540=CYLINDRICAL_SURFACE('',#49787,0.2) ;
#9541=CYLINDRICAL_SURFACE('',#49793,0.95) ;
#9542=CYLINDRICAL_SURFACE('',#49794,0.2) ;
#9543=CYLINDRICAL_SURFACE('',#49801,0.95) ;
#9544=CYLINDRICAL_SURFACE('',#49802,0.2) ;
#9545=CYLINDRICAL_SURFACE('',#49811,0.2) ;
#9546=CYLINDRICAL_SURFACE('',#49815,0.2) ;
#9547=CYLINDRICAL_SURFACE('',#49816,0.2) ;
#9548=CYLINDRICAL_SURFACE('',#49822,0.2) ;
#9549=CYLINDRICAL_SURFACE('',#49827,0.2) ;
#9550=CYLINDRICAL_SURFACE('',#49828,0.2) ;
#9551=CYLINDRICAL_SURFACE('',#49833,0.2) ;
#9552=CYLINDRICAL_SURFACE('',#49837,0.2) ;
#9553=CYLINDRICAL_SURFACE('',#49838,0.2) ;
#9554=CYLINDRICAL_SURFACE('',#49839,0.2) ;
#9555=CYLINDRICAL_SURFACE('',#49840,0.2) ;
#9556=CYLINDRICAL_SURFACE('',#49841,0.2) ;
#10747=FACE_OUTER_BOUND('',#13839,.T.) ;
#10748=FACE_OUTER_BOUND('',#13840,.T.) ;
#10749=FACE_OUTER_BOUND('',#13841,.T.) ;
#10750=FACE_OUTER_BOUND('',#13842,.T.) ;
#10751=FACE_OUTER_BOUND('',#13843,.T.) ;
#10752=FACE_OUTER_BOUND('',#13844,.T.) ;
#10753=FACE_OUTER_BOUND('',#13845,.T.) ;
#10754=FACE_OUTER_BOUND('',#13846,.T.) ;
#10755=FACE_OUTER_BOUND('',#13847,.T.) ;
#10756=FACE_OUTER_BOUND('',#13848,.T.) ;
#10757=FACE_OUTER_BOUND('',#13849,.T.) ;
#10758=FACE_OUTER_BOUND('',#13850,.T.) ;
#10759=FACE_OUTER_BOUND('',#13851,.T.) ;
#10760=FACE_OUTER_BOUND('',#13852,.T.) ;
#10761=FACE_OUTER_BOUND('',#13853,.T.) ;
#10762=FACE_OUTER_BOUND('',#13854,.T.) ;
#10763=FACE_OUTER_BOUND('',#13855,.T.) ;
#10764=FACE_OUTER_BOUND('',#13856,.T.) ;
#10765=FACE_OUTER_BOUND('',#13857,.T.) ;
#10766=FACE_OUTER_BOUND('',#13858,.T.) ;
#10767=FACE_OUTER_BOUND('',#13859,.T.) ;
#10768=FACE_OUTER_BOUND('',#13860,.T.) ;
#10769=FACE_OUTER_BOUND('',#13861,.T.) ;
#10770=FACE_OUTER_BOUND('',#13862,.T.) ;
#10771=FACE_OUTER_BOUND('',#13863,.T.) ;
#10772=FACE_OUTER_BOUND('',#13864,.T.) ;
#10773=FACE_OUTER_BOUND('',#13865,.T.) ;
#10774=FACE_OUTER_BOUND('',#13866,.T.) ;
#10775=FACE_OUTER_BOUND('',#13867,.T.) ;
#10776=FACE_OUTER_BOUND('',#13868,.T.) ;
#10777=FACE_OUTER_BOUND('',#13869,.T.) ;
#10778=FACE_OUTER_BOUND('',#13870,.T.) ;
#10779=FACE_OUTER_BOUND('',#13871,.T.) ;
#10780=FACE_OUTER_BOUND('',#13872,.T.) ;
#10781=FACE_OUTER_BOUND('',#13873,.T.) ;
#10782=FACE_OUTER_BOUND('',#13874,.T.) ;
#10783=FACE_OUTER_BOUND('',#13875,.T.) ;
#10784=FACE_OUTER_BOUND('',#13876,.T.) ;
#10785=FACE_OUTER_BOUND('',#13877,.T.) ;
#10786=FACE_OUTER_BOUND('',#13878,.T.) ;
#10787=FACE_OUTER_BOUND('',#13879,.T.) ;
#10788=FACE_OUTER_BOUND('',#13880,.T.) ;
#10789=FACE_OUTER_BOUND('',#13881,.T.) ;
#10790=FACE_OUTER_BOUND('',#13882,.T.) ;
#10791=FACE_OUTER_BOUND('',#13883,.T.) ;
#10792=FACE_OUTER_BOUND('',#13884,.T.) ;
#10793=FACE_OUTER_BOUND('',#13885,.T.) ;
#10794=FACE_OUTER_BOUND('',#13886,.T.) ;
#10795=FACE_OUTER_BOUND('',#13887,.T.) ;
#10796=FACE_OUTER_BOUND('',#13888,.T.) ;
#10797=FACE_OUTER_BOUND('',#13889,.T.) ;
#10798=FACE_OUTER_BOUND('',#13890,.T.) ;
#10799=FACE_OUTER_BOUND('',#13891,.T.) ;
#10800=FACE_OUTER_BOUND('',#13892,.T.) ;
#10801=FACE_OUTER_BOUND('',#13893,.T.) ;
#10802=FACE_OUTER_BOUND('',#13894,.T.) ;
#10803=FACE_OUTER_BOUND('',#13895,.T.) ;
#10804=FACE_OUTER_BOUND('',#13896,.T.) ;
#10805=FACE_OUTER_BOUND('',#13897,.T.) ;
#10806=FACE_OUTER_BOUND('',#13898,.T.) ;
#10807=FACE_OUTER_BOUND('',#13899,.T.) ;
#10808=FACE_OUTER_BOUND('',#13900,.T.) ;
#10809=FACE_OUTER_BOUND('',#13901,.T.) ;
#10810=FACE_OUTER_BOUND('',#13902,.T.) ;
#10811=FACE_OUTER_BOUND('',#13903,.T.) ;
#10812=FACE_OUTER_BOUND('',#13904,.T.) ;
#10813=FACE_OUTER_BOUND('',#13905,.T.) ;
#10814=FACE_OUTER_BOUND('',#13906,.T.) ;
#10815=FACE_OUTER_BOUND('',#13907,.T.) ;
#10816=FACE_OUTER_BOUND('',#13908,.T.) ;
#10817=FACE_OUTER_BOUND('',#13909,.T.) ;
#10818=FACE_OUTER_BOUND('',#13910,.T.) ;
#10819=FACE_OUTER_BOUND('',#13911,.T.) ;
#10820=FACE_OUTER_BOUND('',#13912,.T.) ;
#10821=FACE_OUTER_BOUND('',#13913,.T.) ;
#10822=FACE_OUTER_BOUND('',#13914,.T.) ;
#10823=FACE_OUTER_BOUND('',#13915,.T.) ;
#10824=FACE_OUTER_BOUND('',#13916,.T.) ;
#10825=FACE_OUTER_BOUND('',#13917,.T.) ;
#10826=FACE_OUTER_BOUND('',#13918,.T.) ;
#10827=FACE_OUTER_BOUND('',#13919,.T.) ;
#10828=FACE_OUTER_BOUND('',#13920,.T.) ;
#10829=FACE_OUTER_BOUND('',#13921,.T.) ;
#10830=FACE_OUTER_BOUND('',#13922,.T.) ;
#10831=FACE_OUTER_BOUND('',#13923,.T.) ;
#10832=FACE_OUTER_BOUND('',#13924,.T.) ;
#10833=FACE_OUTER_BOUND('',#13925,.T.) ;
#10834=FACE_OUTER_BOUND('',#13926,.T.) ;
#10835=FACE_OUTER_BOUND('',#13927,.T.) ;
#10836=FACE_OUTER_BOUND('',#13928,.T.) ;
#10837=FACE_OUTER_BOUND('',#13929,.T.) ;
#10838=FACE_OUTER_BOUND('',#13930,.T.) ;
#10839=FACE_OUTER_BOUND('',#13931,.T.) ;
#10840=FACE_OUTER_BOUND('',#13932,.T.) ;
#10841=FACE_OUTER_BOUND('',#13933,.T.) ;
#10842=FACE_OUTER_BOUND('',#13934,.T.) ;
#10843=FACE_OUTER_BOUND('',#13935,.T.) ;
#10844=FACE_OUTER_BOUND('',#13936,.T.) ;
#10845=FACE_OUTER_BOUND('',#13937,.T.) ;
#10846=FACE_OUTER_BOUND('',#13938,.T.) ;
#10847=FACE_OUTER_BOUND('',#13939,.T.) ;
#10848=FACE_OUTER_BOUND('',#13940,.T.) ;
#10849=FACE_OUTER_BOUND('',#13941,.T.) ;
#10850=FACE_OUTER_BOUND('',#13942,.T.) ;
#10851=FACE_OUTER_BOUND('',#13943,.T.) ;
#10852=FACE_OUTER_BOUND('',#13944,.T.) ;
#10853=FACE_OUTER_BOUND('',#13945,.T.) ;
#10854=FACE_OUTER_BOUND('',#13946,.T.) ;
#10855=FACE_OUTER_BOUND('',#13947,.T.) ;
#10856=FACE_OUTER_BOUND('',#13948,.T.) ;
#10857=FACE_OUTER_BOUND('',#13949,.T.) ;
#10858=FACE_OUTER_BOUND('',#13950,.T.) ;
#10859=FACE_OUTER_BOUND('',#13951,.T.) ;
#10860=FACE_OUTER_BOUND('',#13952,.T.) ;
#10861=FACE_OUTER_BOUND('',#13953,.T.) ;
#10862=FACE_OUTER_BOUND('',#13954,.T.) ;
#10863=FACE_OUTER_BOUND('',#13955,.T.) ;
#10864=FACE_OUTER_BOUND('',#13956,.T.) ;
#10865=FACE_OUTER_BOUND('',#13957,.T.) ;
#10866=FACE_OUTER_BOUND('',#13958,.T.) ;
#10867=FACE_OUTER_BOUND('',#13959,.T.) ;
#10868=FACE_OUTER_BOUND('',#13960,.T.) ;
#10869=FACE_OUTER_BOUND('',#13961,.T.) ;
#10870=FACE_OUTER_BOUND('',#13962,.T.) ;
#10871=FACE_OUTER_BOUND('',#13963,.T.) ;
#10872=FACE_OUTER_BOUND('',#13964,.T.) ;
#10873=FACE_OUTER_BOUND('',#13965,.T.) ;
#10874=FACE_OUTER_BOUND('',#13966,.T.) ;
#10875=FACE_OUTER_BOUND('',#13967,.T.) ;
#10876=FACE_OUTER_BOUND('',#13968,.T.) ;
#10877=FACE_OUTER_BOUND('',#13969,.T.) ;
#10878=FACE_OUTER_BOUND('',#13970,.T.) ;
#10879=FACE_OUTER_BOUND('',#13971,.T.) ;
#10880=FACE_OUTER_BOUND('',#13972,.T.) ;
#10881=FACE_OUTER_BOUND('',#13973,.T.) ;
#10882=FACE_OUTER_BOUND('',#13974,.T.) ;
#10883=FACE_OUTER_BOUND('',#13975,.T.) ;
#10884=FACE_OUTER_BOUND('',#13976,.T.) ;
#10885=FACE_OUTER_BOUND('',#13977,.T.) ;
#10886=FACE_OUTER_BOUND('',#13978,.T.) ;
#10887=FACE_OUTER_BOUND('',#13979,.T.) ;
#10888=FACE_OUTER_BOUND('',#13980,.T.) ;
#10889=FACE_OUTER_BOUND('',#13981,.T.) ;
#10890=FACE_OUTER_BOUND('',#13982,.T.) ;
#10891=FACE_OUTER_BOUND('',#13983,.T.) ;
#10892=FACE_OUTER_BOUND('',#13984,.T.) ;
#10893=FACE_OUTER_BOUND('',#13985,.T.) ;
#10894=FACE_OUTER_BOUND('',#13986,.T.) ;
#10895=FACE_OUTER_BOUND('',#13987,.T.) ;
#10896=FACE_OUTER_BOUND('',#13988,.T.) ;
#10897=FACE_OUTER_BOUND('',#13989,.T.) ;
#10898=FACE_OUTER_BOUND('',#13990,.T.) ;
#10899=FACE_OUTER_BOUND('',#13991,.T.) ;
#10900=FACE_OUTER_BOUND('',#13992,.T.) ;
#10901=FACE_OUTER_BOUND('',#13993,.T.) ;
#10902=FACE_OUTER_BOUND('',#13994,.T.) ;
#10903=FACE_OUTER_BOUND('',#13995,.T.) ;
#10904=FACE_OUTER_BOUND('',#13996,.T.) ;
#10905=FACE_OUTER_BOUND('',#13997,.T.) ;
#10906=FACE_OUTER_BOUND('',#13998,.T.) ;
#10907=FACE_OUTER_BOUND('',#13999,.T.) ;
#10908=FACE_OUTER_BOUND('',#14000,.T.) ;
#10909=FACE_OUTER_BOUND('',#14001,.T.) ;
#10910=FACE_OUTER_BOUND('',#14002,.T.) ;
#10911=FACE_OUTER_BOUND('',#14003,.T.) ;
#10912=FACE_OUTER_BOUND('',#14004,.T.) ;
#10913=FACE_OUTER_BOUND('',#14005,.T.) ;
#10914=FACE_OUTER_BOUND('',#14006,.T.) ;
#10915=FACE_OUTER_BOUND('',#14007,.T.) ;
#10916=FACE_OUTER_BOUND('',#14008,.T.) ;
#10917=FACE_OUTER_BOUND('',#14009,.T.) ;
#10918=FACE_OUTER_BOUND('',#14010,.T.) ;
#10919=FACE_OUTER_BOUND('',#14011,.T.) ;
#10920=FACE_OUTER_BOUND('',#14012,.T.) ;
#10921=FACE_OUTER_BOUND('',#14013,.T.) ;
#10922=FACE_OUTER_BOUND('',#14014,.T.) ;
#10923=FACE_OUTER_BOUND('',#14015,.T.) ;
#10924=FACE_OUTER_BOUND('',#14016,.T.) ;
#10925=FACE_OUTER_BOUND('',#14017,.T.) ;
#10926=FACE_OUTER_BOUND('',#14018,.T.) ;
#10927=FACE_OUTER_BOUND('',#14019,.T.) ;
#10928=FACE_OUTER_BOUND('',#14020,.T.) ;
#10929=FACE_OUTER_BOUND('',#14021,.T.) ;
#10930=FACE_OUTER_BOUND('',#14022,.T.) ;
#10931=FACE_OUTER_BOUND('',#14023,.T.) ;
#10932=FACE_OUTER_BOUND('',#14024,.T.) ;
#10933=FACE_OUTER_BOUND('',#14025,.T.) ;
#10934=FACE_OUTER_BOUND('',#14026,.T.) ;
#10935=FACE_OUTER_BOUND('',#14027,.T.) ;
#10936=FACE_OUTER_BOUND('',#14028,.T.) ;
#10937=FACE_OUTER_BOUND('',#14029,.T.) ;
#10938=FACE_OUTER_BOUND('',#14030,.T.) ;
#10939=FACE_OUTER_BOUND('',#14031,.T.) ;
#10940=FACE_OUTER_BOUND('',#14032,.T.) ;
#10941=FACE_OUTER_BOUND('',#14033,.T.) ;
#10942=FACE_OUTER_BOUND('',#14034,.T.) ;
#10943=FACE_OUTER_BOUND('',#14035,.T.) ;
#10944=FACE_OUTER_BOUND('',#14036,.T.) ;
#10945=FACE_OUTER_BOUND('',#14037,.T.) ;
#10946=FACE_OUTER_BOUND('',#14038,.T.) ;
#10947=FACE_OUTER_BOUND('',#14039,.T.) ;
#10948=FACE_OUTER_BOUND('',#14040,.T.) ;
#10949=FACE_OUTER_BOUND('',#14041,.T.) ;
#10950=FACE_OUTER_BOUND('',#14043,.T.) ;
#10951=FACE_OUTER_BOUND('',#14044,.T.) ;
#10952=FACE_OUTER_BOUND('',#14045,.T.) ;
#10953=FACE_OUTER_BOUND('',#14046,.T.) ;
#10954=FACE_OUTER_BOUND('',#14047,.T.) ;
#10955=FACE_OUTER_BOUND('',#14048,.T.) ;
#10956=FACE_OUTER_BOUND('',#14049,.T.) ;
#10957=FACE_OUTER_BOUND('',#14050,.T.) ;
#10958=FACE_OUTER_BOUND('',#14051,.T.) ;
#10959=FACE_OUTER_BOUND('',#14052,.T.) ;
#10960=FACE_OUTER_BOUND('',#14053,.T.) ;
#10961=FACE_OUTER_BOUND('',#14054,.T.) ;
#10962=FACE_OUTER_BOUND('',#14055,.T.) ;
#10963=FACE_OUTER_BOUND('',#14056,.T.) ;
#10964=FACE_OUTER_BOUND('',#14057,.T.) ;
#10965=FACE_OUTER_BOUND('',#14058,.T.) ;
#10966=FACE_OUTER_BOUND('',#14059,.T.) ;
#10967=FACE_OUTER_BOUND('',#14060,.T.) ;
#10968=FACE_OUTER_BOUND('',#14061,.T.) ;
#10969=FACE_OUTER_BOUND('',#14062,.T.) ;
#10970=FACE_OUTER_BOUND('',#14063,.T.) ;
#10971=FACE_OUTER_BOUND('',#14064,.T.) ;
#10972=FACE_OUTER_BOUND('',#14065,.T.) ;
#10973=FACE_OUTER_BOUND('',#14066,.T.) ;
#10974=FACE_OUTER_BOUND('',#14067,.T.) ;
#10975=FACE_OUTER_BOUND('',#14068,.T.) ;
#10976=FACE_OUTER_BOUND('',#14069,.T.) ;
#10977=FACE_OUTER_BOUND('',#14070,.T.) ;
#10978=FACE_OUTER_BOUND('',#14071,.T.) ;
#10979=FACE_OUTER_BOUND('',#14072,.T.) ;
#10980=FACE_OUTER_BOUND('',#14073,.T.) ;
#10981=FACE_OUTER_BOUND('',#14074,.T.) ;
#10982=FACE_OUTER_BOUND('',#14075,.T.) ;
#10983=FACE_OUTER_BOUND('',#14076,.T.) ;
#10984=FACE_OUTER_BOUND('',#14077,.T.) ;
#10985=FACE_OUTER_BOUND('',#14078,.T.) ;
#10986=FACE_OUTER_BOUND('',#14079,.T.) ;
#10987=FACE_OUTER_BOUND('',#14080,.T.) ;
#10988=FACE_OUTER_BOUND('',#14081,.T.) ;
#10989=FACE_OUTER_BOUND('',#14082,.T.) ;
#10990=FACE_OUTER_BOUND('',#14083,.T.) ;
#10991=FACE_OUTER_BOUND('',#14084,.T.) ;
#10992=FACE_OUTER_BOUND('',#14085,.T.) ;
#10993=FACE_OUTER_BOUND('',#14086,.T.) ;
#10994=FACE_OUTER_BOUND('',#14087,.T.) ;
#10995=FACE_OUTER_BOUND('',#14088,.T.) ;
#10996=FACE_OUTER_BOUND('',#14089,.T.) ;
#10997=FACE_OUTER_BOUND('',#14090,.T.) ;
#10998=FACE_OUTER_BOUND('',#14091,.T.) ;
#10999=FACE_OUTER_BOUND('',#14092,.T.) ;
#11000=FACE_OUTER_BOUND('',#14093,.T.) ;
#11001=FACE_OUTER_BOUND('',#14094,.T.) ;
#11002=FACE_OUTER_BOUND('',#14095,.T.) ;
#11003=FACE_OUTER_BOUND('',#14096,.T.) ;
#11004=FACE_OUTER_BOUND('',#14097,.T.) ;
#11005=FACE_OUTER_BOUND('',#14098,.T.) ;
#13839=EDGE_LOOP('',(#30994,#30995,#30996,#30997)) ;
#13840=EDGE_LOOP('',(#30998,#30999,#31000,#31001,#31002,#31003,#31004,#31005,
#31006,#31007,#31008,#31009,#31010,#31011,#31012,#31013,#31014,#31015,#31016,
#31017,#31018,#31019,#31020,#31021,#31022,#31023,#31024,#31025,#31026,#31027,
#31028,#31029,#31030,#31031,#31032,#31033,#31034,#31035,#31036,#31037,#31038,
#31039,#31040,#31041,#31042,#31043,#31044,#31045,#31046,#31047,#31048,#31049,
#31050,#31051,#31052,#31053,#31054,#31055,#31056,#31057,#31058,#31059,#31060,
#31061,#31062,#31063,#31064,#31065,#31066,#31067,#31068,#31069,#31070,#31071,
#31072,#31073,#31074,#31075,#31076,#31077,#31078,#31079,#31080,#31081)) ;
#13841=EDGE_LOOP('',(#31082)) ;
#13842=EDGE_LOOP('',(#31083,#31084,#31085,#31086)) ;
#13843=EDGE_LOOP('',(#31087,#31088,#31089,#31090)) ;
#13844=EDGE_LOOP('',(#31091,#31092,#31093,#31094)) ;
#13845=EDGE_LOOP('',(#31095,#31096,#31097,#31098)) ;
#13846=EDGE_LOOP('',(#31099,#31100,#31101,#31102)) ;
#13847=EDGE_LOOP('',(#31103,#31104,#31105,#31106)) ;
#13848=EDGE_LOOP('',(#31107,#31108,#31109,#31110)) ;
#13849=EDGE_LOOP('',(#31111,#31112,#31113,#31114)) ;
#13850=EDGE_LOOP('',(#31115,#31116,#31117,#31118)) ;
#13851=EDGE_LOOP('',(#31119,#31120,#31121,#31122)) ;
#13852=EDGE_LOOP('',(#31123,#31124,#31125,#31126)) ;
#13853=EDGE_LOOP('',(#31127,#31128,#31129,#31130)) ;
#13854=EDGE_LOOP('',(#31131,#31132,#31133,#31134)) ;
#13855=EDGE_LOOP('',(#31135,#31136,#31137,#31138)) ;
#13856=EDGE_LOOP('',(#31139,#31140,#31141,#31142)) ;
#13857=EDGE_LOOP('',(#31143,#31144,#31145,#31146)) ;
#13858=EDGE_LOOP('',(#31147,#31148,#31149)) ;
#13859=EDGE_LOOP('',(#31150,#31151,#31152)) ;
#13860=EDGE_LOOP('',(#31153,#31154,#31155)) ;
#13861=EDGE_LOOP('',(#31156,#31157,#31158)) ;
#13862=EDGE_LOOP('',(#31159,#31160,#31161)) ;
#13863=EDGE_LOOP('',(#31162,#31163,#31164)) ;
#13864=EDGE_LOOP('',(#31165,#31166,#31167)) ;
#13865=EDGE_LOOP('',(#31168,#31169,#31170)) ;
#13866=EDGE_LOOP('',(#31171,#31172,#31173,#31174)) ;
#13867=EDGE_LOOP('',(#31175,#31176,#31177,#31178)) ;
#13868=EDGE_LOOP('',(#31179,#31180,#31181,#31182)) ;
#13869=EDGE_LOOP('',(#31183,#31184,#31185,#31186)) ;
#13870=EDGE_LOOP('',(#31187,#31188,#31189,#31190)) ;
#13871=EDGE_LOOP('',(#31191,#31192,#31193,#31194)) ;
#13872=EDGE_LOOP('',(#31195,#31196,#31197,#31198)) ;
#13873=EDGE_LOOP('',(#31199,#31200,#31201,#31202)) ;
#13874=EDGE_LOOP('',(#31203,#31204,#31205,#31206)) ;
#13875=EDGE_LOOP('',(#31207,#31208,#31209,#31210)) ;
#13876=EDGE_LOOP('',(#31211,#31212,#31213,#31214)) ;
#13877=EDGE_LOOP('',(#31215,#31216,#31217,#31218)) ;
#13878=EDGE_LOOP('',(#31219,#31220,#31221,#31222,#31223,#31224,#31225,#31226,
#31227,#31228,#31229,#31230,#31231,#31232,#31233,#31234)) ;
#13879=EDGE_LOOP('',(#31235,#31236,#31237)) ;
#13880=EDGE_LOOP('',(#31238,#31239,#31240)) ;
#13881=EDGE_LOOP('',(#31241,#31242,#31243)) ;
#13882=EDGE_LOOP('',(#31244,#31245,#31246,#31247)) ;
#13883=EDGE_LOOP('',(#31248,#31249,#31250)) ;
#13884=EDGE_LOOP('',(#31251,#31252,#31253)) ;
#13885=EDGE_LOOP('',(#31254,#31255,#31256,#31257)) ;
#13886=EDGE_LOOP('',(#31258,#31259,#31260)) ;
#13887=EDGE_LOOP('',(#31261,#31262,#31263)) ;
#13888=EDGE_LOOP('',(#31264,#31265,#31266,#31267)) ;
#13889=EDGE_LOOP('',(#31268,#31269,#31270)) ;
#13890=EDGE_LOOP('',(#31271,#31272,#31273)) ;
#13891=EDGE_LOOP('',(#31274,#31275,#31276,#31277)) ;
#13892=EDGE_LOOP('',(#31278,#31279,#31280)) ;
#13893=EDGE_LOOP('',(#31281,#31282,#31283)) ;
#13894=EDGE_LOOP('',(#31284,#31285,#31286,#31287)) ;
#13895=EDGE_LOOP('',(#31288,#31289,#31290)) ;
#13896=EDGE_LOOP('',(#31291,#31292,#31293)) ;
#13897=EDGE_LOOP('',(#31294,#31295,#31296,#31297)) ;
#13898=EDGE_LOOP('',(#31298,#31299,#31300)) ;
#13899=EDGE_LOOP('',(#31301,#31302,#31303)) ;
#13900=EDGE_LOOP('',(#31304,#31305,#31306,#31307)) ;
#13901=EDGE_LOOP('',(#31308,#31309,#31310)) ;
#13902=EDGE_LOOP('',(#31311,#31312,#31313)) ;
#13903=EDGE_LOOP('',(#31314,#31315,#31316,#31317,#31318)) ;
#13904=EDGE_LOOP('',(#31319,#31320,#31321)) ;
#13905=EDGE_LOOP('',(#31322,#31323,#31324)) ;
#13906=EDGE_LOOP('',(#31325,#31326,#31327,#31328)) ;
#13907=EDGE_LOOP('',(#31329,#31330,#31331)) ;
#13908=EDGE_LOOP('',(#31332,#31333,#31334)) ;
#13909=EDGE_LOOP('',(#31335,#31336,#31337,#31338)) ;
#13910=EDGE_LOOP('',(#31339,#31340,#31341)) ;
#13911=EDGE_LOOP('',(#31342,#31343,#31344)) ;
#13912=EDGE_LOOP('',(#31345,#31346,#31347,#31348)) ;
#13913=EDGE_LOOP('',(#31349,#31350,#31351)) ;
#13914=EDGE_LOOP('',(#31352,#31353,#31354)) ;
#13915=EDGE_LOOP('',(#31355,#31356,#31357,#31358)) ;
#13916=EDGE_LOOP('',(#31359,#31360,#31361)) ;
#13917=EDGE_LOOP('',(#31362,#31363,#31364)) ;
#13918=EDGE_LOOP('',(#31365,#31366,#31367,#31368)) ;
#13919=EDGE_LOOP('',(#31369,#31370,#31371)) ;
#13920=EDGE_LOOP('',(#31372,#31373,#31374)) ;
#13921=EDGE_LOOP('',(#31375,#31376,#31377,#31378)) ;
#13922=EDGE_LOOP('',(#31379,#31380,#31381)) ;
#13923=EDGE_LOOP('',(#31382,#31383,#31384)) ;
#13924=EDGE_LOOP('',(#31385,#31386,#31387,#31388)) ;
#13925=EDGE_LOOP('',(#31389,#31390,#31391)) ;
#13926=EDGE_LOOP('',(#31392,#31393,#31394)) ;
#13927=EDGE_LOOP('',(#31395,#31396,#31397,#31398)) ;
#13928=EDGE_LOOP('',(#31399,#31400,#31401)) ;
#13929=EDGE_LOOP('',(#31402,#31403,#31404)) ;
#13930=EDGE_LOOP('',(#31405,#31406,#31407,#31408)) ;
#13931=EDGE_LOOP('',(#31409,#31410,#31411)) ;
#13932=EDGE_LOOP('',(#31412,#31413,#31414)) ;
#13933=EDGE_LOOP('',(#31415,#31416,#31417,#31418)) ;
#13934=EDGE_LOOP('',(#31419,#31420,#31421)) ;
#13935=EDGE_LOOP('',(#31422,#31423,#31424)) ;
#13936=EDGE_LOOP('',(#31425,#31426,#31427,#31428)) ;
#13937=EDGE_LOOP('',(#31429,#31430,#31431)) ;
#13938=EDGE_LOOP('',(#31432,#31433,#31434,#31435)) ;
#13939=EDGE_LOOP('',(#31436,#31437,#31438,#31439)) ;
#13940=EDGE_LOOP('',(#31440,#31441,#31442,#31443)) ;
#13941=EDGE_LOOP('',(#31444,#31445,#31446,#31447)) ;
#13942=EDGE_LOOP('',(#31448,#31449,#31450,#31451)) ;
#13943=EDGE_LOOP('',(#31452,#31453,#31454,#31455)) ;
#13944=EDGE_LOOP('',(#31456,#31457,#31458,#31459,#31460,#31461)) ;
#13945=EDGE_LOOP('',(#31462,#31463,#31464,#31465)) ;
#13946=EDGE_LOOP('',(#31466,#31467,#31468,#31469)) ;
#13947=EDGE_LOOP('',(#31470,#31471,#31472,#31473)) ;
#13948=EDGE_LOOP('',(#31474,#31475,#31476,#31477,#31478,#31479)) ;
#13949=EDGE_LOOP('',(#31480,#31481,#31482,#31483)) ;
#13950=EDGE_LOOP('',(#31484,#31485,#31486,#31487,#31488,#31489)) ;
#13951=EDGE_LOOP('',(#31490,#31491,#31492,#31493)) ;
#13952=EDGE_LOOP('',(#31494,#31495,#31496,#31497)) ;
#13953=EDGE_LOOP('',(#31498,#31499,#31500,#31501)) ;
#13954=EDGE_LOOP('',(#31502,#31503,#31504,#31505)) ;
#13955=EDGE_LOOP('',(#31506,#31507,#31508,#31509)) ;
#13956=EDGE_LOOP('',(#31510,#31511,#31512,#31513,#31514,#31515)) ;
#13957=EDGE_LOOP('',(#31516,#31517,#31518,#31519)) ;
#13958=EDGE_LOOP('',(#31520,#31521,#31522,#31523,#31524,#31525)) ;
#13959=EDGE_LOOP('',(#31526,#31527,#31528,#31529)) ;
#13960=EDGE_LOOP('',(#31530,#31531,#31532,#31533)) ;
#13961=EDGE_LOOP('',(#31534,#31535,#31536,#31537)) ;
#13962=EDGE_LOOP('',(#31538,#31539,#31540,#31541)) ;
#13963=EDGE_LOOP('',(#31542,#31543,#31544,#31545)) ;
#13964=EDGE_LOOP('',(#31546,#31547,#31548,#31549,#31550,#31551)) ;
#13965=EDGE_LOOP('',(#31552,#31553,#31554,#31555)) ;
#13966=EDGE_LOOP('',(#31556,#31557,#31558,#31559,#31560,#31561)) ;
#13967=EDGE_LOOP('',(#31562,#31563,#31564,#31565)) ;
#13968=EDGE_LOOP('',(#31566,#31567,#31568,#31569)) ;
#13969=EDGE_LOOP('',(#31570,#31571,#31572,#31573)) ;
#13970=EDGE_LOOP('',(#31574,#31575,#31576,#31577)) ;
#13971=EDGE_LOOP('',(#31578,#31579,#31580,#31581)) ;
#13972=EDGE_LOOP('',(#31582,#31583,#31584,#31585,#31586,#31587)) ;
#13973=EDGE_LOOP('',(#31588,#31589,#31590,#31591)) ;
#13974=EDGE_LOOP('',(#31592,#31593,#31594,#31595,#31596,#31597)) ;
#13975=EDGE_LOOP('',(#31598,#31599,#31600,#31601)) ;
#13976=EDGE_LOOP('',(#31602,#31603,#31604,#31605)) ;
#13977=EDGE_LOOP('',(#31606,#31607,#31608,#31609)) ;
#13978=EDGE_LOOP('',(#31610,#31611,#31612,#31613)) ;
#13979=EDGE_LOOP('',(#31614,#31615,#31616,#31617)) ;
#13980=EDGE_LOOP('',(#31618,#31619,#31620,#31621,#31622,#31623)) ;
#13981=EDGE_LOOP('',(#31624,#31625,#31626,#31627)) ;
#13982=EDGE_LOOP('',(#31628,#31629,#31630,#31631,#31632,#31633)) ;
#13983=EDGE_LOOP('',(#31634,#31635,#31636,#31637)) ;
#13984=EDGE_LOOP('',(#31638,#31639,#31640,#31641)) ;
#13985=EDGE_LOOP('',(#31642,#31643,#31644,#31645)) ;
#13986=EDGE_LOOP('',(#31646,#31647,#31648,#31649)) ;
#13987=EDGE_LOOP('',(#31650,#31651,#31652,#31653)) ;
#13988=EDGE_LOOP('',(#31654,#31655,#31656,#31657,#31658,#31659)) ;
#13989=EDGE_LOOP('',(#31660,#31661,#31662,#31663)) ;
#13990=EDGE_LOOP('',(#31664,#31665,#31666,#31667,#31668,#31669,#31670)) ;
#13991=EDGE_LOOP('',(#31671,#31672,#31673,#31674)) ;
#13992=EDGE_LOOP('',(#31675,#31676,#31677,#31678)) ;
#13993=EDGE_LOOP('',(#31679,#31680,#31681,#31682)) ;
#13994=EDGE_LOOP('',(#31683,#31684,#31685,#31686)) ;
#13995=EDGE_LOOP('',(#31687,#31688,#31689,#31690)) ;
#13996=EDGE_LOOP('',(#31691,#31692,#31693,#31694,#31695,#31696)) ;
#13997=EDGE_LOOP('',(#31697,#31698,#31699,#31700)) ;
#13998=EDGE_LOOP('',(#31701,#31702,#31703,#31704,#31705,#31706)) ;
#13999=EDGE_LOOP('',(#31707,#31708,#31709,#31710)) ;
#14000=EDGE_LOOP('',(#31711,#31712,#31713,#31714)) ;
#14001=EDGE_LOOP('',(#31715,#31716,#31717,#31718)) ;
#14002=EDGE_LOOP('',(#31719,#31720,#31721,#31722)) ;
#14003=EDGE_LOOP('',(#31723,#31724,#31725,#31726)) ;
#14004=EDGE_LOOP('',(#31727,#31728,#31729,#31730,#31731,#31732)) ;
#14005=EDGE_LOOP('',(#31733,#31734,#31735,#31736)) ;
#14006=EDGE_LOOP('',(#31737,#31738,#31739,#31740,#31741,#31742)) ;
#14007=EDGE_LOOP('',(#31743,#31744,#31745,#31746)) ;
#14008=EDGE_LOOP('',(#31747,#31748,#31749,#31750)) ;
#14009=EDGE_LOOP('',(#31751,#31752,#31753,#31754)) ;
#14010=EDGE_LOOP('',(#31755,#31756,#31757,#31758)) ;
#14011=EDGE_LOOP('',(#31759,#31760,#31761,#31762)) ;
#14012=EDGE_LOOP('',(#31763,#31764,#31765,#31766,#31767,#31768)) ;
#14013=EDGE_LOOP('',(#31769,#31770,#31771,#31772)) ;
#14014=EDGE_LOOP('',(#31773,#31774,#31775,#31776,#31777,#31778)) ;
#14015=EDGE_LOOP('',(#31779,#31780,#31781,#31782)) ;
#14016=EDGE_LOOP('',(#31783,#31784,#31785,#31786)) ;
#14017=EDGE_LOOP('',(#31787,#31788,#31789,#31790)) ;
#14018=EDGE_LOOP('',(#31791,#31792,#31793,#31794,#31795,#31796)) ;
#14019=EDGE_LOOP('',(#31797,#31798,#31799,#31800,#31801,#31802)) ;
#14020=EDGE_LOOP('',(#31803,#31804,#31805,#31806,#31807,#31808)) ;
#14021=EDGE_LOOP('',(#31809,#31810,#31811,#31812,#31813,#31814)) ;
#14022=EDGE_LOOP('',(#31815,#31816,#31817,#31818,#31819,#31820)) ;
#14023=EDGE_LOOP('',(#31821,#31822,#31823,#31824,#31825,#31826)) ;
#14024=EDGE_LOOP('',(#31827,#31828,#31829,#31830,#31831,#31832)) ;
#14025=EDGE_LOOP('',(#31833,#31834,#31835,#31836,#31837,#31838)) ;
#14026=EDGE_LOOP('',(#31839,#31840,#31841,#31842,#31843,#31844)) ;
#14027=EDGE_LOOP('',(#31845,#31846,#31847,#31848,#31849,#31850)) ;
#14028=EDGE_LOOP('',(#31851,#31852,#31853,#31854,#31855,#31856)) ;
#14029=EDGE_LOOP('',(#31857,#31858,#31859,#31860,#31861,#31862)) ;
#14030=EDGE_LOOP('',(#31863,#31864,#31865,#31866,#31867,#31868)) ;
#14031=EDGE_LOOP('',(#31869,#31870,#31871,#31872,#31873,#31874)) ;
#14032=EDGE_LOOP('',(#31875,#31876,#31877,#31878,#31879,#31880)) ;
#14033=EDGE_LOOP('',(#31881,#31882,#31883,#31884,#31885,#31886)) ;
#14034=EDGE_LOOP('',(#31887,#31888,#31889,#31890,#31891,#31892)) ;
#14035=EDGE_LOOP('',(#31893,#31894,#31895,#31896,#31897,#31898)) ;
#14036=EDGE_LOOP('',(#31899,#31900,#31901,#31902,#31903,#31904)) ;
#14037=EDGE_LOOP('',(#31905,#31906,#31907,#31908,#31909,#31910)) ;
#14038=EDGE_LOOP('',(#31911,#31912,#31913,#31914,#31915,#31916)) ;
#14039=EDGE_LOOP('',(#31917,#31918,#31919,#31920,#31921,#31922,#31923,#31924,
#31925,#31926,#31927,#31928,#31929,#31930,#31931,#31932,#31933,#31934,#31935,
#31936,#31937,#31938,#31939,#31940,#31941,#31942,#31943,#31944,#31945,#31946,
#31947,#31948,#31949,#31950,#31951,#31952,#31953,#31954,#31955,#31956,#31957,
#31958,#31959,#31960)) ;
#14040=EDGE_LOOP('',(#31961,#31962,#31963,#31964)) ;
#14041=EDGE_LOOP('',(#31965)) ;
#14042=EDGE_LOOP('',(#31966,#31967,#31968,#31969,#31970,#31971,#31972,#31973,
#31974,#31975,#31976,#31977,#31978,#31979,#31980,#31981,#31982,#31983,#31984,
#31985,#31986,#31987,#31988,#31989)) ;
#14043=EDGE_LOOP('',(#31990,#31991,#31992,#31993)) ;
#14044=EDGE_LOOP('',(#31994,#31995,#31996,#31997)) ;
#14045=EDGE_LOOP('',(#31998,#31999,#32000,#32001)) ;
#14046=EDGE_LOOP('',(#32002,#32003,#32004,#32005)) ;
#14047=EDGE_LOOP('',(#32006,#32007,#32008,#32009)) ;
#14048=EDGE_LOOP('',(#32010,#32011,#32012,#32013)) ;
#14049=EDGE_LOOP('',(#32014,#32015,#32016,#32017)) ;
#14050=EDGE_LOOP('',(#32018,#32019,#32020,#32021)) ;
#14051=EDGE_LOOP('',(#32022,#32023,#32024,#32025)) ;
#14052=EDGE_LOOP('',(#32026,#32027,#32028,#32029)) ;
#14053=EDGE_LOOP('',(#32030,#32031,#32032,#32033)) ;
#14054=EDGE_LOOP('',(#32034,#32035,#32036,#32037)) ;
#14055=EDGE_LOOP('',(#32038,#32039,#32040,#32041)) ;
#14056=EDGE_LOOP('',(#32042,#32043,#32044,#32045)) ;
#14057=EDGE_LOOP('',(#32046,#32047,#32048,#32049)) ;
#14058=EDGE_LOOP('',(#32050,#32051,#32052,#32053)) ;
#14059=EDGE_LOOP('',(#32054,#32055,#32056,#32057)) ;
#14060=EDGE_LOOP('',(#32058,#32059,#32060,#32061)) ;
#14061=EDGE_LOOP('',(#32062,#32063,#32064,#32065)) ;
#14062=EDGE_LOOP('',(#32066,#32067,#32068,#32069)) ;
#14063=EDGE_LOOP('',(#32070,#32071,#32072,#32073)) ;
#14064=EDGE_LOOP('',(#32074,#32075,#32076,#32077)) ;
#14065=EDGE_LOOP('',(#32078,#32079,#32080,#32081)) ;
#14066=EDGE_LOOP('',(#32082,#32083,#32084,#32085)) ;
#14067=EDGE_LOOP('',(#32086,#32087,#32088,#32089)) ;
#14068=EDGE_LOOP('',(#32090,#32091,#32092,#32093)) ;
#14069=EDGE_LOOP('',(#32094,#32095,#32096,#32097)) ;
#14070=EDGE_LOOP('',(#32098,#32099,#32100,#32101)) ;
#14071=EDGE_LOOP('',(#32102,#32103,#32104,#32105)) ;
#14072=EDGE_LOOP('',(#32106,#32107,#32108,#32109)) ;
#14073=EDGE_LOOP('',(#32110,#32111,#32112,#32113)) ;
#14074=EDGE_LOOP('',(#32114,#32115,#32116,#32117)) ;
#14075=EDGE_LOOP('',(#32118,#32119)) ;
#14076=EDGE_LOOP('',(#32120,#32121)) ;
#14077=EDGE_LOOP('',(#32122,#32123)) ;
#14078=EDGE_LOOP('',(#32124,#32125)) ;
#14079=EDGE_LOOP('',(#32126,#32127)) ;
#14080=EDGE_LOOP('',(#32128,#32129)) ;
#14081=EDGE_LOOP('',(#32130,#32131)) ;
#14082=EDGE_LOOP('',(#32132,#32133)) ;
#14083=EDGE_LOOP('',(#32134,#32135)) ;
#14084=EDGE_LOOP('',(#32136,#32137)) ;
#14085=EDGE_LOOP('',(#32138,#32139)) ;
#14086=EDGE_LOOP('',(#32140,#32141)) ;
#14087=EDGE_LOOP('',(#32142,#32143)) ;
#14088=EDGE_LOOP('',(#32144,#32145)) ;
#14089=EDGE_LOOP('',(#32146,#32147)) ;
#14090=EDGE_LOOP('',(#32148,#32149)) ;
#14091=EDGE_LOOP('',(#32150,#32151)) ;
#14092=EDGE_LOOP('',(#32152,#32153)) ;
#14093=EDGE_LOOP('',(#32154,#32155)) ;
#14094=EDGE_LOOP('',(#32156,#32157)) ;
#14095=EDGE_LOOP('',(#32158,#32159,#32160,#32161)) ;
#14096=EDGE_LOOP('',(#32162,#32163,#32164,#32165)) ;
#14097=EDGE_LOOP('',(#32166,#32167,#32168,#32169)) ;
#14098=EDGE_LOOP('',(#32170,#32171,#32172,#32173)) ;
#17034=CIRCLE('',#49313,5.8) ;
#17035=CIRCLE('',#49314,0.2) ;
#17036=CIRCLE('',#49315,6.) ;
#17037=CIRCLE('',#49317,6.) ;
#17038=CIRCLE('',#49318,6.) ;
#17039=CIRCLE('',#49319,6.) ;
#17040=CIRCLE('',#49320,6.) ;
#17041=CIRCLE('',#49321,6.) ;
#17042=CIRCLE('',#49322,6.) ;
#17043=CIRCLE('',#49323,6.) ;
#17044=CIRCLE('',#49324,6.) ;
#17045=CIRCLE('',#49325,6.) ;
#17046=CIRCLE('',#49326,6.) ;
#17047=CIRCLE('',#49327,6.) ;
#17048=CIRCLE('',#49328,6.) ;
#17049=CIRCLE('',#49329,6.) ;
#17050=CIRCLE('',#49330,6.) ;
#17051=CIRCLE('',#49331,6.) ;
#17052=CIRCLE('',#49332,6.) ;
#17053=CIRCLE('',#49333,6.) ;
#17054=CIRCLE('',#49334,6.) ;
#17055=CIRCLE('',#49335,6.) ;
#17056=CIRCLE('',#49336,6.) ;
#17057=CIRCLE('',#49337,6.) ;
#17058=CIRCLE('',#49338,6.) ;
#17059=CIRCLE('',#49339,6.) ;
#17060=CIRCLE('',#49340,6.) ;
#17061=CIRCLE('',#49341,6.) ;
#17062=CIRCLE('',#49342,6.) ;
#17063=CIRCLE('',#49343,6.) ;
#17064=CIRCLE('',#49344,6.) ;
#17065=CIRCLE('',#49345,6.) ;
#17066=CIRCLE('',#49346,6.) ;
#17067=CIRCLE('',#49347,6.) ;
#17068=CIRCLE('',#49348,6.) ;
#17069=CIRCLE('',#49349,6.) ;
#17070=CIRCLE('',#49350,6.) ;
#17071=CIRCLE('',#49351,6.) ;
#17072=CIRCLE('',#49352,6.) ;
#17073=CIRCLE('',#49353,6.) ;
#17074=CIRCLE('',#49354,6.) ;
#17075=CIRCLE('',#49355,6.) ;
#17076=CIRCLE('',#49356,6.) ;
#17077=CIRCLE('',#49357,6.) ;
#17078=CIRCLE('',#49360,0.199999999999987) ;
#17079=CIRCLE('',#49361,0.2) ;
#17080=CIRCLE('',#49363,0.199999999999996) ;
#17081=CIRCLE('',#49364,0.2) ;
#17082=CIRCLE('',#49366,0.2) ;
#17083=CIRCLE('',#49367,0.95) ;
#17084=CIRCLE('',#49368,1.15) ;
#17085=CIRCLE('',#49370,0.2) ;
#17086=CIRCLE('',#49372,0.199999999999996) ;
#17087=CIRCLE('',#49373,0.2) ;
#17088=CIRCLE('',#49375,0.199999999999996) ;
#17089=CIRCLE('',#49376,0.2) ;
#17090=CIRCLE('',#49378,0.2) ;
#17091=CIRCLE('',#49379,0.95) ;
#17092=CIRCLE('',#49380,1.15) ;
#17093=CIRCLE('',#49382,0.2) ;
#17094=CIRCLE('',#49384,0.199999999999996) ;
#17095=CIRCLE('',#49385,0.2) ;
#17096=CIRCLE('',#49387,0.200000000000005) ;
#17097=CIRCLE('',#49388,0.2) ;
#17098=CIRCLE('',#49390,0.2) ;
#17099=CIRCLE('',#49391,0.95) ;
#17100=CIRCLE('',#49392,1.15) ;
#17101=CIRCLE('',#49394,0.2) ;
#17102=CIRCLE('',#49396,0.199999999999996) ;
#17103=CIRCLE('',#49397,0.2) ;
#17104=CIRCLE('',#49399,0.200000000000031) ;
#17105=CIRCLE('',#49400,1.15) ;
#17106=CIRCLE('',#49401,0.2) ;
#17107=CIRCLE('',#49402,0.95) ;
#17108=CIRCLE('',#49404,0.2) ;
#17109=CIRCLE('',#49406,0.199999999999996) ;
#17110=CIRCLE('',#49408,0.199999999999995) ;
#17111=CIRCLE('',#49410,0.199999999999995) ;
#17112=CIRCLE('',#49412,0.199999999999995) ;
#17113=CIRCLE('',#49414,0.200000000000001) ;
#17114=CIRCLE('',#49416,0.199999999999988) ;
#17115=CIRCLE('',#49418,0.199999999999995) ;
#17116=CIRCLE('',#49420,0.200000000000001) ;
#17117=CIRCLE('',#49422,0.199999999999995) ;
#17118=CIRCLE('',#49425,0.199999999999996) ;
#17119=CIRCLE('',#49428,0.199999999999996) ;
#17120=CIRCLE('',#49431,0.95) ;
#17121=CIRCLE('',#49434,0.199999999999996) ;
#17122=CIRCLE('',#49437,0.199999999999996) ;
#17123=CIRCLE('',#49440,0.95) ;
#17124=CIRCLE('',#49443,0.199999999999995) ;
#17125=CIRCLE('',#49444,0.199999999999992) ;
#17126=CIRCLE('',#49445,0.199999999999994) ;
#17127=CIRCLE('',#49447,0.199999999999988) ;
#17128=CIRCLE('',#49448,0.199999999999996) ;
#17129=CIRCLE('',#49449,0.199999999999999) ;
#17130=CIRCLE('',#49451,0.199999999999999) ;
#17131=CIRCLE('',#49452,0.199999999999982) ;
#17132=CIRCLE('',#49453,0.2) ;
#17133=CIRCLE('',#49455,5.969599660801) ;
#17134=CIRCLE('',#49457,0.200000000000008) ;
#17135=CIRCLE('',#49458,0.19999999999999) ;
#17136=CIRCLE('',#49459,0.200000000000008) ;
#17137=CIRCLE('',#49461,0.199999999999994) ;
#17138=CIRCLE('',#49462,0.199999999999987) ;
#17139=CIRCLE('',#49463,0.199999999999998) ;
#17140=CIRCLE('',#49465,0.20000000000001) ;
#17141=CIRCLE('',#49466,0.199999999999985) ;
#17142=CIRCLE('',#49467,0.2) ;
#17143=CIRCLE('',#49469,0.200000000000011) ;
#17144=CIRCLE('',#49470,0.199999999999991) ;
#17145=CIRCLE('',#49471,0.200000000000002) ;
#17146=CIRCLE('',#49473,5.96959966080102) ;
#17147=CIRCLE('',#49475,0.199999999999997) ;
#17148=CIRCLE('',#49476,0.199999999999996) ;
#17149=CIRCLE('',#49477,0.200000000000025) ;
#17150=CIRCLE('',#49479,0.200000000000012) ;
#17151=CIRCLE('',#49480,0.199999999999987) ;
#17152=CIRCLE('',#49481,0.199999999999999) ;
#17153=CIRCLE('',#49483,0.20000000000003) ;
#17154=CIRCLE('',#49484,0.200000000000018) ;
#17155=CIRCLE('',#49485,0.200000000000015) ;
#17156=CIRCLE('',#49487,0.19999999999999) ;
#17157=CIRCLE('',#49488,0.200000000000018) ;
#17158=CIRCLE('',#49489,0.200000000000003) ;
#17159=CIRCLE('',#49491,5.96959966080103) ;
#17160=CIRCLE('',#49493,0.200000000000015) ;
#17161=CIRCLE('',#49494,0.200000000000001) ;
#17162=CIRCLE('',#49495,0.200000000000003) ;
#17163=CIRCLE('',#49497,0.200000000000041) ;
#17164=CIRCLE('',#49498,0.199999999999999) ;
#17165=CIRCLE('',#49499,0.200000000000003) ;
#17166=CIRCLE('',#49501,0.199999999999998) ;
#17167=CIRCLE('',#49502,0.200000000000007) ;
#17168=CIRCLE('',#49503,0.200000000000005) ;
#17169=CIRCLE('',#49505,0.199999999999993) ;
#17170=CIRCLE('',#49506,0.200000000000012) ;
#17171=CIRCLE('',#49507,0.199999999999966) ;
#17172=CIRCLE('',#49509,5.96959966080102) ;
#17173=CIRCLE('',#49511,0.200000000000011) ;
#17174=CIRCLE('',#49512,0.200000000000011) ;
#17175=CIRCLE('',#49513,0.200000000000004) ;
#17176=CIRCLE('',#49515,0.200000000000011) ;
#17177=CIRCLE('',#49516,0.199999999999993) ;
#17178=CIRCLE('',#49517,0.199999999999993) ;
#17179=CIRCLE('',#49519,0.199999999999991) ;
#17180=CIRCLE('',#49520,0.200000000000016) ;
#17181=CIRCLE('',#49521,0.199999999999994) ;
#17182=CIRCLE('',#49523,0.199999999999997) ;
#17183=CIRCLE('',#49524,0.200000000000006) ;
#17184=CIRCLE('',#49525,0.199999999999972) ;
#17185=CIRCLE('',#49527,5.96959966080102) ;
#17186=CIRCLE('',#49529,0.200000000000025) ;
#17187=CIRCLE('',#49530,0.199999999999982) ;
#17188=CIRCLE('',#49531,0.200000000000005) ;
#17189=CIRCLE('',#49533,0.200000000000004) ;
#17190=CIRCLE('',#49534,0.199999999999997) ;
#17191=CIRCLE('',#49535,0.200000000000013) ;
#17192=CIRCLE('',#49537,0.199999999999988) ;
#17193=CIRCLE('',#49538,0.199999999999999) ;
#17194=CIRCLE('',#49539,0.200000000000008) ;
#17195=CIRCLE('',#49541,0.199999999999983) ;
#17196=CIRCLE('',#49542,0.200000000000023) ;
#17197=CIRCLE('',#49543,0.199999999999958) ;
#17198=CIRCLE('',#49545,5.96959966080103) ;
#17199=CIRCLE('',#49547,0.199999999999977) ;
#17200=CIRCLE('',#49548,0.199999999999992) ;
#17201=CIRCLE('',#49549,0.200000000000011) ;
#17202=CIRCLE('',#49551,0.200000000000011) ;
#17203=CIRCLE('',#49552,0.199999999999988) ;
#17204=CIRCLE('',#49553,0.200000000000004) ;
#17205=CIRCLE('',#49555,0.200000000000011) ;
#17206=CIRCLE('',#49556,0.199999999999997) ;
#17207=CIRCLE('',#49557,0.200000000000003) ;
#17208=CIRCLE('',#49559,0.200000000000004) ;
#17209=CIRCLE('',#49560,0.200000000000027) ;
#17210=CIRCLE('',#49561,0.200000000000023) ;
#17211=CIRCLE('',#49563,5.96959966080103) ;
#17212=CIRCLE('',#49565,0.200000000000041) ;
#17213=CIRCLE('',#49566,0.199999999999997) ;
#17214=CIRCLE('',#49567,0.200000000000006) ;
#17215=CIRCLE('',#49569,0.199999999999987) ;
#17216=CIRCLE('',#49570,0.199999999999974) ;
#17217=CIRCLE('',#49571,0.200000000000003) ;
#17218=CIRCLE('',#49573,0.19999999999999) ;
#17219=CIRCLE('',#49574,0.200000000000024) ;
#17220=CIRCLE('',#49575,0.199999999999975) ;
#17221=CIRCLE('',#49577,0.199999999999998) ;
#17222=CIRCLE('',#49578,0.199999999999994) ;
#17223=CIRCLE('',#49579,0.199999999999988) ;
#17224=CIRCLE('',#49581,5.96959966080101) ;
#17225=CIRCLE('',#49583,0.199999999999973) ;
#17226=CIRCLE('',#49584,0.199999999999997) ;
#17227=CIRCLE('',#49585,0.200000000000006) ;
#17228=CIRCLE('',#49587,0.200000000000005) ;
#17229=CIRCLE('',#49588,0.199999999999995) ;
#17230=CIRCLE('',#49589,0.199999999999988) ;
#17231=CIRCLE('',#49591,0.199999999999998) ;
#17232=CIRCLE('',#49592,0.200000000000031) ;
#17233=CIRCLE('',#49593,0.199999999999995) ;
#17234=CIRCLE('',#49595,0.20000000000001) ;
#17235=CIRCLE('',#49596,0.199999999999985) ;
#17236=CIRCLE('',#49597,0.200000000000003) ;
#17237=CIRCLE('',#49599,5.96959966080101) ;
#17238=CIRCLE('',#49601,0.199999999999984) ;
#17239=CIRCLE('',#49602,0.199999999999994) ;
#17240=CIRCLE('',#49603,0.199999999999998) ;
#17241=CIRCLE('',#49605,0.200000000000008) ;
#17242=CIRCLE('',#49606,0.199999999999995) ;
#17243=CIRCLE('',#49607,0.199999999999974) ;
#17244=CIRCLE('',#49609,0.199999999999963) ;
#17245=CIRCLE('',#49610,0.199999999999986) ;
#17246=CIRCLE('',#49611,0.199999999999991) ;
#17247=CIRCLE('',#49613,0.199999999999988) ;
#17248=CIRCLE('',#49614,0.199999999999968) ;
#17249=CIRCLE('',#49615,0.199999999999999) ;
#17250=CIRCLE('',#49617,5.96959966080098) ;
#17251=CIRCLE('',#49619,0.199999999999995) ;
#17252=CIRCLE('',#49620,0.199999999999996) ;
#17253=CIRCLE('',#49621,0.199999999999998) ;
#17254=CIRCLE('',#49623,5.96959966080099) ;
#17255=CIRCLE('',#49628,5.8) ;
#17256=CIRCLE('',#49631,5.96959966080104) ;
#17257=CIRCLE('',#49634,5.8) ;
#17258=CIRCLE('',#49637,5.8) ;
#17259=CIRCLE('',#49641,5.96959966080103) ;
#17260=CIRCLE('',#49644,5.8) ;
#17261=CIRCLE('',#49647,5.8) ;
#17262=CIRCLE('',#49651,5.96959966080101) ;
#17263=CIRCLE('',#49654,5.8) ;
#17264=CIRCLE('',#49657,5.8) ;
#17265=CIRCLE('',#49661,5.96959966080102) ;
#17266=CIRCLE('',#49664,5.8) ;
#17267=CIRCLE('',#49667,5.8) ;
#17268=CIRCLE('',#49671,5.96959966080103) ;
#17269=CIRCLE('',#49674,5.8) ;
#17270=CIRCLE('',#49677,5.8) ;
#17271=CIRCLE('',#49681,5.96959966080102) ;
#17272=CIRCLE('',#49684,5.8) ;
#17273=CIRCLE('',#49687,5.8) ;
#17274=CIRCLE('',#49691,5.96959966080101) ;
#17275=CIRCLE('',#49694,5.8) ;
#17276=CIRCLE('',#49697,5.8) ;
#17277=CIRCLE('',#49701,5.96959966080101) ;
#17278=CIRCLE('',#49704,5.8) ;
#17279=CIRCLE('',#49707,5.8) ;
#17280=CIRCLE('',#49711,5.96959966080104) ;
#17281=CIRCLE('',#49714,5.8) ;
#17282=CIRCLE('',#49717,5.8) ;
#17283=CIRCLE('',#49721,5.8) ;
#17284=CIRCLE('',#49723,0.599999999999996) ;
#17285=CIRCLE('',#49725,0.599999999999996) ;
#17286=CIRCLE('',#49727,0.599999999999996) ;
#17287=CIRCLE('',#49729,0.599999999999996) ;
#17288=CIRCLE('',#49731,0.599999999999996) ;
#17289=CIRCLE('',#49733,0.599999999999996) ;
#17290=CIRCLE('',#49735,0.599999999999996) ;
#17291=CIRCLE('',#49737,0.599999999999996) ;
#17292=CIRCLE('',#49739,0.599999999999996) ;
#17293=CIRCLE('',#49741,0.599999999999996) ;
#17294=CIRCLE('',#49743,0.599999999999996) ;
#17295=CIRCLE('',#49745,0.599999999999996) ;
#17296=CIRCLE('',#49747,0.599999999999996) ;
#17297=CIRCLE('',#49749,0.599999999999996) ;
#17298=CIRCLE('',#49751,0.599999999999996) ;
#17299=CIRCLE('',#49753,0.599999999999996) ;
#17300=CIRCLE('',#49755,0.599999999999996) ;
#17301=CIRCLE('',#49757,0.599999999999996) ;
#17302=CIRCLE('',#49759,0.599999999999996) ;
#17303=CIRCLE('',#49761,0.599999999999996) ;
#17304=CIRCLE('',#49763,5.3087501324996) ;
#17305=CIRCLE('',#49765,0.200000000000005) ;
#17306=CIRCLE('',#49766,0.75) ;
#17307=CIRCLE('',#49767,0.2) ;
#17308=CIRCLE('',#49769,5.13915047169858) ;
#17309=CIRCLE('',#49770,0.399999999999992) ;
#17310=CIRCLE('',#49771,0.399999999999992) ;
#17311=CIRCLE('',#49772,0.75) ;
#17312=CIRCLE('',#49773,0.399999999999992) ;
#17313=CIRCLE('',#49774,0.399999999999992) ;
#17314=CIRCLE('',#49775,0.75) ;
#17315=CIRCLE('',#49776,0.399999999999992) ;
#17316=CIRCLE('',#49777,0.399999999999983) ;
#17317=CIRCLE('',#49778,0.75) ;
#17318=CIRCLE('',#49779,0.399999999999992) ;
#17319=CIRCLE('',#49780,0.399999999999992) ;
#17320=CIRCLE('',#49782,0.199999999999996) ;
#17321=CIRCLE('',#49785,0.199999999999996) ;
#17322=CIRCLE('',#49786,0.2) ;
#17323=CIRCLE('',#49788,0.199999999999996) ;
#17324=CIRCLE('',#49790,0.200000000000031) ;
#17325=CIRCLE('',#49791,0.2) ;
#17326=CIRCLE('',#49792,0.95) ;
#17327=CIRCLE('',#49795,0.199999999999996) ;
#17328=CIRCLE('',#49798,0.200000000000005) ;
#17329=CIRCLE('',#49799,0.2) ;
#17330=CIRCLE('',#49800,0.95) ;
#17331=CIRCLE('',#49803,0.199999999999996) ;
#17332=CIRCLE('',#49805,0.2) ;
#17333=CIRCLE('',#49807,0.2) ;
#17334=CIRCLE('',#49809,0.199999999999996) ;
#17335=CIRCLE('',#49810,0.2) ;
#17336=CIRCLE('',#49813,0.2) ;
#17337=CIRCLE('',#49814,0.199999999999996) ;
#17338=CIRCLE('',#49818,0.2) ;
#17339=CIRCLE('',#49820,0.199999999999996) ;
#17340=CIRCLE('',#49821,0.2) ;
#17341=CIRCLE('',#49824,0.199999999999996) ;
#17342=CIRCLE('',#49825,0.199999999999996) ;
#17343=CIRCLE('',#49826,0.2) ;
#17344=CIRCLE('',#49830,0.199999999999996) ;
#17345=CIRCLE('',#49831,0.199999999999996) ;
#17346=CIRCLE('',#49832,0.2) ;
#17347=CIRCLE('',#49835,0.199999999999996) ;
#17348=CIRCLE('',#49836,0.2) ;
#19561=VERTEX_POINT('',#69888) ;
#19562=VERTEX_POINT('',#69890) ;
#19563=VERTEX_POINT('',#69894) ;
#19564=VERTEX_POINT('',#69896) ;
#19565=VERTEX_POINT('',#69898) ;
#19566=VERTEX_POINT('',#69900) ;
#19567=VERTEX_POINT('',#69902) ;
#19568=VERTEX_POINT('',#69904) ;
#19569=VERTEX_POINT('',#69906) ;
#19570=VERTEX_POINT('',#69908) ;
#19571=VERTEX_POINT('',#69910) ;
#19572=VERTEX_POINT('',#69912) ;
#19573=VERTEX_POINT('',#69914) ;
#19574=VERTEX_POINT('',#69916) ;
#19575=VERTEX_POINT('',#69918) ;
#19576=VERTEX_POINT('',#69920) ;
#19577=VERTEX_POINT('',#69922) ;
#19578=VERTEX_POINT('',#69924) ;
#19579=VERTEX_POINT('',#69926) ;
#19580=VERTEX_POINT('',#69928) ;
#19581=VERTEX_POINT('',#69930) ;
#19582=VERTEX_POINT('',#69932) ;
#19583=VERTEX_POINT('',#69934) ;
#19584=VERTEX_POINT('',#69936) ;
#19585=VERTEX_POINT('',#69938) ;
#19586=VERTEX_POINT('',#69940) ;
#19587=VERTEX_POINT('',#69942) ;
#19588=VERTEX_POINT('',#69944) ;
#19589=VERTEX_POINT('',#69946) ;
#19590=VERTEX_POINT('',#69948) ;
#19591=VERTEX_POINT('',#69950) ;
#19592=VERTEX_POINT('',#69952) ;
#19593=VERTEX_POINT('',#69954) ;
#19594=VERTEX_POINT('',#69956) ;
#19595=VERTEX_POINT('',#69958) ;
#19596=VERTEX_POINT('',#69960) ;
#19597=VERTEX_POINT('',#69962) ;
#19598=VERTEX_POINT('',#69964) ;
#19599=VERTEX_POINT('',#69966) ;
#19600=VERTEX_POINT('',#69968) ;
#19601=VERTEX_POINT('',#69970) ;
#19602=VERTEX_POINT('',#69972) ;
#19603=VERTEX_POINT('',#69974) ;
#19604=VERTEX_POINT('',#69976) ;
#19605=VERTEX_POINT('',#69978) ;
#19606=VERTEX_POINT('',#69980) ;
#19607=VERTEX_POINT('',#69982) ;
#19608=VERTEX_POINT('',#69984) ;
#19609=VERTEX_POINT('',#69986) ;
#19610=VERTEX_POINT('',#69988) ;
#19611=VERTEX_POINT('',#69990) ;
#19612=VERTEX_POINT('',#69992) ;
#19613=VERTEX_POINT('',#69994) ;
#19614=VERTEX_POINT('',#69996) ;
#19615=VERTEX_POINT('',#69998) ;
#19616=VERTEX_POINT('',#70000) ;
#19617=VERTEX_POINT('',#70002) ;
#19618=VERTEX_POINT('',#70004) ;
#19619=VERTEX_POINT('',#70006) ;
#19620=VERTEX_POINT('',#70008) ;
#19621=VERTEX_POINT('',#70010) ;
#19622=VERTEX_POINT('',#70012) ;
#19623=VERTEX_POINT('',#70014) ;
#19624=VERTEX_POINT('',#70016) ;
#19625=VERTEX_POINT('',#70018) ;
#19626=VERTEX_POINT('',#70020) ;
#19627=VERTEX_POINT('',#70022) ;
#19628=VERTEX_POINT('',#70024) ;
#19629=VERTEX_POINT('',#70026) ;
#19630=VERTEX_POINT('',#70028) ;
#19631=VERTEX_POINT('',#70030) ;
#19632=VERTEX_POINT('',#70032) ;
#19633=VERTEX_POINT('',#70034) ;
#19634=VERTEX_POINT('',#70036) ;
#19635=VERTEX_POINT('',#70038) ;
#19636=VERTEX_POINT('',#70040) ;
#19637=VERTEX_POINT('',#70042) ;
#19638=VERTEX_POINT('',#70044) ;
#19639=VERTEX_POINT('',#70046) ;
#19640=VERTEX_POINT('',#70048) ;
#19641=VERTEX_POINT('',#70050) ;
#19642=VERTEX_POINT('',#70052) ;
#19643=VERTEX_POINT('',#70054) ;
#19644=VERTEX_POINT('',#70059) ;
#19645=VERTEX_POINT('',#70060) ;
#19646=VERTEX_POINT('',#70062) ;
#19647=VERTEX_POINT('',#70064) ;
#19648=VERTEX_POINT('',#70068) ;
#19649=VERTEX_POINT('',#70069) ;
#19650=VERTEX_POINT('',#70071) ;
#19651=VERTEX_POINT('',#70073) ;
#19652=VERTEX_POINT('',#70077) ;
#19653=VERTEX_POINT('',#70078) ;
#19654=VERTEX_POINT('',#70083) ;
#19655=VERTEX_POINT('',#70088) ;
#19656=VERTEX_POINT('',#70089) ;
#19657=VERTEX_POINT('',#70092) ;
#19658=VERTEX_POINT('',#70096) ;
#19659=VERTEX_POINT('',#70097) ;
#19660=VERTEX_POINT('',#70099) ;
#19661=VERTEX_POINT('',#70101) ;
#19662=VERTEX_POINT('',#70105) ;
#19663=VERTEX_POINT('',#70106) ;
#19664=VERTEX_POINT('',#70111) ;
#19665=VERTEX_POINT('',#70116) ;
#19666=VERTEX_POINT('',#70117) ;
#19667=VERTEX_POINT('',#70120) ;
#19668=VERTEX_POINT('',#70124) ;
#19669=VERTEX_POINT('',#70125) ;
#19670=VERTEX_POINT('',#70127) ;
#19671=VERTEX_POINT('',#70129) ;
#19672=VERTEX_POINT('',#70133) ;
#19673=VERTEX_POINT('',#70134) ;
#19674=VERTEX_POINT('',#70139) ;
#19675=VERTEX_POINT('',#70144) ;
#19676=VERTEX_POINT('',#70145) ;
#19677=VERTEX_POINT('',#70148) ;
#19678=VERTEX_POINT('',#70152) ;
#19679=VERTEX_POINT('',#70153) ;
#19680=VERTEX_POINT('',#70155) ;
#19681=VERTEX_POINT('',#70157) ;
#19682=VERTEX_POINT('',#70161) ;
#19683=VERTEX_POINT('',#70166) ;
#19684=VERTEX_POINT('',#70187) ;
#19685=VERTEX_POINT('',#70189) ;
#19686=VERTEX_POINT('',#70193) ;
#19687=VERTEX_POINT('',#70197) ;
#19688=VERTEX_POINT('',#70201) ;
#19689=VERTEX_POINT('',#70205) ;
#19690=VERTEX_POINT('',#70209) ;
#19691=VERTEX_POINT('',#70213) ;
#19692=VERTEX_POINT('',#70217) ;
#19693=VERTEX_POINT('',#70221) ;
#19694=VERTEX_POINT('',#70225) ;
#19695=VERTEX_POINT('',#70229) ;
#19696=VERTEX_POINT('',#70233) ;
#19697=VERTEX_POINT('',#70238) ;
#19698=VERTEX_POINT('',#70240) ;
#19699=VERTEX_POINT('',#70244) ;
#19700=VERTEX_POINT('',#70246) ;
#19701=VERTEX_POINT('',#70250) ;
#19702=VERTEX_POINT('',#70252) ;
#19703=VERTEX_POINT('',#70258) ;
#19704=VERTEX_POINT('',#70260) ;
#19705=VERTEX_POINT('',#70264) ;
#19706=VERTEX_POINT('',#70266) ;
#19707=VERTEX_POINT('',#70536) ;
#19708=VERTEX_POINT('',#70538) ;
#19709=VERTEX_POINT('',#70542) ;
#19710=VERTEX_POINT('',#70544) ;
#19711=VERTEX_POINT('',#70550) ;
#19712=VERTEX_POINT('',#70552) ;
#19713=VERTEX_POINT('',#70556) ;
#19714=VERTEX_POINT('',#70558) ;
#19715=VERTEX_POINT('',#70755) ;
#19716=VERTEX_POINT('',#70757) ;
#19717=VERTEX_POINT('',#70761) ;
#19718=VERTEX_POINT('',#70763) ;
#19719=VERTEX_POINT('',#70769) ;
#19720=VERTEX_POINT('',#70771) ;
#19721=VERTEX_POINT('',#70775) ;
#19722=VERTEX_POINT('',#70777) ;
#19723=VERTEX_POINT('',#70974) ;
#19724=VERTEX_POINT('',#70976) ;
#19725=VERTEX_POINT('',#70980) ;
#19726=VERTEX_POINT('',#70982) ;
#19727=VERTEX_POINT('',#70988) ;
#19728=VERTEX_POINT('',#70990) ;
#19729=VERTEX_POINT('',#70994) ;
#19730=VERTEX_POINT('',#70996) ;
#19731=VERTEX_POINT('',#71074) ;
#19732=VERTEX_POINT('',#71198) ;
#19733=VERTEX_POINT('',#71200) ;
#19734=VERTEX_POINT('',#71204) ;
#19735=VERTEX_POINT('',#71206) ;
#19736=VERTEX_POINT('',#71212) ;
#19737=VERTEX_POINT('',#71214) ;
#19738=VERTEX_POINT('',#71218) ;
#19739=VERTEX_POINT('',#71220) ;
#19740=VERTEX_POINT('',#71426) ;
#19741=VERTEX_POINT('',#71428) ;
#19742=VERTEX_POINT('',#71432) ;
#19743=VERTEX_POINT('',#71434) ;
#19744=VERTEX_POINT('',#71440) ;
#19745=VERTEX_POINT('',#71442) ;
#19746=VERTEX_POINT('',#71446) ;
#19747=VERTEX_POINT('',#71448) ;
#19748=VERTEX_POINT('',#71645) ;
#19749=VERTEX_POINT('',#71647) ;
#19750=VERTEX_POINT('',#71651) ;
#19751=VERTEX_POINT('',#71653) ;
#19752=VERTEX_POINT('',#71659) ;
#19753=VERTEX_POINT('',#71661) ;
#19754=VERTEX_POINT('',#71665) ;
#19755=VERTEX_POINT('',#71667) ;
#19756=VERTEX_POINT('',#71864) ;
#19757=VERTEX_POINT('',#71866) ;
#19758=VERTEX_POINT('',#71870) ;
#19759=VERTEX_POINT('',#71872) ;
#19760=VERTEX_POINT('',#71878) ;
#19761=VERTEX_POINT('',#71880) ;
#19762=VERTEX_POINT('',#71884) ;
#19763=VERTEX_POINT('',#71886) ;
#19764=VERTEX_POINT('',#72071) ;
#19765=VERTEX_POINT('',#72073) ;
#19766=VERTEX_POINT('',#72077) ;
#19767=VERTEX_POINT('',#72079) ;
#19768=VERTEX_POINT('',#72085) ;
#19769=VERTEX_POINT('',#72087) ;
#19770=VERTEX_POINT('',#72091) ;
#19771=VERTEX_POINT('',#72093) ;
#19772=VERTEX_POINT('',#72202) ;
#19773=VERTEX_POINT('',#72204) ;
#19774=VERTEX_POINT('',#72208) ;
#19775=VERTEX_POINT('',#72210) ;
#19776=VERTEX_POINT('',#72216) ;
#19777=VERTEX_POINT('',#72218) ;
#19778=VERTEX_POINT('',#72402) ;
#19779=VERTEX_POINT('',#72419) ;
#19780=VERTEX_POINT('',#72630) ;
#19781=VERTEX_POINT('',#72645) ;
#19782=VERTEX_POINT('',#72652) ;
#19783=VERTEX_POINT('',#72661) ;
#19784=VERTEX_POINT('',#72680) ;
#19785=VERTEX_POINT('',#72697) ;
#19786=VERTEX_POINT('',#72704) ;
#19787=VERTEX_POINT('',#72713) ;
#19788=VERTEX_POINT('',#72728) ;
#19789=VERTEX_POINT('',#72735) ;
#19790=VERTEX_POINT('',#72940) ;
#19791=VERTEX_POINT('',#72955) ;
#19792=VERTEX_POINT('',#72974) ;
#19793=VERTEX_POINT('',#72991) ;
#19794=VERTEX_POINT('',#72998) ;
#19795=VERTEX_POINT('',#73007) ;
#19796=VERTEX_POINT('',#73022) ;
#19797=VERTEX_POINT('',#73029) ;
#19798=VERTEX_POINT('',#73231) ;
#19799=VERTEX_POINT('',#73246) ;
#19800=VERTEX_POINT('',#73265) ;
#19801=VERTEX_POINT('',#73282) ;
#19802=VERTEX_POINT('',#73289) ;
#19803=VERTEX_POINT('',#73298) ;
#19804=VERTEX_POINT('',#73313) ;
#19805=VERTEX_POINT('',#73320) ;
#19806=VERTEX_POINT('',#73434) ;
#19807=VERTEX_POINT('',#73449) ;
#19808=VERTEX_POINT('',#73468) ;
#19809=VERTEX_POINT('',#73485) ;
#19810=VERTEX_POINT('',#73492) ;
#19811=VERTEX_POINT('',#73501) ;
#19812=VERTEX_POINT('',#73516) ;
#19813=VERTEX_POINT('',#73523) ;
#19814=VERTEX_POINT('',#73710) ;
#19815=VERTEX_POINT('',#73725) ;
#19816=VERTEX_POINT('',#73744) ;
#19817=VERTEX_POINT('',#73761) ;
#19818=VERTEX_POINT('',#73768) ;
#19819=VERTEX_POINT('',#73777) ;
#19820=VERTEX_POINT('',#73792) ;
#19821=VERTEX_POINT('',#73799) ;
#19822=VERTEX_POINT('',#74001) ;
#19823=VERTEX_POINT('',#74016) ;
#19824=VERTEX_POINT('',#74035) ;
#19825=VERTEX_POINT('',#74052) ;
#19826=VERTEX_POINT('',#74059) ;
#19827=VERTEX_POINT('',#74068) ;
#19828=VERTEX_POINT('',#74083) ;
#19829=VERTEX_POINT('',#74090) ;
#19830=VERTEX_POINT('',#74295) ;
#19831=VERTEX_POINT('',#74310) ;
#19832=VERTEX_POINT('',#74329) ;
#19833=VERTEX_POINT('',#74346) ;
#19834=VERTEX_POINT('',#74353) ;
#19835=VERTEX_POINT('',#74362) ;
#19836=VERTEX_POINT('',#74377) ;
#19837=VERTEX_POINT('',#74384) ;
#19838=VERTEX_POINT('',#74571) ;
#19839=VERTEX_POINT('',#74586) ;
#19840=VERTEX_POINT('',#74605) ;
#19841=VERTEX_POINT('',#74622) ;
#19842=VERTEX_POINT('',#74629) ;
#19843=VERTEX_POINT('',#74638) ;
#19844=VERTEX_POINT('',#74653) ;
#19845=VERTEX_POINT('',#74660) ;
#19846=VERTEX_POINT('',#74774) ;
#19847=VERTEX_POINT('',#74789) ;
#19848=VERTEX_POINT('',#74808) ;
#19849=VERTEX_POINT('',#74825) ;
#19850=VERTEX_POINT('',#74832) ;
#19851=VERTEX_POINT('',#74841) ;
#19852=VERTEX_POINT('',#74856) ;
#19853=VERTEX_POINT('',#74863) ;
#19854=VERTEX_POINT('',#75053) ;
#19855=VERTEX_POINT('',#75068) ;
#19856=VERTEX_POINT('',#75085) ;
#19857=VERTEX_POINT('',#75092) ;
#19858=VERTEX_POINT('',#75141) ;
#19859=VERTEX_POINT('',#75145) ;
#19860=VERTEX_POINT('',#75147) ;
#19861=VERTEX_POINT('',#75151) ;
#19862=VERTEX_POINT('',#75153) ;
#19863=VERTEX_POINT('',#75155) ;
#19864=VERTEX_POINT('',#75157) ;
#19865=VERTEX_POINT('',#75159) ;
#19866=VERTEX_POINT('',#75161) ;
#19867=VERTEX_POINT('',#75163) ;
#19868=VERTEX_POINT('',#75165) ;
#19869=VERTEX_POINT('',#75167) ;
#19870=VERTEX_POINT('',#75169) ;
#19871=VERTEX_POINT('',#75171) ;
#19872=VERTEX_POINT('',#75173) ;
#19873=VERTEX_POINT('',#75175) ;
#19874=VERTEX_POINT('',#75177) ;
#19875=VERTEX_POINT('',#75179) ;
#19876=VERTEX_POINT('',#75181) ;
#19877=VERTEX_POINT('',#75183) ;
#19878=VERTEX_POINT('',#75185) ;
#19879=VERTEX_POINT('',#75187) ;
#19880=VERTEX_POINT('',#75189) ;
#19881=VERTEX_POINT('',#75191) ;
#19882=VERTEX_POINT('',#75193) ;
#19883=VERTEX_POINT('',#75195) ;
#19884=VERTEX_POINT('',#75199) ;
#19885=VERTEX_POINT('',#75210) ;
#19886=VERTEX_POINT('',#75212) ;
#19887=VERTEX_POINT('',#75219) ;
#19888=VERTEX_POINT('',#75226) ;
#19889=VERTEX_POINT('',#75249) ;
#19890=VERTEX_POINT('',#75255) ;
#19891=VERTEX_POINT('',#75257) ;
#19892=VERTEX_POINT('',#75266) ;
#19893=VERTEX_POINT('',#75268) ;
#19894=VERTEX_POINT('',#75274) ;
#23775=EDGE_CURVE('',#19561,#19561,#17034,.T.) ;
#23776=EDGE_CURVE('',#19561,#19562,#17035,.T.) ;
#23777=EDGE_CURVE('',#19562,#19562,#17036,.T.) ;
#23778=EDGE_CURVE('',#19562,#19563,#3032,.T.) ;
#23779=EDGE_CURVE('',#19564,#19563,#17037,.T.) ;
#23780=EDGE_CURVE('',#19565,#19564,#3033,.T.) ;
#23781=EDGE_CURVE('',#19566,#19565,#17038,.T.) ;
#23782=EDGE_CURVE('',#19567,#19566,#3034,.T.) ;
#23783=EDGE_CURVE('',#19568,#19567,#17039,.T.) ;
#23784=EDGE_CURVE('',#19569,#19568,#3035,.T.) ;
#23785=EDGE_CURVE('',#19570,#19569,#17040,.T.) ;
#23786=EDGE_CURVE('',#19571,#19570,#3036,.T.) ;
#23787=EDGE_CURVE('',#19572,#19571,#17041,.T.) ;
#23788=EDGE_CURVE('',#19573,#19572,#3037,.T.) ;
#23789=EDGE_CURVE('',#19574,#19573,#17042,.T.) ;
#23790=EDGE_CURVE('',#19575,#19574,#3038,.T.) ;
#23791=EDGE_CURVE('',#19576,#19575,#17043,.T.) ;
#23792=EDGE_CURVE('',#19577,#19576,#3039,.T.) ;
#23793=EDGE_CURVE('',#19578,#19577,#17044,.T.) ;
#23794=EDGE_CURVE('',#19579,#19578,#3040,.T.) ;
#23795=EDGE_CURVE('',#19580,#19579,#17045,.T.) ;
#23796=EDGE_CURVE('',#19581,#19580,#3041,.T.) ;
#23797=EDGE_CURVE('',#19582,#19581,#17046,.T.) ;
#23798=EDGE_CURVE('',#19583,#19582,#3042,.T.) ;
#23799=EDGE_CURVE('',#19584,#19583,#17047,.T.) ;
#23800=EDGE_CURVE('',#19585,#19584,#3043,.T.) ;
#23801=EDGE_CURVE('',#19586,#19585,#17048,.T.) ;
#23802=EDGE_CURVE('',#19587,#19586,#3044,.T.) ;
#23803=EDGE_CURVE('',#19588,#19587,#17049,.T.) ;
#23804=EDGE_CURVE('',#19589,#19588,#3045,.T.) ;
#23805=EDGE_CURVE('',#19590,#19589,#17050,.T.) ;
#23806=EDGE_CURVE('',#19591,#19590,#3046,.T.) ;
#23807=EDGE_CURVE('',#19592,#19591,#17051,.T.) ;
#23808=EDGE_CURVE('',#19593,#19592,#3047,.T.) ;
#23809=EDGE_CURVE('',#19594,#19593,#17052,.T.) ;
#23810=EDGE_CURVE('',#19595,#19594,#3048,.T.) ;
#23811=EDGE_CURVE('',#19596,#19595,#17053,.T.) ;
#23812=EDGE_CURVE('',#19597,#19596,#3049,.T.) ;
#23813=EDGE_CURVE('',#19598,#19597,#17054,.T.) ;
#23814=EDGE_CURVE('',#19599,#19598,#3050,.T.) ;
#23815=EDGE_CURVE('',#19600,#19599,#17055,.T.) ;
#23816=EDGE_CURVE('',#19601,#19600,#3051,.T.) ;
#23817=EDGE_CURVE('',#19602,#19601,#17056,.T.) ;
#23818=EDGE_CURVE('',#19603,#19602,#3052,.T.) ;
#23819=EDGE_CURVE('',#19604,#19603,#17057,.T.) ;
#23820=EDGE_CURVE('',#19605,#19604,#3053,.T.) ;
#23821=EDGE_CURVE('',#19606,#19605,#17058,.T.) ;
#23822=EDGE_CURVE('',#19607,#19606,#3054,.T.) ;
#23823=EDGE_CURVE('',#19608,#19607,#17059,.T.) ;
#23824=EDGE_CURVE('',#19609,#19608,#3055,.T.) ;
#23825=EDGE_CURVE('',#19610,#19609,#17060,.T.) ;
#23826=EDGE_CURVE('',#19611,#19610,#3056,.T.) ;
#23827=EDGE_CURVE('',#19612,#19611,#17061,.T.) ;
#23828=EDGE_CURVE('',#19613,#19612,#3057,.T.) ;
#23829=EDGE_CURVE('',#19614,#19613,#17062,.T.) ;
#23830=EDGE_CURVE('',#19615,#19614,#3058,.T.) ;
#23831=EDGE_CURVE('',#19616,#19615,#17063,.T.) ;
#23832=EDGE_CURVE('',#19617,#19616,#3059,.T.) ;
#23833=EDGE_CURVE('',#19618,#19617,#17064,.T.) ;
#23834=EDGE_CURVE('',#19619,#19618,#3060,.T.) ;
#23835=EDGE_CURVE('',#19620,#19619,#17065,.T.) ;
#23836=EDGE_CURVE('',#19621,#19620,#3061,.T.) ;
#23837=EDGE_CURVE('',#19622,#19621,#17066,.T.) ;
#23838=EDGE_CURVE('',#19623,#19622,#3062,.T.) ;
#23839=EDGE_CURVE('',#19624,#19623,#17067,.T.) ;
#23840=EDGE_CURVE('',#19625,#19624,#3063,.T.) ;
#23841=EDGE_CURVE('',#19626,#19625,#17068,.T.) ;
#23842=EDGE_CURVE('',#19627,#19626,#3064,.T.) ;
#23843=EDGE_CURVE('',#19628,#19627,#17069,.T.) ;
#23844=EDGE_CURVE('',#19629,#19628,#3065,.T.) ;
#23845=EDGE_CURVE('',#19630,#19629,#17070,.T.) ;
#23846=EDGE_CURVE('',#19631,#19630,#3066,.T.) ;
#23847=EDGE_CURVE('',#19632,#19631,#17071,.T.) ;
#23848=EDGE_CURVE('',#19633,#19632,#3067,.T.) ;
#23849=EDGE_CURVE('',#19634,#19633,#17072,.T.) ;
#23850=EDGE_CURVE('',#19635,#19634,#3068,.T.) ;
#23851=EDGE_CURVE('',#19636,#19635,#17073,.T.) ;
#23852=EDGE_CURVE('',#19637,#19636,#3069,.T.) ;
#23853=EDGE_CURVE('',#19638,#19637,#17074,.T.) ;
#23854=EDGE_CURVE('',#19639,#19638,#3070,.T.) ;
#23855=EDGE_CURVE('',#19640,#19639,#17075,.T.) ;
#23856=EDGE_CURVE('',#19641,#19640,#3071,.T.) ;
#23857=EDGE_CURVE('',#19642,#19641,#17076,.T.) ;
#23858=EDGE_CURVE('',#19643,#19642,#3072,.T.) ;
#23859=EDGE_CURVE('',#19563,#19643,#17077,.T.) ;
#23860=EDGE_CURVE('',#19644,#19645,#17078,.T.) ;
#23861=EDGE_CURVE('',#19645,#19646,#3073,.T.) ;
#23862=EDGE_CURVE('',#19646,#19647,#17079,.T.) ;
#23863=EDGE_CURVE('',#19647,#19644,#3074,.T.) ;
#23864=EDGE_CURVE('',#19648,#19649,#17080,.T.) ;
#23865=EDGE_CURVE('',#19649,#19650,#3075,.T.) ;
#23866=EDGE_CURVE('',#19650,#19651,#17081,.T.) ;
#23867=EDGE_CURVE('',#19651,#19648,#3076,.T.) ;
#23868=EDGE_CURVE('',#19652,#19653,#17082,.T.) ;
#23869=EDGE_CURVE('',#19653,#19651,#17083,.T.) ;
#23870=EDGE_CURVE('',#19650,#19652,#17084,.T.) ;
#23871=EDGE_CURVE('',#19645,#19654,#17085,.T.) ;
#23872=EDGE_CURVE('',#19654,#19653,#3077,.T.) ;
#23873=EDGE_CURVE('',#19652,#19645,#3078,.T.) ;
#23874=EDGE_CURVE('',#19655,#19656,#17086,.T.) ;
#23875=EDGE_CURVE('',#19656,#19649,#3079,.T.) ;
#23876=EDGE_CURVE('',#19649,#19657,#17087,.T.) ;
#23877=EDGE_CURVE('',#19657,#19655,#3080,.T.) ;
#23878=EDGE_CURVE('',#19658,#19659,#17088,.T.) ;
#23879=EDGE_CURVE('',#19659,#19660,#3081,.T.) ;
#23880=EDGE_CURVE('',#19660,#19661,#17089,.T.) ;
#23881=EDGE_CURVE('',#19661,#19658,#3082,.T.) ;
#23882=EDGE_CURVE('',#19662,#19663,#17090,.T.) ;
#23883=EDGE_CURVE('',#19663,#19661,#17091,.T.) ;
#23884=EDGE_CURVE('',#19660,#19662,#17092,.T.) ;
#23885=EDGE_CURVE('',#19656,#19664,#17093,.T.) ;
#23886=EDGE_CURVE('',#19664,#19663,#3083,.T.) ;
#23887=EDGE_CURVE('',#19662,#19656,#3084,.T.) ;
#23888=EDGE_CURVE('',#19665,#19666,#17094,.T.) ;
#23889=EDGE_CURVE('',#19666,#19659,#3085,.T.) ;
#23890=EDGE_CURVE('',#19659,#19667,#17095,.T.) ;
#23891=EDGE_CURVE('',#19667,#19665,#3086,.T.) ;
#23892=EDGE_CURVE('',#19668,#19669,#17096,.T.) ;
#23893=EDGE_CURVE('',#19669,#19670,#3087,.T.) ;
#23894=EDGE_CURVE('',#19670,#19671,#17097,.T.) ;
#23895=EDGE_CURVE('',#19671,#19668,#3088,.T.) ;
#23896=EDGE_CURVE('',#19672,#19673,#17098,.T.) ;
#23897=EDGE_CURVE('',#19673,#19671,#17099,.T.) ;
#23898=EDGE_CURVE('',#19670,#19672,#17100,.T.) ;
#23899=EDGE_CURVE('',#19666,#19674,#17101,.T.) ;
#23900=EDGE_CURVE('',#19674,#19673,#3089,.T.) ;
#23901=EDGE_CURVE('',#19672,#19666,#3090,.T.) ;
#23902=EDGE_CURVE('',#19675,#19676,#17102,.T.) ;
#23903=EDGE_CURVE('',#19676,#19669,#3091,.T.) ;
#23904=EDGE_CURVE('',#19669,#19677,#17103,.T.) ;
#23905=EDGE_CURVE('',#19677,#19675,#3092,.T.) ;
#23906=EDGE_CURVE('',#19678,#19679,#17104,.T.) ;
#23907=EDGE_CURVE('',#19679,#19680,#17105,.T.) ;
#23908=EDGE_CURVE('',#19680,#19681,#17106,.T.) ;
#23909=EDGE_CURVE('',#19681,#19678,#17107,.T.) ;
#23910=EDGE_CURVE('',#19676,#19682,#17108,.T.) ;
#23911=EDGE_CURVE('',#19682,#19681,#3093,.T.) ;
#23912=EDGE_CURVE('',#19680,#19676,#3094,.T.) ;
#23913=EDGE_CURVE('',#19683,#19646,#17109,.T.) ;
#23914=EDGE_CURVE('',#19646,#19679,#3095,.T.) ;
#23915=EDGE_CURVE('',#19678,#19683,#3096,.T.) ;
#23916=EDGE_CURVE('',#19675,#19682,#17110,.T.) ;
#23917=EDGE_CURVE('',#19668,#19677,#17111,.T.) ;
#23918=EDGE_CURVE('',#19665,#19674,#17112,.T.) ;
#23919=EDGE_CURVE('',#19658,#19667,#17113,.T.) ;
#23920=EDGE_CURVE('',#19655,#19664,#17114,.T.) ;
#23921=EDGE_CURVE('',#19648,#19657,#17115,.T.) ;
#23922=EDGE_CURVE('',#19644,#19654,#17116,.T.) ;
#23923=EDGE_CURVE('',#19683,#19647,#17117,.T.) ;
#23924=EDGE_CURVE('',#19684,#19664,#3097,.T.) ;
#23925=EDGE_CURVE('',#19685,#19684,#3098,.T.) ;
#23926=EDGE_CURVE('',#19663,#19685,#3099,.T.) ;
#23927=EDGE_CURVE('',#19655,#19686,#3100,.T.) ;
#23928=EDGE_CURVE('',#19686,#19684,#17118,.F.) ;
#23929=EDGE_CURVE('',#19687,#19657,#3101,.T.) ;
#23930=EDGE_CURVE('',#19686,#19687,#3102,.T.) ;
#23931=EDGE_CURVE('',#19648,#19688,#3103,.T.) ;
#23932=EDGE_CURVE('',#19688,#19687,#17119,.F.) ;
#23933=EDGE_CURVE('',#19689,#19651,#3104,.T.) ;
#23934=EDGE_CURVE('',#19688,#19689,#3105,.T.) ;
#23935=EDGE_CURVE('',#19653,#19690,#3106,.T.) ;
#23936=EDGE_CURVE('',#19689,#19690,#17120,.T.) ;
#23937=EDGE_CURVE('',#19691,#19654,#3107,.T.) ;
#23938=EDGE_CURVE('',#19690,#19691,#3108,.T.) ;
#23939=EDGE_CURVE('',#19644,#19692,#3109,.T.) ;
#23940=EDGE_CURVE('',#19692,#19691,#17121,.F.) ;
#23941=EDGE_CURVE('',#19693,#19647,#3110,.T.) ;
#23942=EDGE_CURVE('',#19692,#19693,#3111,.T.) ;
#23943=EDGE_CURVE('',#19683,#19694,#3112,.T.) ;
#23944=EDGE_CURVE('',#19694,#19693,#17122,.F.) ;
#23945=EDGE_CURVE('',#19695,#19678,#3113,.T.) ;
#23946=EDGE_CURVE('',#19694,#19695,#3114,.T.) ;
#23947=EDGE_CURVE('',#19681,#19696,#3115,.T.) ;
#23948=EDGE_CURVE('',#19695,#19696,#17123,.T.) ;
#23949=EDGE_CURVE('',#19697,#19629,#17124,.F.) ;
#23950=EDGE_CURVE('',#19698,#19697,#17125,.F.) ;
#23951=EDGE_CURVE('',#19629,#19698,#17126,.F.) ;
#23952=EDGE_CURVE('',#19626,#19699,#17127,.F.) ;
#23953=EDGE_CURVE('',#19700,#19626,#17128,.F.) ;
#23954=EDGE_CURVE('',#19699,#19700,#17129,.F.) ;
#23955=EDGE_CURVE('',#19630,#19701,#17130,.F.) ;
#23956=EDGE_CURVE('',#19702,#19630,#17131,.F.) ;
#23957=EDGE_CURVE('',#19701,#19702,#17132,.F.) ;
#23958=EDGE_CURVE('',#19698,#19702,#17133,.T.) ;
#23959=EDGE_CURVE('',#19703,#19625,#17134,.F.) ;
#23960=EDGE_CURVE('',#19704,#19703,#17135,.F.) ;
#23961=EDGE_CURVE('',#19625,#19704,#17136,.F.) ;
#23962=EDGE_CURVE('',#19705,#19633,#17137,.F.) ;
#23963=EDGE_CURVE('',#19706,#19705,#17138,.F.) ;
#23964=EDGE_CURVE('',#19633,#19706,#17139,.F.) ;
#23965=EDGE_CURVE('',#19702,#19706,#774,.T.) ;
#23966=EDGE_CURVE('',#19705,#19701,#775,.T.) ;
#23967=EDGE_CURVE('',#19622,#19707,#17140,.F.) ;
#23968=EDGE_CURVE('',#19708,#19622,#17141,.F.) ;
#23969=EDGE_CURVE('',#19707,#19708,#17142,.F.) ;
#23970=EDGE_CURVE('',#19634,#19709,#17143,.F.) ;
#23971=EDGE_CURVE('',#19710,#19634,#17144,.F.) ;
#23972=EDGE_CURVE('',#19709,#19710,#17145,.F.) ;
#23973=EDGE_CURVE('',#19706,#19710,#17146,.T.) ;
#23974=EDGE_CURVE('',#19711,#19621,#17147,.F.) ;
#23975=EDGE_CURVE('',#19712,#19711,#17148,.F.) ;
#23976=EDGE_CURVE('',#19621,#19712,#17149,.F.) ;
#23977=EDGE_CURVE('',#19713,#19637,#17150,.F.) ;
#23978=EDGE_CURVE('',#19714,#19713,#17151,.F.) ;
#23979=EDGE_CURVE('',#19637,#19714,#17152,.F.) ;
#23980=EDGE_CURVE('',#19710,#19714,#776,.T.) ;
#23981=EDGE_CURVE('',#19713,#19709,#777,.T.) ;
#23982=EDGE_CURVE('',#19618,#19715,#17153,.F.) ;
#23983=EDGE_CURVE('',#19716,#19618,#17154,.F.) ;
#23984=EDGE_CURVE('',#19715,#19716,#17155,.F.) ;
#23985=EDGE_CURVE('',#19638,#19717,#17156,.F.) ;
#23986=EDGE_CURVE('',#19718,#19638,#17157,.F.) ;
#23987=EDGE_CURVE('',#19717,#19718,#17158,.F.) ;
#23988=EDGE_CURVE('',#19714,#19718,#17159,.T.) ;
#23989=EDGE_CURVE('',#19719,#19617,#17160,.F.) ;
#23990=EDGE_CURVE('',#19720,#19719,#17161,.F.) ;
#23991=EDGE_CURVE('',#19617,#19720,#17162,.F.) ;
#23992=EDGE_CURVE('',#19721,#19641,#17163,.F.) ;
#23993=EDGE_CURVE('',#19722,#19721,#17164,.F.) ;
#23994=EDGE_CURVE('',#19641,#19722,#17165,.F.) ;
#23995=EDGE_CURVE('',#19718,#19722,#778,.T.) ;
#23996=EDGE_CURVE('',#19721,#19717,#779,.T.) ;
#23997=EDGE_CURVE('',#19614,#19723,#17166,.F.) ;
#23998=EDGE_CURVE('',#19724,#19614,#17167,.F.) ;
#23999=EDGE_CURVE('',#19723,#19724,#17168,.F.) ;
#24000=EDGE_CURVE('',#19642,#19725,#17169,.F.) ;
#24001=EDGE_CURVE('',#19726,#19642,#17170,.F.) ;
#24002=EDGE_CURVE('',#19725,#19726,#17171,.F.) ;
#24003=EDGE_CURVE('',#19722,#19726,#17172,.T.) ;
#24004=EDGE_CURVE('',#19727,#19613,#17173,.F.) ;
#24005=EDGE_CURVE('',#19728,#19727,#17174,.F.) ;
#24006=EDGE_CURVE('',#19613,#19728,#17175,.F.) ;
#24007=EDGE_CURVE('',#19729,#19565,#17176,.F.) ;
#24008=EDGE_CURVE('',#19730,#19729,#17177,.F.) ;
#24009=EDGE_CURVE('',#19565,#19730,#17178,.F.) ;
#24010=EDGE_CURVE('',#19726,#19731,#780,.T.) ;
#24011=EDGE_CURVE('',#19731,#19730,#781,.T.) ;
#24012=EDGE_CURVE('',#19729,#19725,#782,.T.) ;
#24013=EDGE_CURVE('',#19610,#19732,#17179,.F.) ;
#24014=EDGE_CURVE('',#19733,#19610,#17180,.F.) ;
#24015=EDGE_CURVE('',#19732,#19733,#17181,.F.) ;
#24016=EDGE_CURVE('',#19566,#19734,#17182,.F.) ;
#24017=EDGE_CURVE('',#19735,#19566,#17183,.F.) ;
#24018=EDGE_CURVE('',#19734,#19735,#17184,.F.) ;
#24019=EDGE_CURVE('',#19730,#19735,#17185,.T.) ;
#24020=EDGE_CURVE('',#19736,#19609,#17186,.F.) ;
#24021=EDGE_CURVE('',#19737,#19736,#17187,.F.) ;
#24022=EDGE_CURVE('',#19609,#19737,#17188,.F.) ;
#24023=EDGE_CURVE('',#19738,#19569,#17189,.F.) ;
#24024=EDGE_CURVE('',#19739,#19738,#17190,.F.) ;
#24025=EDGE_CURVE('',#19569,#19739,#17191,.F.) ;
#24026=EDGE_CURVE('',#19735,#19739,#783,.T.) ;
#24027=EDGE_CURVE('',#19738,#19734,#784,.T.) ;
#24028=EDGE_CURVE('',#19606,#19740,#17192,.F.) ;
#24029=EDGE_CURVE('',#19741,#19606,#17193,.F.) ;
#24030=EDGE_CURVE('',#19740,#19741,#17194,.F.) ;
#24031=EDGE_CURVE('',#19570,#19742,#17195,.F.) ;
#24032=EDGE_CURVE('',#19743,#19570,#17196,.F.) ;
#24033=EDGE_CURVE('',#19742,#19743,#17197,.F.) ;
#24034=EDGE_CURVE('',#19739,#19743,#17198,.T.) ;
#24035=EDGE_CURVE('',#19744,#19605,#17199,.F.) ;
#24036=EDGE_CURVE('',#19745,#19744,#17200,.F.) ;
#24037=EDGE_CURVE('',#19605,#19745,#17201,.F.) ;
#24038=EDGE_CURVE('',#19746,#19573,#17202,.F.) ;
#24039=EDGE_CURVE('',#19747,#19746,#17203,.F.) ;
#24040=EDGE_CURVE('',#19573,#19747,#17204,.F.) ;
#24041=EDGE_CURVE('',#19743,#19747,#785,.T.) ;
#24042=EDGE_CURVE('',#19746,#19742,#786,.T.) ;
#24043=EDGE_CURVE('',#19602,#19748,#17205,.F.) ;
#24044=EDGE_CURVE('',#19749,#19602,#17206,.F.) ;
#24045=EDGE_CURVE('',#19748,#19749,#17207,.F.) ;
#24046=EDGE_CURVE('',#19574,#19750,#17208,.F.) ;
#24047=EDGE_CURVE('',#19751,#19574,#17209,.F.) ;
#24048=EDGE_CURVE('',#19750,#19751,#17210,.F.) ;
#24049=EDGE_CURVE('',#19747,#19751,#17211,.T.) ;
#24050=EDGE_CURVE('',#19752,#19601,#17212,.F.) ;
#24051=EDGE_CURVE('',#19753,#19752,#17213,.F.) ;
#24052=EDGE_CURVE('',#19601,#19753,#17214,.F.) ;
#24053=EDGE_CURVE('',#19754,#19577,#17215,.F.) ;
#24054=EDGE_CURVE('',#19755,#19754,#17216,.F.) ;
#24055=EDGE_CURVE('',#19577,#19755,#17217,.F.) ;
#24056=EDGE_CURVE('',#19751,#19755,#787,.T.) ;
#24057=EDGE_CURVE('',#19754,#19750,#788,.T.) ;
#24058=EDGE_CURVE('',#19598,#19756,#17218,.F.) ;
#24059=EDGE_CURVE('',#19757,#19598,#17219,.F.) ;
#24060=EDGE_CURVE('',#19756,#19757,#17220,.F.) ;
#24061=EDGE_CURVE('',#19578,#19758,#17221,.F.) ;
#24062=EDGE_CURVE('',#19759,#19578,#17222,.F.) ;
#24063=EDGE_CURVE('',#19758,#19759,#17223,.F.) ;
#24064=EDGE_CURVE('',#19755,#19759,#17224,.T.) ;
#24065=EDGE_CURVE('',#19760,#19597,#17225,.F.) ;
#24066=EDGE_CURVE('',#19761,#19760,#17226,.F.) ;
#24067=EDGE_CURVE('',#19597,#19761,#17227,.F.) ;
#24068=EDGE_CURVE('',#19762,#19581,#17228,.F.) ;
#24069=EDGE_CURVE('',#19763,#19762,#17229,.F.) ;
#24070=EDGE_CURVE('',#19581,#19763,#17230,.F.) ;
#24071=EDGE_CURVE('',#19759,#19763,#789,.T.) ;
#24072=EDGE_CURVE('',#19762,#19758,#790,.T.) ;
#24073=EDGE_CURVE('',#19594,#19764,#17231,.F.) ;
#24074=EDGE_CURVE('',#19765,#19594,#17232,.F.) ;
#24075=EDGE_CURVE('',#19764,#19765,#17233,.F.) ;
#24076=EDGE_CURVE('',#19582,#19766,#17234,.F.) ;
#24077=EDGE_CURVE('',#19767,#19582,#17235,.F.) ;
#24078=EDGE_CURVE('',#19766,#19767,#17236,.F.) ;
#24079=EDGE_CURVE('',#19763,#19767,#17237,.T.) ;
#24080=EDGE_CURVE('',#19768,#19593,#17238,.F.) ;
#24081=EDGE_CURVE('',#19769,#19768,#17239,.F.) ;
#24082=EDGE_CURVE('',#19593,#19769,#17240,.F.) ;
#24083=EDGE_CURVE('',#19770,#19585,#17241,.F.) ;
#24084=EDGE_CURVE('',#19771,#19770,#17242,.F.) ;
#24085=EDGE_CURVE('',#19585,#19771,#17243,.F.) ;
#24086=EDGE_CURVE('',#19767,#19771,#791,.T.) ;
#24087=EDGE_CURVE('',#19770,#19766,#792,.T.) ;
#24088=EDGE_CURVE('',#19590,#19772,#17244,.F.) ;
#24089=EDGE_CURVE('',#19773,#19590,#17245,.F.) ;
#24090=EDGE_CURVE('',#19772,#19773,#17246,.F.) ;
#24091=EDGE_CURVE('',#19586,#19774,#17247,.F.) ;
#24092=EDGE_CURVE('',#19775,#19586,#17248,.F.) ;
#24093=EDGE_CURVE('',#19774,#19775,#17249,.F.) ;
#24094=EDGE_CURVE('',#19771,#19775,#17250,.T.) ;
#24095=EDGE_CURVE('',#19776,#19589,#17251,.F.) ;
#24096=EDGE_CURVE('',#19777,#19776,#17252,.F.) ;
#24097=EDGE_CURVE('',#19589,#19777,#17253,.F.) ;
#24098=EDGE_CURVE('',#19775,#19777,#793,.T.) ;
#24099=EDGE_CURVE('',#19776,#19774,#794,.T.) ;
#24100=EDGE_CURVE('',#19777,#19773,#17254,.T.) ;
#24101=EDGE_CURVE('',#19778,#19776,#3116,.T.) ;
#24102=EDGE_CURVE('',#19588,#19778,#795,.T.) ;
#24103=EDGE_CURVE('',#19774,#19779,#3117,.T.) ;
#24104=EDGE_CURVE('',#19779,#19587,#796,.T.) ;
#24105=EDGE_CURVE('',#19773,#19769,#797,.T.) ;
#24106=EDGE_CURVE('',#19768,#19772,#798,.T.) ;
#24107=EDGE_CURVE('',#19772,#19780,#3118,.T.) ;
#24108=EDGE_CURVE('',#19780,#19591,#799,.T.) ;
#24109=EDGE_CURVE('',#19779,#19781,#800,.T.) ;
#24110=EDGE_CURVE('',#19781,#19782,#17255,.T.) ;
#24111=EDGE_CURVE('',#19782,#19778,#801,.T.) ;
#24112=EDGE_CURVE('',#19783,#19770,#3119,.T.) ;
#24113=EDGE_CURVE('',#19584,#19783,#802,.T.) ;
#24114=EDGE_CURVE('',#19769,#19765,#17256,.T.) ;
#24115=EDGE_CURVE('',#19784,#19768,#3120,.T.) ;
#24116=EDGE_CURVE('',#19592,#19784,#803,.T.) ;
#24117=EDGE_CURVE('',#19780,#19785,#804,.T.) ;
#24118=EDGE_CURVE('',#19785,#19786,#17257,.T.) ;
#24119=EDGE_CURVE('',#19786,#19784,#805,.T.) ;
#24120=EDGE_CURVE('',#19766,#19787,#3121,.T.) ;
#24121=EDGE_CURVE('',#19787,#19583,#806,.T.) ;
#24122=EDGE_CURVE('',#19787,#19788,#807,.T.) ;
#24123=EDGE_CURVE('',#19788,#19789,#17258,.T.) ;
#24124=EDGE_CURVE('',#19789,#19783,#808,.T.) ;
#24125=EDGE_CURVE('',#19765,#19761,#809,.T.) ;
#24126=EDGE_CURVE('',#19760,#19764,#810,.T.) ;
#24127=EDGE_CURVE('',#19764,#19790,#3122,.T.) ;
#24128=EDGE_CURVE('',#19790,#19595,#811,.T.) ;
#24129=EDGE_CURVE('',#19791,#19762,#3123,.T.) ;
#24130=EDGE_CURVE('',#19580,#19791,#812,.T.) ;
#24131=EDGE_CURVE('',#19761,#19757,#17259,.T.) ;
#24132=EDGE_CURVE('',#19792,#19760,#3124,.T.) ;
#24133=EDGE_CURVE('',#19596,#19792,#813,.T.) ;
#24134=EDGE_CURVE('',#19790,#19793,#814,.T.) ;
#24135=EDGE_CURVE('',#19793,#19794,#17260,.T.) ;
#24136=EDGE_CURVE('',#19794,#19792,#815,.T.) ;
#24137=EDGE_CURVE('',#19758,#19795,#3125,.T.) ;
#24138=EDGE_CURVE('',#19795,#19579,#816,.T.) ;
#24139=EDGE_CURVE('',#19795,#19796,#817,.T.) ;
#24140=EDGE_CURVE('',#19796,#19797,#17261,.T.) ;
#24141=EDGE_CURVE('',#19797,#19791,#818,.T.) ;
#24142=EDGE_CURVE('',#19757,#19753,#819,.T.) ;
#24143=EDGE_CURVE('',#19752,#19756,#820,.T.) ;
#24144=EDGE_CURVE('',#19756,#19798,#3126,.T.) ;
#24145=EDGE_CURVE('',#19798,#19599,#821,.T.) ;
#24146=EDGE_CURVE('',#19799,#19754,#3127,.T.) ;
#24147=EDGE_CURVE('',#19576,#19799,#822,.T.) ;
#24148=EDGE_CURVE('',#19753,#19749,#17262,.T.) ;
#24149=EDGE_CURVE('',#19800,#19752,#3128,.T.) ;
#24150=EDGE_CURVE('',#19600,#19800,#823,.T.) ;
#24151=EDGE_CURVE('',#19798,#19801,#824,.T.) ;
#24152=EDGE_CURVE('',#19801,#19802,#17263,.T.) ;
#24153=EDGE_CURVE('',#19802,#19800,#825,.T.) ;
#24154=EDGE_CURVE('',#19750,#19803,#3129,.T.) ;
#24155=EDGE_CURVE('',#19803,#19575,#826,.T.) ;
#24156=EDGE_CURVE('',#19803,#19804,#827,.T.) ;
#24157=EDGE_CURVE('',#19804,#19805,#17264,.T.) ;
#24158=EDGE_CURVE('',#19805,#19799,#828,.T.) ;
#24159=EDGE_CURVE('',#19749,#19745,#829,.T.) ;
#24160=EDGE_CURVE('',#19744,#19748,#830,.T.) ;
#24161=EDGE_CURVE('',#19748,#19806,#3130,.T.) ;
#24162=EDGE_CURVE('',#19806,#19603,#831,.T.) ;
#24163=EDGE_CURVE('',#19807,#19746,#3131,.T.) ;
#24164=EDGE_CURVE('',#19572,#19807,#832,.T.) ;
#24165=EDGE_CURVE('',#19745,#19741,#17265,.T.) ;
#24166=EDGE_CURVE('',#19808,#19744,#3132,.T.) ;
#24167=EDGE_CURVE('',#19604,#19808,#833,.T.) ;
#24168=EDGE_CURVE('',#19806,#19809,#834,.T.) ;
#24169=EDGE_CURVE('',#19809,#19810,#17266,.T.) ;
#24170=EDGE_CURVE('',#19810,#19808,#835,.T.) ;
#24171=EDGE_CURVE('',#19742,#19811,#3133,.T.) ;
#24172=EDGE_CURVE('',#19811,#19571,#836,.T.) ;
#24173=EDGE_CURVE('',#19811,#19812,#837,.T.) ;
#24174=EDGE_CURVE('',#19812,#19813,#17267,.T.) ;
#24175=EDGE_CURVE('',#19813,#19807,#838,.T.) ;
#24176=EDGE_CURVE('',#19741,#19737,#839,.T.) ;
#24177=EDGE_CURVE('',#19736,#19740,#840,.T.) ;
#24178=EDGE_CURVE('',#19740,#19814,#3134,.T.) ;
#24179=EDGE_CURVE('',#19814,#19607,#841,.T.) ;
#24180=EDGE_CURVE('',#19815,#19738,#3135,.T.) ;
#24181=EDGE_CURVE('',#19568,#19815,#842,.T.) ;
#24182=EDGE_CURVE('',#19737,#19733,#17268,.T.) ;
#24183=EDGE_CURVE('',#19816,#19736,#3136,.T.) ;
#24184=EDGE_CURVE('',#19608,#19816,#843,.T.) ;
#24185=EDGE_CURVE('',#19814,#19817,#844,.T.) ;
#24186=EDGE_CURVE('',#19817,#19818,#17269,.T.) ;
#24187=EDGE_CURVE('',#19818,#19816,#845,.T.) ;
#24188=EDGE_CURVE('',#19734,#19819,#3137,.T.) ;
#24189=EDGE_CURVE('',#19819,#19567,#846,.T.) ;
#24190=EDGE_CURVE('',#19819,#19820,#847,.T.) ;
#24191=EDGE_CURVE('',#19820,#19821,#17270,.T.) ;
#24192=EDGE_CURVE('',#19821,#19815,#848,.T.) ;
#24193=EDGE_CURVE('',#19733,#19728,#849,.T.) ;
#24194=EDGE_CURVE('',#19727,#19732,#850,.T.) ;
#24195=EDGE_CURVE('',#19732,#19822,#3138,.T.) ;
#24196=EDGE_CURVE('',#19822,#19611,#851,.T.) ;
#24197=EDGE_CURVE('',#19823,#19729,#3139,.T.) ;
#24198=EDGE_CURVE('',#19564,#19823,#852,.T.) ;
#24199=EDGE_CURVE('',#19728,#19724,#17271,.T.) ;
#24200=EDGE_CURVE('',#19824,#19727,#3140,.T.) ;
#24201=EDGE_CURVE('',#19612,#19824,#853,.T.) ;
#24202=EDGE_CURVE('',#19822,#19825,#854,.T.) ;
#24203=EDGE_CURVE('',#19825,#19826,#17272,.T.) ;
#24204=EDGE_CURVE('',#19826,#19824,#855,.T.) ;
#24205=EDGE_CURVE('',#19725,#19827,#3141,.T.) ;
#24206=EDGE_CURVE('',#19827,#19643,#856,.T.) ;
#24207=EDGE_CURVE('',#19827,#19828,#857,.T.) ;
#24208=EDGE_CURVE('',#19828,#19829,#17273,.T.) ;
#24209=EDGE_CURVE('',#19829,#19823,#858,.T.) ;
#24210=EDGE_CURVE('',#19724,#19720,#859,.T.) ;
#24211=EDGE_CURVE('',#19719,#19723,#860,.T.) ;
#24212=EDGE_CURVE('',#19723,#19830,#3142,.T.) ;
#24213=EDGE_CURVE('',#19830,#19615,#861,.T.) ;
#24214=EDGE_CURVE('',#19831,#19721,#3143,.T.) ;
#24215=EDGE_CURVE('',#19640,#19831,#862,.T.) ;
#24216=EDGE_CURVE('',#19720,#19716,#17274,.T.) ;
#24217=EDGE_CURVE('',#19832,#19719,#3144,.T.) ;
#24218=EDGE_CURVE('',#19616,#19832,#863,.T.) ;
#24219=EDGE_CURVE('',#19830,#19833,#864,.T.) ;
#24220=EDGE_CURVE('',#19833,#19834,#17275,.T.) ;
#24221=EDGE_CURVE('',#19834,#19832,#865,.T.) ;
#24222=EDGE_CURVE('',#19717,#19835,#3145,.T.) ;
#24223=EDGE_CURVE('',#19835,#19639,#866,.T.) ;
#24224=EDGE_CURVE('',#19835,#19836,#867,.T.) ;
#24225=EDGE_CURVE('',#19836,#19837,#17276,.T.) ;
#24226=EDGE_CURVE('',#19837,#19831,#868,.T.) ;
#24227=EDGE_CURVE('',#19716,#19712,#869,.T.) ;
#24228=EDGE_CURVE('',#19711,#19715,#870,.T.) ;
#24229=EDGE_CURVE('',#19715,#19838,#3146,.T.) ;
#24230=EDGE_CURVE('',#19838,#19619,#871,.T.) ;
#24231=EDGE_CURVE('',#19839,#19713,#3147,.T.) ;
#24232=EDGE_CURVE('',#19636,#19839,#872,.T.) ;
#24233=EDGE_CURVE('',#19712,#19708,#17277,.T.) ;
#24234=EDGE_CURVE('',#19840,#19711,#3148,.T.) ;
#24235=EDGE_CURVE('',#19620,#19840,#873,.T.) ;
#24236=EDGE_CURVE('',#19838,#19841,#874,.T.) ;
#24237=EDGE_CURVE('',#19841,#19842,#17278,.T.) ;
#24238=EDGE_CURVE('',#19842,#19840,#875,.T.) ;
#24239=EDGE_CURVE('',#19709,#19843,#3149,.T.) ;
#24240=EDGE_CURVE('',#19843,#19635,#876,.T.) ;
#24241=EDGE_CURVE('',#19843,#19844,#877,.T.) ;
#24242=EDGE_CURVE('',#19844,#19845,#17279,.T.) ;
#24243=EDGE_CURVE('',#19845,#19839,#878,.T.) ;
#24244=EDGE_CURVE('',#19708,#19704,#879,.T.) ;
#24245=EDGE_CURVE('',#19703,#19707,#880,.T.) ;
#24246=EDGE_CURVE('',#19707,#19846,#3150,.T.) ;
#24247=EDGE_CURVE('',#19846,#19623,#881,.T.) ;
#24248=EDGE_CURVE('',#19847,#19705,#3151,.T.) ;
#24249=EDGE_CURVE('',#19632,#19847,#882,.T.) ;
#24250=EDGE_CURVE('',#19704,#19700,#17280,.T.) ;
#24251=EDGE_CURVE('',#19848,#19703,#3152,.T.) ;
#24252=EDGE_CURVE('',#19624,#19848,#883,.T.) ;
#24253=EDGE_CURVE('',#19846,#19849,#884,.T.) ;
#24254=EDGE_CURVE('',#19849,#19850,#17281,.T.) ;
#24255=EDGE_CURVE('',#19850,#19848,#885,.T.) ;
#24256=EDGE_CURVE('',#19701,#19851,#3153,.T.) ;
#24257=EDGE_CURVE('',#19851,#19631,#886,.T.) ;
#24258=EDGE_CURVE('',#19851,#19852,#887,.T.) ;
#24259=EDGE_CURVE('',#19852,#19853,#17282,.T.) ;
#24260=EDGE_CURVE('',#19853,#19847,#888,.T.) ;
#24261=EDGE_CURVE('',#19700,#19698,#889,.T.) ;
#24262=EDGE_CURVE('',#19697,#19699,#890,.T.) ;
#24263=EDGE_CURVE('',#19699,#19854,#3154,.T.) ;
#24264=EDGE_CURVE('',#19854,#19627,#891,.T.) ;
#24265=EDGE_CURVE('',#19855,#19697,#3155,.T.) ;
#24266=EDGE_CURVE('',#19628,#19855,#892,.T.) ;
#24267=EDGE_CURVE('',#19854,#19856,#893,.T.) ;
#24268=EDGE_CURVE('',#19856,#19857,#17283,.T.) ;
#24269=EDGE_CURVE('',#19857,#19855,#894,.T.) ;
#24270=EDGE_CURVE('',#19852,#19853,#17284,.T.) ;
#24271=EDGE_CURVE('',#19844,#19845,#17285,.T.) ;
#24272=EDGE_CURVE('',#19836,#19837,#17286,.T.) ;
#24273=EDGE_CURVE('',#19828,#19829,#17287,.T.) ;
#24274=EDGE_CURVE('',#19820,#19821,#17288,.T.) ;
#24275=EDGE_CURVE('',#19812,#19813,#17289,.T.) ;
#24276=EDGE_CURVE('',#19804,#19805,#17290,.T.) ;
#24277=EDGE_CURVE('',#19796,#19797,#17291,.T.) ;
#24278=EDGE_CURVE('',#19788,#19789,#17292,.T.) ;
#24279=EDGE_CURVE('',#19781,#19782,#17293,.T.) ;
#24280=EDGE_CURVE('',#19785,#19786,#17294,.T.) ;
#24281=EDGE_CURVE('',#19793,#19794,#17295,.T.) ;
#24282=EDGE_CURVE('',#19801,#19802,#17296,.T.) ;
#24283=EDGE_CURVE('',#19809,#19810,#17297,.T.) ;
#24284=EDGE_CURVE('',#19817,#19818,#17298,.T.) ;
#24285=EDGE_CURVE('',#19825,#19826,#17299,.T.) ;
#24286=EDGE_CURVE('',#19833,#19834,#17300,.T.) ;
#24287=EDGE_CURVE('',#19841,#19842,#17301,.T.) ;
#24288=EDGE_CURVE('',#19849,#19850,#17302,.T.) ;
#24289=EDGE_CURVE('',#19856,#19857,#17303,.T.) ;
#24290=EDGE_CURVE('',#19731,#19858,#3156,.T.) ;
#24291=EDGE_CURVE('',#19858,#19858,#17304,.T.) ;
#24292=EDGE_CURVE('',#19696,#19859,#17305,.T.) ;
#24293=EDGE_CURVE('',#19859,#19860,#17306,.T.) ;
#24294=EDGE_CURVE('',#19860,#19695,#17307,.T.) ;
#24295=EDGE_CURVE('',#19861,#19861,#17308,.T.) ;
#24296=EDGE_CURVE('',#19862,#19859,#3157,.T.) ;
#24297=EDGE_CURVE('',#19863,#19862,#17309,.T.) ;
#24298=EDGE_CURVE('',#19864,#19863,#3158,.T.) ;
#24299=EDGE_CURVE('',#19865,#19864,#17310,.T.) ;
#24300=EDGE_CURVE('',#19866,#19865,#3159,.T.) ;
#24301=EDGE_CURVE('',#19867,#19866,#17311,.T.) ;
#24302=EDGE_CURVE('',#19868,#19867,#3160,.T.) ;
#24303=EDGE_CURVE('',#19869,#19868,#17312,.T.) ;
#24304=EDGE_CURVE('',#19870,#19869,#3161,.T.) ;
#24305=EDGE_CURVE('',#19871,#19870,#17313,.T.) ;
#24306=EDGE_CURVE('',#19872,#19871,#3162,.T.) ;
#24307=EDGE_CURVE('',#19873,#19872,#17314,.T.) ;
#24308=EDGE_CURVE('',#19874,#19873,#3163,.T.) ;
#24309=EDGE_CURVE('',#19875,#19874,#17315,.T.) ;
#24310=EDGE_CURVE('',#19876,#19875,#3164,.T.) ;
#24311=EDGE_CURVE('',#19877,#19876,#17316,.T.) ;
#24312=EDGE_CURVE('',#19878,#19877,#3165,.T.) ;
#24313=EDGE_CURVE('',#19879,#19878,#17317,.T.) ;
#24314=EDGE_CURVE('',#19880,#19879,#3166,.T.) ;
#24315=EDGE_CURVE('',#19881,#19880,#17318,.T.) ;
#24316=EDGE_CURVE('',#19882,#19881,#3167,.T.) ;
#24317=EDGE_CURVE('',#19883,#19882,#17319,.T.) ;
#24318=EDGE_CURVE('',#19860,#19883,#3168,.T.) ;
#24319=EDGE_CURVE('',#19696,#19884,#3169,.T.) ;
#24320=EDGE_CURVE('',#19884,#19862,#17320,.T.) ;
#24321=EDGE_CURVE('',#19884,#19682,#3170,.T.) ;
#24322=EDGE_CURVE('',#19690,#19879,#17321,.T.) ;
#24323=EDGE_CURVE('',#19878,#19689,#17322,.T.) ;
#24324=EDGE_CURVE('',#19691,#19880,#17323,.T.) ;
#24325=EDGE_CURVE('',#19885,#19867,#17324,.T.) ;
#24326=EDGE_CURVE('',#19866,#19886,#17325,.T.) ;
#24327=EDGE_CURVE('',#19886,#19885,#17326,.T.) ;
#24328=EDGE_CURVE('',#19673,#19885,#3171,.T.) ;
#24329=EDGE_CURVE('',#19886,#19671,#3172,.T.) ;
#24330=EDGE_CURVE('',#19885,#19887,#3173,.T.) ;
#24331=EDGE_CURVE('',#19887,#19868,#17327,.T.) ;
#24332=EDGE_CURVE('',#19887,#19674,#3174,.T.) ;
#24333=EDGE_CURVE('',#19685,#19873,#17328,.T.) ;
#24334=EDGE_CURVE('',#19872,#19888,#17329,.T.) ;
#24335=EDGE_CURVE('',#19888,#19685,#17330,.T.) ;
#24336=EDGE_CURVE('',#19888,#19661,#3175,.T.) ;
#24337=EDGE_CURVE('',#19684,#19874,#17331,.T.) ;
#24338=EDGE_CURVE('',#19858,#19861,#17332,.T.) ;
#24339=EDGE_CURVE('',#19881,#19692,#17333,.T.) ;
#24340=EDGE_CURVE('',#19693,#19882,#17334,.T.) ;
#24341=EDGE_CURVE('',#19883,#19694,#17335,.T.) ;
#24342=EDGE_CURVE('',#19877,#19688,#17336,.T.) ;
#24343=EDGE_CURVE('',#19687,#19876,#17337,.T.) ;
#24344=EDGE_CURVE('',#19875,#19686,#17338,.T.) ;
#24345=EDGE_CURVE('',#19889,#19884,#17339,.F.) ;
#24346=EDGE_CURVE('',#19863,#19889,#17340,.T.) ;
#24347=EDGE_CURVE('',#19675,#19889,#3176,.T.) ;
#24348=EDGE_CURVE('',#19890,#19864,#17341,.T.) ;
#24349=EDGE_CURVE('',#19891,#19890,#17342,.F.) ;
#24350=EDGE_CURVE('',#19865,#19891,#17343,.T.) ;
#24351=EDGE_CURVE('',#19889,#19890,#3177,.T.) ;
#24352=EDGE_CURVE('',#19668,#19891,#3178,.T.) ;
#24353=EDGE_CURVE('',#19890,#19677,#3179,.T.) ;
#24354=EDGE_CURVE('',#19892,#19870,#17344,.T.) ;
#24355=EDGE_CURVE('',#19893,#19892,#17345,.F.) ;
#24356=EDGE_CURVE('',#19871,#19893,#17346,.T.) ;
#24357=EDGE_CURVE('',#19891,#19886,#3180,.T.) ;
#24358=EDGE_CURVE('',#19894,#19887,#17347,.F.) ;
#24359=EDGE_CURVE('',#19869,#19894,#17348,.T.) ;
#24360=EDGE_CURVE('',#19665,#19894,#3181,.T.) ;
#24361=EDGE_CURVE('',#19894,#19892,#3182,.T.) ;
#24362=EDGE_CURVE('',#19658,#19893,#3183,.T.) ;
#24363=EDGE_CURVE('',#19892,#19667,#3184,.T.) ;
#24364=EDGE_CURVE('',#19893,#19888,#3185,.T.) ;
#30994=ORIENTED_EDGE('',*,*,#23775,.T.) ;
#30995=ORIENTED_EDGE('',*,*,#23776,.T.) ;
#30996=ORIENTED_EDGE('',*,*,#23777,.T.) ;
#30997=ORIENTED_EDGE('',*,*,#23776,.F.) ;
#30998=ORIENTED_EDGE('',*,*,#23777,.F.) ;
#30999=ORIENTED_EDGE('',*,*,#23778,.T.) ;
#31000=ORIENTED_EDGE('',*,*,#23779,.F.) ;
#31001=ORIENTED_EDGE('',*,*,#23780,.F.) ;
#31002=ORIENTED_EDGE('',*,*,#23781,.F.) ;
#31003=ORIENTED_EDGE('',*,*,#23782,.F.) ;
#31004=ORIENTED_EDGE('',*,*,#23783,.F.) ;
#31005=ORIENTED_EDGE('',*,*,#23784,.F.) ;
#31006=ORIENTED_EDGE('',*,*,#23785,.F.) ;
#31007=ORIENTED_EDGE('',*,*,#23786,.F.) ;
#31008=ORIENTED_EDGE('',*,*,#23787,.F.) ;
#31009=ORIENTED_EDGE('',*,*,#23788,.F.) ;
#31010=ORIENTED_EDGE('',*,*,#23789,.F.) ;
#31011=ORIENTED_EDGE('',*,*,#23790,.F.) ;
#31012=ORIENTED_EDGE('',*,*,#23791,.F.) ;
#31013=ORIENTED_EDGE('',*,*,#23792,.F.) ;
#31014=ORIENTED_EDGE('',*,*,#23793,.F.) ;
#31015=ORIENTED_EDGE('',*,*,#23794,.F.) ;
#31016=ORIENTED_EDGE('',*,*,#23795,.F.) ;
#31017=ORIENTED_EDGE('',*,*,#23796,.F.) ;
#31018=ORIENTED_EDGE('',*,*,#23797,.F.) ;
#31019=ORIENTED_EDGE('',*,*,#23798,.F.) ;
#31020=ORIENTED_EDGE('',*,*,#23799,.F.) ;
#31021=ORIENTED_EDGE('',*,*,#23800,.F.) ;
#31022=ORIENTED_EDGE('',*,*,#23801,.F.) ;
#31023=ORIENTED_EDGE('',*,*,#23802,.F.) ;
#31024=ORIENTED_EDGE('',*,*,#23803,.F.) ;
#31025=ORIENTED_EDGE('',*,*,#23804,.F.) ;
#31026=ORIENTED_EDGE('',*,*,#23805,.F.) ;
#31027=ORIENTED_EDGE('',*,*,#23806,.F.) ;
#31028=ORIENTED_EDGE('',*,*,#23807,.F.) ;
#31029=ORIENTED_EDGE('',*,*,#23808,.F.) ;
#31030=ORIENTED_EDGE('',*,*,#23809,.F.) ;
#31031=ORIENTED_EDGE('',*,*,#23810,.F.) ;
#31032=ORIENTED_EDGE('',*,*,#23811,.F.) ;
#31033=ORIENTED_EDGE('',*,*,#23812,.F.) ;
#31034=ORIENTED_EDGE('',*,*,#23813,.F.) ;
#31035=ORIENTED_EDGE('',*,*,#23814,.F.) ;
#31036=ORIENTED_EDGE('',*,*,#23815,.F.) ;
#31037=ORIENTED_EDGE('',*,*,#23816,.F.) ;
#31038=ORIENTED_EDGE('',*,*,#23817,.F.) ;
#31039=ORIENTED_EDGE('',*,*,#23818,.F.) ;
#31040=ORIENTED_EDGE('',*,*,#23819,.F.) ;
#31041=ORIENTED_EDGE('',*,*,#23820,.F.) ;
#31042=ORIENTED_EDGE('',*,*,#23821,.F.) ;
#31043=ORIENTED_EDGE('',*,*,#23822,.F.) ;
#31044=ORIENTED_EDGE('',*,*,#23823,.F.) ;
#31045=ORIENTED_EDGE('',*,*,#23824,.F.) ;
#31046=ORIENTED_EDGE('',*,*,#23825,.F.) ;
#31047=ORIENTED_EDGE('',*,*,#23826,.F.) ;
#31048=ORIENTED_EDGE('',*,*,#23827,.F.) ;
#31049=ORIENTED_EDGE('',*,*,#23828,.F.) ;
#31050=ORIENTED_EDGE('',*,*,#23829,.F.) ;
#31051=ORIENTED_EDGE('',*,*,#23830,.F.) ;
#31052=ORIENTED_EDGE('',*,*,#23831,.F.) ;
#31053=ORIENTED_EDGE('',*,*,#23832,.F.) ;
#31054=ORIENTED_EDGE('',*,*,#23833,.F.) ;
#31055=ORIENTED_EDGE('',*,*,#23834,.F.) ;
#31056=ORIENTED_EDGE('',*,*,#23835,.F.) ;
#31057=ORIENTED_EDGE('',*,*,#23836,.F.) ;
#31058=ORIENTED_EDGE('',*,*,#23837,.F.) ;
#31059=ORIENTED_EDGE('',*,*,#23838,.F.) ;
#31060=ORIENTED_EDGE('',*,*,#23839,.F.) ;
#31061=ORIENTED_EDGE('',*,*,#23840,.F.) ;
#31062=ORIENTED_EDGE('',*,*,#23841,.F.) ;
#31063=ORIENTED_EDGE('',*,*,#23842,.F.) ;
#31064=ORIENTED_EDGE('',*,*,#23843,.F.) ;
#31065=ORIENTED_EDGE('',*,*,#23844,.F.) ;
#31066=ORIENTED_EDGE('',*,*,#23845,.F.) ;
#31067=ORIENTED_EDGE('',*,*,#23846,.F.) ;
#31068=ORIENTED_EDGE('',*,*,#23847,.F.) ;
#31069=ORIENTED_EDGE('',*,*,#23848,.F.) ;
#31070=ORIENTED_EDGE('',*,*,#23849,.F.) ;
#31071=ORIENTED_EDGE('',*,*,#23850,.F.) ;
#31072=ORIENTED_EDGE('',*,*,#23851,.F.) ;
#31073=ORIENTED_EDGE('',*,*,#23852,.F.) ;
#31074=ORIENTED_EDGE('',*,*,#23853,.F.) ;
#31075=ORIENTED_EDGE('',*,*,#23854,.F.) ;
#31076=ORIENTED_EDGE('',*,*,#23855,.F.) ;
#31077=ORIENTED_EDGE('',*,*,#23856,.F.) ;
#31078=ORIENTED_EDGE('',*,*,#23857,.F.) ;
#31079=ORIENTED_EDGE('',*,*,#23858,.F.) ;
#31080=ORIENTED_EDGE('',*,*,#23859,.F.) ;
#31081=ORIENTED_EDGE('',*,*,#23778,.F.) ;
#31082=ORIENTED_EDGE('',*,*,#23775,.F.) ;
#31083=ORIENTED_EDGE('',*,*,#23860,.T.) ;
#31084=ORIENTED_EDGE('',*,*,#23861,.T.) ;
#31085=ORIENTED_EDGE('',*,*,#23862,.T.) ;
#31086=ORIENTED_EDGE('',*,*,#23863,.T.) ;
#31087=ORIENTED_EDGE('',*,*,#23864,.T.) ;
#31088=ORIENTED_EDGE('',*,*,#23865,.T.) ;
#31089=ORIENTED_EDGE('',*,*,#23866,.T.) ;
#31090=ORIENTED_EDGE('',*,*,#23867,.T.) ;
#31091=ORIENTED_EDGE('',*,*,#23868,.T.) ;
#31092=ORIENTED_EDGE('',*,*,#23869,.T.) ;
#31093=ORIENTED_EDGE('',*,*,#23866,.F.) ;
#31094=ORIENTED_EDGE('',*,*,#23870,.T.) ;
#31095=ORIENTED_EDGE('',*,*,#23871,.T.) ;
#31096=ORIENTED_EDGE('',*,*,#23872,.T.) ;
#31097=ORIENTED_EDGE('',*,*,#23868,.F.) ;
#31098=ORIENTED_EDGE('',*,*,#23873,.T.) ;
#31099=ORIENTED_EDGE('',*,*,#23874,.T.) ;
#31100=ORIENTED_EDGE('',*,*,#23875,.T.) ;
#31101=ORIENTED_EDGE('',*,*,#23876,.T.) ;
#31102=ORIENTED_EDGE('',*,*,#23877,.T.) ;
#31103=ORIENTED_EDGE('',*,*,#23878,.T.) ;
#31104=ORIENTED_EDGE('',*,*,#23879,.T.) ;
#31105=ORIENTED_EDGE('',*,*,#23880,.T.) ;
#31106=ORIENTED_EDGE('',*,*,#23881,.T.) ;
#31107=ORIENTED_EDGE('',*,*,#23882,.T.) ;
#31108=ORIENTED_EDGE('',*,*,#23883,.T.) ;
#31109=ORIENTED_EDGE('',*,*,#23880,.F.) ;
#31110=ORIENTED_EDGE('',*,*,#23884,.T.) ;
#31111=ORIENTED_EDGE('',*,*,#23885,.T.) ;
#31112=ORIENTED_EDGE('',*,*,#23886,.T.) ;
#31113=ORIENTED_EDGE('',*,*,#23882,.F.) ;
#31114=ORIENTED_EDGE('',*,*,#23887,.T.) ;
#31115=ORIENTED_EDGE('',*,*,#23888,.T.) ;
#31116=ORIENTED_EDGE('',*,*,#23889,.T.) ;
#31117=ORIENTED_EDGE('',*,*,#23890,.T.) ;
#31118=ORIENTED_EDGE('',*,*,#23891,.T.) ;
#31119=ORIENTED_EDGE('',*,*,#23892,.T.) ;
#31120=ORIENTED_EDGE('',*,*,#23893,.T.) ;
#31121=ORIENTED_EDGE('',*,*,#23894,.T.) ;
#31122=ORIENTED_EDGE('',*,*,#23895,.T.) ;
#31123=ORIENTED_EDGE('',*,*,#23896,.T.) ;
#31124=ORIENTED_EDGE('',*,*,#23897,.T.) ;
#31125=ORIENTED_EDGE('',*,*,#23894,.F.) ;
#31126=ORIENTED_EDGE('',*,*,#23898,.T.) ;
#31127=ORIENTED_EDGE('',*,*,#23899,.T.) ;
#31128=ORIENTED_EDGE('',*,*,#23900,.T.) ;
#31129=ORIENTED_EDGE('',*,*,#23896,.F.) ;
#31130=ORIENTED_EDGE('',*,*,#23901,.T.) ;
#31131=ORIENTED_EDGE('',*,*,#23902,.T.) ;
#31132=ORIENTED_EDGE('',*,*,#23903,.T.) ;
#31133=ORIENTED_EDGE('',*,*,#23904,.T.) ;
#31134=ORIENTED_EDGE('',*,*,#23905,.T.) ;
#31135=ORIENTED_EDGE('',*,*,#23906,.T.) ;
#31136=ORIENTED_EDGE('',*,*,#23907,.T.) ;
#31137=ORIENTED_EDGE('',*,*,#23908,.T.) ;
#31138=ORIENTED_EDGE('',*,*,#23909,.T.) ;
#31139=ORIENTED_EDGE('',*,*,#23910,.T.) ;
#31140=ORIENTED_EDGE('',*,*,#23911,.T.) ;
#31141=ORIENTED_EDGE('',*,*,#23908,.F.) ;
#31142=ORIENTED_EDGE('',*,*,#23912,.T.) ;
#31143=ORIENTED_EDGE('',*,*,#23913,.T.) ;
#31144=ORIENTED_EDGE('',*,*,#23914,.T.) ;
#31145=ORIENTED_EDGE('',*,*,#23906,.F.) ;
#31146=ORIENTED_EDGE('',*,*,#23915,.T.) ;
#31147=ORIENTED_EDGE('',*,*,#23910,.F.) ;
#31148=ORIENTED_EDGE('',*,*,#23902,.F.) ;
#31149=ORIENTED_EDGE('',*,*,#23916,.T.) ;
#31150=ORIENTED_EDGE('',*,*,#23904,.F.) ;
#31151=ORIENTED_EDGE('',*,*,#23892,.F.) ;
#31152=ORIENTED_EDGE('',*,*,#23917,.T.) ;
#31153=ORIENTED_EDGE('',*,*,#23899,.F.) ;
#31154=ORIENTED_EDGE('',*,*,#23888,.F.) ;
#31155=ORIENTED_EDGE('',*,*,#23918,.T.) ;
#31156=ORIENTED_EDGE('',*,*,#23890,.F.) ;
#31157=ORIENTED_EDGE('',*,*,#23878,.F.) ;
#31158=ORIENTED_EDGE('',*,*,#23919,.T.) ;
#31159=ORIENTED_EDGE('',*,*,#23885,.F.) ;
#31160=ORIENTED_EDGE('',*,*,#23874,.F.) ;
#31161=ORIENTED_EDGE('',*,*,#23920,.T.) ;
#31162=ORIENTED_EDGE('',*,*,#23876,.F.) ;
#31163=ORIENTED_EDGE('',*,*,#23864,.F.) ;
#31164=ORIENTED_EDGE('',*,*,#23921,.T.) ;
#31165=ORIENTED_EDGE('',*,*,#23871,.F.) ;
#31166=ORIENTED_EDGE('',*,*,#23860,.F.) ;
#31167=ORIENTED_EDGE('',*,*,#23922,.T.) ;
#31168=ORIENTED_EDGE('',*,*,#23862,.F.) ;
#31169=ORIENTED_EDGE('',*,*,#23913,.F.) ;
#31170=ORIENTED_EDGE('',*,*,#23923,.T.) ;
#31171=ORIENTED_EDGE('',*,*,#23886,.F.) ;
#31172=ORIENTED_EDGE('',*,*,#23924,.F.) ;
#31173=ORIENTED_EDGE('',*,*,#23925,.F.) ;
#31174=ORIENTED_EDGE('',*,*,#23926,.F.) ;
#31175=ORIENTED_EDGE('',*,*,#23920,.F.) ;
#31176=ORIENTED_EDGE('',*,*,#23927,.T.) ;
#31177=ORIENTED_EDGE('',*,*,#23928,.T.) ;
#31178=ORIENTED_EDGE('',*,*,#23924,.T.) ;
#31179=ORIENTED_EDGE('',*,*,#23877,.F.) ;
#31180=ORIENTED_EDGE('',*,*,#23929,.F.) ;
#31181=ORIENTED_EDGE('',*,*,#23930,.F.) ;
#31182=ORIENTED_EDGE('',*,*,#23927,.F.) ;
#31183=ORIENTED_EDGE('',*,*,#23921,.F.) ;
#31184=ORIENTED_EDGE('',*,*,#23931,.T.) ;
#31185=ORIENTED_EDGE('',*,*,#23932,.T.) ;
#31186=ORIENTED_EDGE('',*,*,#23929,.T.) ;
#31187=ORIENTED_EDGE('',*,*,#23867,.F.) ;
#31188=ORIENTED_EDGE('',*,*,#23933,.F.) ;
#31189=ORIENTED_EDGE('',*,*,#23934,.F.) ;
#31190=ORIENTED_EDGE('',*,*,#23931,.F.) ;
#31191=ORIENTED_EDGE('',*,*,#23869,.F.) ;
#31192=ORIENTED_EDGE('',*,*,#23935,.T.) ;
#31193=ORIENTED_EDGE('',*,*,#23936,.F.) ;
#31194=ORIENTED_EDGE('',*,*,#23933,.T.) ;
#31195=ORIENTED_EDGE('',*,*,#23872,.F.) ;
#31196=ORIENTED_EDGE('',*,*,#23937,.F.) ;
#31197=ORIENTED_EDGE('',*,*,#23938,.F.) ;
#31198=ORIENTED_EDGE('',*,*,#23935,.F.) ;
#31199=ORIENTED_EDGE('',*,*,#23922,.F.) ;
#31200=ORIENTED_EDGE('',*,*,#23939,.T.) ;
#31201=ORIENTED_EDGE('',*,*,#23940,.T.) ;
#31202=ORIENTED_EDGE('',*,*,#23937,.T.) ;
#31203=ORIENTED_EDGE('',*,*,#23863,.F.) ;
#31204=ORIENTED_EDGE('',*,*,#23941,.F.) ;
#31205=ORIENTED_EDGE('',*,*,#23942,.F.) ;
#31206=ORIENTED_EDGE('',*,*,#23939,.F.) ;
#31207=ORIENTED_EDGE('',*,*,#23923,.F.) ;
#31208=ORIENTED_EDGE('',*,*,#23943,.T.) ;
#31209=ORIENTED_EDGE('',*,*,#23944,.T.) ;
#31210=ORIENTED_EDGE('',*,*,#23941,.T.) ;
#31211=ORIENTED_EDGE('',*,*,#23915,.F.) ;
#31212=ORIENTED_EDGE('',*,*,#23945,.F.) ;
#31213=ORIENTED_EDGE('',*,*,#23946,.F.) ;
#31214=ORIENTED_EDGE('',*,*,#23943,.F.) ;
#31215=ORIENTED_EDGE('',*,*,#23909,.F.) ;
#31216=ORIENTED_EDGE('',*,*,#23947,.T.) ;
#31217=ORIENTED_EDGE('',*,*,#23948,.F.) ;
#31218=ORIENTED_EDGE('',*,*,#23945,.T.) ;
#31219=ORIENTED_EDGE('',*,*,#23907,.F.) ;
#31220=ORIENTED_EDGE('',*,*,#23914,.F.) ;
#31221=ORIENTED_EDGE('',*,*,#23861,.F.) ;
#31222=ORIENTED_EDGE('',*,*,#23873,.F.) ;
#31223=ORIENTED_EDGE('',*,*,#23870,.F.) ;
#31224=ORIENTED_EDGE('',*,*,#23865,.F.) ;
#31225=ORIENTED_EDGE('',*,*,#23875,.F.) ;
#31226=ORIENTED_EDGE('',*,*,#23887,.F.) ;
#31227=ORIENTED_EDGE('',*,*,#23884,.F.) ;
#31228=ORIENTED_EDGE('',*,*,#23879,.F.) ;
#31229=ORIENTED_EDGE('',*,*,#23889,.F.) ;
#31230=ORIENTED_EDGE('',*,*,#23901,.F.) ;
#31231=ORIENTED_EDGE('',*,*,#23898,.F.) ;
#31232=ORIENTED_EDGE('',*,*,#23893,.F.) ;
#31233=ORIENTED_EDGE('',*,*,#23903,.F.) ;
#31234=ORIENTED_EDGE('',*,*,#23912,.F.) ;
#31235=ORIENTED_EDGE('',*,*,#23949,.F.) ;
#31236=ORIENTED_EDGE('',*,*,#23950,.F.) ;
#31237=ORIENTED_EDGE('',*,*,#23951,.F.) ;
#31238=ORIENTED_EDGE('',*,*,#23952,.F.) ;
#31239=ORIENTED_EDGE('',*,*,#23953,.F.) ;
#31240=ORIENTED_EDGE('',*,*,#23954,.F.) ;
#31241=ORIENTED_EDGE('',*,*,#23955,.F.) ;
#31242=ORIENTED_EDGE('',*,*,#23956,.F.) ;
#31243=ORIENTED_EDGE('',*,*,#23957,.F.) ;
#31244=ORIENTED_EDGE('',*,*,#23951,.T.) ;
#31245=ORIENTED_EDGE('',*,*,#23958,.T.) ;
#31246=ORIENTED_EDGE('',*,*,#23956,.T.) ;
#31247=ORIENTED_EDGE('',*,*,#23845,.T.) ;
#31248=ORIENTED_EDGE('',*,*,#23959,.F.) ;
#31249=ORIENTED_EDGE('',*,*,#23960,.F.) ;
#31250=ORIENTED_EDGE('',*,*,#23961,.F.) ;
#31251=ORIENTED_EDGE('',*,*,#23962,.F.) ;
#31252=ORIENTED_EDGE('',*,*,#23963,.F.) ;
#31253=ORIENTED_EDGE('',*,*,#23964,.F.) ;
#31254=ORIENTED_EDGE('',*,*,#23957,.T.) ;
#31255=ORIENTED_EDGE('',*,*,#23965,.T.) ;
#31256=ORIENTED_EDGE('',*,*,#23963,.T.) ;
#31257=ORIENTED_EDGE('',*,*,#23966,.T.) ;
#31258=ORIENTED_EDGE('',*,*,#23967,.F.) ;
#31259=ORIENTED_EDGE('',*,*,#23968,.F.) ;
#31260=ORIENTED_EDGE('',*,*,#23969,.F.) ;
#31261=ORIENTED_EDGE('',*,*,#23970,.F.) ;
#31262=ORIENTED_EDGE('',*,*,#23971,.F.) ;
#31263=ORIENTED_EDGE('',*,*,#23972,.F.) ;
#31264=ORIENTED_EDGE('',*,*,#23964,.T.) ;
#31265=ORIENTED_EDGE('',*,*,#23973,.T.) ;
#31266=ORIENTED_EDGE('',*,*,#23971,.T.) ;
#31267=ORIENTED_EDGE('',*,*,#23849,.T.) ;
#31268=ORIENTED_EDGE('',*,*,#23974,.F.) ;
#31269=ORIENTED_EDGE('',*,*,#23975,.F.) ;
#31270=ORIENTED_EDGE('',*,*,#23976,.F.) ;
#31271=ORIENTED_EDGE('',*,*,#23977,.F.) ;
#31272=ORIENTED_EDGE('',*,*,#23978,.F.) ;
#31273=ORIENTED_EDGE('',*,*,#23979,.F.) ;
#31274=ORIENTED_EDGE('',*,*,#23972,.T.) ;
#31275=ORIENTED_EDGE('',*,*,#23980,.T.) ;
#31276=ORIENTED_EDGE('',*,*,#23978,.T.) ;
#31277=ORIENTED_EDGE('',*,*,#23981,.T.) ;
#31278=ORIENTED_EDGE('',*,*,#23982,.F.) ;
#31279=ORIENTED_EDGE('',*,*,#23983,.F.) ;
#31280=ORIENTED_EDGE('',*,*,#23984,.F.) ;
#31281=ORIENTED_EDGE('',*,*,#23985,.F.) ;
#31282=ORIENTED_EDGE('',*,*,#23986,.F.) ;
#31283=ORIENTED_EDGE('',*,*,#23987,.F.) ;
#31284=ORIENTED_EDGE('',*,*,#23979,.T.) ;
#31285=ORIENTED_EDGE('',*,*,#23988,.T.) ;
#31286=ORIENTED_EDGE('',*,*,#23986,.T.) ;
#31287=ORIENTED_EDGE('',*,*,#23853,.T.) ;
#31288=ORIENTED_EDGE('',*,*,#23989,.F.) ;
#31289=ORIENTED_EDGE('',*,*,#23990,.F.) ;
#31290=ORIENTED_EDGE('',*,*,#23991,.F.) ;
#31291=ORIENTED_EDGE('',*,*,#23992,.F.) ;
#31292=ORIENTED_EDGE('',*,*,#23993,.F.) ;
#31293=ORIENTED_EDGE('',*,*,#23994,.F.) ;
#31294=ORIENTED_EDGE('',*,*,#23987,.T.) ;
#31295=ORIENTED_EDGE('',*,*,#23995,.T.) ;
#31296=ORIENTED_EDGE('',*,*,#23993,.T.) ;
#31297=ORIENTED_EDGE('',*,*,#23996,.T.) ;
#31298=ORIENTED_EDGE('',*,*,#23997,.F.) ;
#31299=ORIENTED_EDGE('',*,*,#23998,.F.) ;
#31300=ORIENTED_EDGE('',*,*,#23999,.F.) ;
#31301=ORIENTED_EDGE('',*,*,#24000,.F.) ;
#31302=ORIENTED_EDGE('',*,*,#24001,.F.) ;
#31303=ORIENTED_EDGE('',*,*,#24002,.F.) ;
#31304=ORIENTED_EDGE('',*,*,#23994,.T.) ;
#31305=ORIENTED_EDGE('',*,*,#24003,.T.) ;
#31306=ORIENTED_EDGE('',*,*,#24001,.T.) ;
#31307=ORIENTED_EDGE('',*,*,#23857,.T.) ;
#31308=ORIENTED_EDGE('',*,*,#24004,.F.) ;
#31309=ORIENTED_EDGE('',*,*,#24005,.F.) ;
#31310=ORIENTED_EDGE('',*,*,#24006,.F.) ;
#31311=ORIENTED_EDGE('',*,*,#24007,.F.) ;
#31312=ORIENTED_EDGE('',*,*,#24008,.F.) ;
#31313=ORIENTED_EDGE('',*,*,#24009,.F.) ;
#31314=ORIENTED_EDGE('',*,*,#24002,.T.) ;
#31315=ORIENTED_EDGE('',*,*,#24010,.T.) ;
#31316=ORIENTED_EDGE('',*,*,#24011,.T.) ;
#31317=ORIENTED_EDGE('',*,*,#24008,.T.) ;
#31318=ORIENTED_EDGE('',*,*,#24012,.T.) ;
#31319=ORIENTED_EDGE('',*,*,#24013,.F.) ;
#31320=ORIENTED_EDGE('',*,*,#24014,.F.) ;
#31321=ORIENTED_EDGE('',*,*,#24015,.F.) ;
#31322=ORIENTED_EDGE('',*,*,#24016,.F.) ;
#31323=ORIENTED_EDGE('',*,*,#24017,.F.) ;
#31324=ORIENTED_EDGE('',*,*,#24018,.F.) ;
#31325=ORIENTED_EDGE('',*,*,#24009,.T.) ;
#31326=ORIENTED_EDGE('',*,*,#24019,.T.) ;
#31327=ORIENTED_EDGE('',*,*,#24017,.T.) ;
#31328=ORIENTED_EDGE('',*,*,#23781,.T.) ;
#31329=ORIENTED_EDGE('',*,*,#24020,.F.) ;
#31330=ORIENTED_EDGE('',*,*,#24021,.F.) ;
#31331=ORIENTED_EDGE('',*,*,#24022,.F.) ;
#31332=ORIENTED_EDGE('',*,*,#24023,.F.) ;
#31333=ORIENTED_EDGE('',*,*,#24024,.F.) ;
#31334=ORIENTED_EDGE('',*,*,#24025,.F.) ;
#31335=ORIENTED_EDGE('',*,*,#24018,.T.) ;
#31336=ORIENTED_EDGE('',*,*,#24026,.T.) ;
#31337=ORIENTED_EDGE('',*,*,#24024,.T.) ;
#31338=ORIENTED_EDGE('',*,*,#24027,.T.) ;
#31339=ORIENTED_EDGE('',*,*,#24028,.F.) ;
#31340=ORIENTED_EDGE('',*,*,#24029,.F.) ;
#31341=ORIENTED_EDGE('',*,*,#24030,.F.) ;
#31342=ORIENTED_EDGE('',*,*,#24031,.F.) ;
#31343=ORIENTED_EDGE('',*,*,#24032,.F.) ;
#31344=ORIENTED_EDGE('',*,*,#24033,.F.) ;
#31345=ORIENTED_EDGE('',*,*,#24025,.T.) ;
#31346=ORIENTED_EDGE('',*,*,#24034,.T.) ;
#31347=ORIENTED_EDGE('',*,*,#24032,.T.) ;
#31348=ORIENTED_EDGE('',*,*,#23785,.T.) ;
#31349=ORIENTED_EDGE('',*,*,#24035,.F.) ;
#31350=ORIENTED_EDGE('',*,*,#24036,.F.) ;
#31351=ORIENTED_EDGE('',*,*,#24037,.F.) ;
#31352=ORIENTED_EDGE('',*,*,#24038,.F.) ;
#31353=ORIENTED_EDGE('',*,*,#24039,.F.) ;
#31354=ORIENTED_EDGE('',*,*,#24040,.F.) ;
#31355=ORIENTED_EDGE('',*,*,#24033,.T.) ;
#31356=ORIENTED_EDGE('',*,*,#24041,.T.) ;
#31357=ORIENTED_EDGE('',*,*,#24039,.T.) ;
#31358=ORIENTED_EDGE('',*,*,#24042,.T.) ;
#31359=ORIENTED_EDGE('',*,*,#24043,.F.) ;
#31360=ORIENTED_EDGE('',*,*,#24044,.F.) ;
#31361=ORIENTED_EDGE('',*,*,#24045,.F.) ;
#31362=ORIENTED_EDGE('',*,*,#24046,.F.) ;
#31363=ORIENTED_EDGE('',*,*,#24047,.F.) ;
#31364=ORIENTED_EDGE('',*,*,#24048,.F.) ;
#31365=ORIENTED_EDGE('',*,*,#24040,.T.) ;
#31366=ORIENTED_EDGE('',*,*,#24049,.T.) ;
#31367=ORIENTED_EDGE('',*,*,#24047,.T.) ;
#31368=ORIENTED_EDGE('',*,*,#23789,.T.) ;
#31369=ORIENTED_EDGE('',*,*,#24050,.F.) ;
#31370=ORIENTED_EDGE('',*,*,#24051,.F.) ;
#31371=ORIENTED_EDGE('',*,*,#24052,.F.) ;
#31372=ORIENTED_EDGE('',*,*,#24053,.F.) ;
#31373=ORIENTED_EDGE('',*,*,#24054,.F.) ;
#31374=ORIENTED_EDGE('',*,*,#24055,.F.) ;
#31375=ORIENTED_EDGE('',*,*,#24048,.T.) ;
#31376=ORIENTED_EDGE('',*,*,#24056,.T.) ;
#31377=ORIENTED_EDGE('',*,*,#24054,.T.) ;
#31378=ORIENTED_EDGE('',*,*,#24057,.T.) ;
#31379=ORIENTED_EDGE('',*,*,#24058,.F.) ;
#31380=ORIENTED_EDGE('',*,*,#24059,.F.) ;
#31381=ORIENTED_EDGE('',*,*,#24060,.F.) ;
#31382=ORIENTED_EDGE('',*,*,#24061,.F.) ;
#31383=ORIENTED_EDGE('',*,*,#24062,.F.) ;
#31384=ORIENTED_EDGE('',*,*,#24063,.F.) ;
#31385=ORIENTED_EDGE('',*,*,#24055,.T.) ;
#31386=ORIENTED_EDGE('',*,*,#24064,.T.) ;
#31387=ORIENTED_EDGE('',*,*,#24062,.T.) ;
#31388=ORIENTED_EDGE('',*,*,#23793,.T.) ;
#31389=ORIENTED_EDGE('',*,*,#24065,.F.) ;
#31390=ORIENTED_EDGE('',*,*,#24066,.F.) ;
#31391=ORIENTED_EDGE('',*,*,#24067,.F.) ;
#31392=ORIENTED_EDGE('',*,*,#24068,.F.) ;
#31393=ORIENTED_EDGE('',*,*,#24069,.F.) ;
#31394=ORIENTED_EDGE('',*,*,#24070,.F.) ;
#31395=ORIENTED_EDGE('',*,*,#24063,.T.) ;
#31396=ORIENTED_EDGE('',*,*,#24071,.T.) ;
#31397=ORIENTED_EDGE('',*,*,#24069,.T.) ;
#31398=ORIENTED_EDGE('',*,*,#24072,.T.) ;
#31399=ORIENTED_EDGE('',*,*,#24073,.F.) ;
#31400=ORIENTED_EDGE('',*,*,#24074,.F.) ;
#31401=ORIENTED_EDGE('',*,*,#24075,.F.) ;
#31402=ORIENTED_EDGE('',*,*,#24076,.F.) ;
#31403=ORIENTED_EDGE('',*,*,#24077,.F.) ;
#31404=ORIENTED_EDGE('',*,*,#24078,.F.) ;
#31405=ORIENTED_EDGE('',*,*,#24070,.T.) ;
#31406=ORIENTED_EDGE('',*,*,#24079,.T.) ;
#31407=ORIENTED_EDGE('',*,*,#24077,.T.) ;
#31408=ORIENTED_EDGE('',*,*,#23797,.T.) ;
#31409=ORIENTED_EDGE('',*,*,#24080,.F.) ;
#31410=ORIENTED_EDGE('',*,*,#24081,.F.) ;
#31411=ORIENTED_EDGE('',*,*,#24082,.F.) ;
#31412=ORIENTED_EDGE('',*,*,#24083,.F.) ;
#31413=ORIENTED_EDGE('',*,*,#24084,.F.) ;
#31414=ORIENTED_EDGE('',*,*,#24085,.F.) ;
#31415=ORIENTED_EDGE('',*,*,#24078,.T.) ;
#31416=ORIENTED_EDGE('',*,*,#24086,.T.) ;
#31417=ORIENTED_EDGE('',*,*,#24084,.T.) ;
#31418=ORIENTED_EDGE('',*,*,#24087,.T.) ;
#31419=ORIENTED_EDGE('',*,*,#24088,.F.) ;
#31420=ORIENTED_EDGE('',*,*,#24089,.F.) ;
#31421=ORIENTED_EDGE('',*,*,#24090,.F.) ;
#31422=ORIENTED_EDGE('',*,*,#24091,.F.) ;
#31423=ORIENTED_EDGE('',*,*,#24092,.F.) ;
#31424=ORIENTED_EDGE('',*,*,#24093,.F.) ;
#31425=ORIENTED_EDGE('',*,*,#24085,.T.) ;
#31426=ORIENTED_EDGE('',*,*,#24094,.T.) ;
#31427=ORIENTED_EDGE('',*,*,#24092,.T.) ;
#31428=ORIENTED_EDGE('',*,*,#23801,.T.) ;
#31429=ORIENTED_EDGE('',*,*,#24095,.F.) ;
#31430=ORIENTED_EDGE('',*,*,#24096,.F.) ;
#31431=ORIENTED_EDGE('',*,*,#24097,.F.) ;
#31432=ORIENTED_EDGE('',*,*,#24093,.T.) ;
#31433=ORIENTED_EDGE('',*,*,#24098,.T.) ;
#31434=ORIENTED_EDGE('',*,*,#24096,.T.) ;
#31435=ORIENTED_EDGE('',*,*,#24099,.T.) ;
#31436=ORIENTED_EDGE('',*,*,#24097,.T.) ;
#31437=ORIENTED_EDGE('',*,*,#24100,.T.) ;
#31438=ORIENTED_EDGE('',*,*,#24089,.T.) ;
#31439=ORIENTED_EDGE('',*,*,#23805,.T.) ;
#31440=ORIENTED_EDGE('',*,*,#24101,.T.) ;
#31441=ORIENTED_EDGE('',*,*,#24095,.T.) ;
#31442=ORIENTED_EDGE('',*,*,#23804,.T.) ;
#31443=ORIENTED_EDGE('',*,*,#24102,.T.) ;
#31444=ORIENTED_EDGE('',*,*,#23802,.T.) ;
#31445=ORIENTED_EDGE('',*,*,#24091,.T.) ;
#31446=ORIENTED_EDGE('',*,*,#24103,.T.) ;
#31447=ORIENTED_EDGE('',*,*,#24104,.T.) ;
#31448=ORIENTED_EDGE('',*,*,#24090,.T.) ;
#31449=ORIENTED_EDGE('',*,*,#24105,.T.) ;
#31450=ORIENTED_EDGE('',*,*,#24081,.T.) ;
#31451=ORIENTED_EDGE('',*,*,#24106,.T.) ;
#31452=ORIENTED_EDGE('',*,*,#23806,.T.) ;
#31453=ORIENTED_EDGE('',*,*,#24088,.T.) ;
#31454=ORIENTED_EDGE('',*,*,#24107,.T.) ;
#31455=ORIENTED_EDGE('',*,*,#24108,.T.) ;
#31456=ORIENTED_EDGE('',*,*,#23803,.T.) ;
#31457=ORIENTED_EDGE('',*,*,#24104,.F.) ;
#31458=ORIENTED_EDGE('',*,*,#24109,.T.) ;
#31459=ORIENTED_EDGE('',*,*,#24110,.T.) ;
#31460=ORIENTED_EDGE('',*,*,#24111,.T.) ;
#31461=ORIENTED_EDGE('',*,*,#24102,.F.) ;
#31462=ORIENTED_EDGE('',*,*,#24112,.T.) ;
#31463=ORIENTED_EDGE('',*,*,#24083,.T.) ;
#31464=ORIENTED_EDGE('',*,*,#23800,.T.) ;
#31465=ORIENTED_EDGE('',*,*,#24113,.T.) ;
#31466=ORIENTED_EDGE('',*,*,#24082,.T.) ;
#31467=ORIENTED_EDGE('',*,*,#24114,.T.) ;
#31468=ORIENTED_EDGE('',*,*,#24074,.T.) ;
#31469=ORIENTED_EDGE('',*,*,#23809,.T.) ;
#31470=ORIENTED_EDGE('',*,*,#24115,.T.) ;
#31471=ORIENTED_EDGE('',*,*,#24080,.T.) ;
#31472=ORIENTED_EDGE('',*,*,#23808,.T.) ;
#31473=ORIENTED_EDGE('',*,*,#24116,.T.) ;
#31474=ORIENTED_EDGE('',*,*,#23807,.T.) ;
#31475=ORIENTED_EDGE('',*,*,#24108,.F.) ;
#31476=ORIENTED_EDGE('',*,*,#24117,.T.) ;
#31477=ORIENTED_EDGE('',*,*,#24118,.T.) ;
#31478=ORIENTED_EDGE('',*,*,#24119,.T.) ;
#31479=ORIENTED_EDGE('',*,*,#24116,.F.) ;
#31480=ORIENTED_EDGE('',*,*,#23798,.T.) ;
#31481=ORIENTED_EDGE('',*,*,#24076,.T.) ;
#31482=ORIENTED_EDGE('',*,*,#24120,.T.) ;
#31483=ORIENTED_EDGE('',*,*,#24121,.T.) ;
#31484=ORIENTED_EDGE('',*,*,#23799,.T.) ;
#31485=ORIENTED_EDGE('',*,*,#24121,.F.) ;
#31486=ORIENTED_EDGE('',*,*,#24122,.T.) ;
#31487=ORIENTED_EDGE('',*,*,#24123,.T.) ;
#31488=ORIENTED_EDGE('',*,*,#24124,.T.) ;
#31489=ORIENTED_EDGE('',*,*,#24113,.F.) ;
#31490=ORIENTED_EDGE('',*,*,#24075,.T.) ;
#31491=ORIENTED_EDGE('',*,*,#24125,.T.) ;
#31492=ORIENTED_EDGE('',*,*,#24066,.T.) ;
#31493=ORIENTED_EDGE('',*,*,#24126,.T.) ;
#31494=ORIENTED_EDGE('',*,*,#23810,.T.) ;
#31495=ORIENTED_EDGE('',*,*,#24073,.T.) ;
#31496=ORIENTED_EDGE('',*,*,#24127,.T.) ;
#31497=ORIENTED_EDGE('',*,*,#24128,.T.) ;
#31498=ORIENTED_EDGE('',*,*,#24129,.T.) ;
#31499=ORIENTED_EDGE('',*,*,#24068,.T.) ;
#31500=ORIENTED_EDGE('',*,*,#23796,.T.) ;
#31501=ORIENTED_EDGE('',*,*,#24130,.T.) ;
#31502=ORIENTED_EDGE('',*,*,#24067,.T.) ;
#31503=ORIENTED_EDGE('',*,*,#24131,.T.) ;
#31504=ORIENTED_EDGE('',*,*,#24059,.T.) ;
#31505=ORIENTED_EDGE('',*,*,#23813,.T.) ;
#31506=ORIENTED_EDGE('',*,*,#24132,.T.) ;
#31507=ORIENTED_EDGE('',*,*,#24065,.T.) ;
#31508=ORIENTED_EDGE('',*,*,#23812,.T.) ;
#31509=ORIENTED_EDGE('',*,*,#24133,.T.) ;
#31510=ORIENTED_EDGE('',*,*,#23811,.T.) ;
#31511=ORIENTED_EDGE('',*,*,#24128,.F.) ;
#31512=ORIENTED_EDGE('',*,*,#24134,.T.) ;
#31513=ORIENTED_EDGE('',*,*,#24135,.T.) ;
#31514=ORIENTED_EDGE('',*,*,#24136,.T.) ;
#31515=ORIENTED_EDGE('',*,*,#24133,.F.) ;
#31516=ORIENTED_EDGE('',*,*,#23794,.T.) ;
#31517=ORIENTED_EDGE('',*,*,#24061,.T.) ;
#31518=ORIENTED_EDGE('',*,*,#24137,.T.) ;
#31519=ORIENTED_EDGE('',*,*,#24138,.T.) ;
#31520=ORIENTED_EDGE('',*,*,#23795,.T.) ;
#31521=ORIENTED_EDGE('',*,*,#24138,.F.) ;
#31522=ORIENTED_EDGE('',*,*,#24139,.T.) ;
#31523=ORIENTED_EDGE('',*,*,#24140,.T.) ;
#31524=ORIENTED_EDGE('',*,*,#24141,.T.) ;
#31525=ORIENTED_EDGE('',*,*,#24130,.F.) ;
#31526=ORIENTED_EDGE('',*,*,#24060,.T.) ;
#31527=ORIENTED_EDGE('',*,*,#24142,.T.) ;
#31528=ORIENTED_EDGE('',*,*,#24051,.T.) ;
#31529=ORIENTED_EDGE('',*,*,#24143,.T.) ;
#31530=ORIENTED_EDGE('',*,*,#23814,.T.) ;
#31531=ORIENTED_EDGE('',*,*,#24058,.T.) ;
#31532=ORIENTED_EDGE('',*,*,#24144,.T.) ;
#31533=ORIENTED_EDGE('',*,*,#24145,.T.) ;
#31534=ORIENTED_EDGE('',*,*,#24146,.T.) ;
#31535=ORIENTED_EDGE('',*,*,#24053,.T.) ;
#31536=ORIENTED_EDGE('',*,*,#23792,.T.) ;
#31537=ORIENTED_EDGE('',*,*,#24147,.T.) ;
#31538=ORIENTED_EDGE('',*,*,#24052,.T.) ;
#31539=ORIENTED_EDGE('',*,*,#24148,.T.) ;
#31540=ORIENTED_EDGE('',*,*,#24044,.T.) ;
#31541=ORIENTED_EDGE('',*,*,#23817,.T.) ;
#31542=ORIENTED_EDGE('',*,*,#24149,.T.) ;
#31543=ORIENTED_EDGE('',*,*,#24050,.T.) ;
#31544=ORIENTED_EDGE('',*,*,#23816,.T.) ;
#31545=ORIENTED_EDGE('',*,*,#24150,.T.) ;
#31546=ORIENTED_EDGE('',*,*,#23815,.T.) ;
#31547=ORIENTED_EDGE('',*,*,#24145,.F.) ;
#31548=ORIENTED_EDGE('',*,*,#24151,.T.) ;
#31549=ORIENTED_EDGE('',*,*,#24152,.T.) ;
#31550=ORIENTED_EDGE('',*,*,#24153,.T.) ;
#31551=ORIENTED_EDGE('',*,*,#24150,.F.) ;
#31552=ORIENTED_EDGE('',*,*,#23790,.T.) ;
#31553=ORIENTED_EDGE('',*,*,#24046,.T.) ;
#31554=ORIENTED_EDGE('',*,*,#24154,.T.) ;
#31555=ORIENTED_EDGE('',*,*,#24155,.T.) ;
#31556=ORIENTED_EDGE('',*,*,#23791,.T.) ;
#31557=ORIENTED_EDGE('',*,*,#24155,.F.) ;
#31558=ORIENTED_EDGE('',*,*,#24156,.T.) ;
#31559=ORIENTED_EDGE('',*,*,#24157,.T.) ;
#31560=ORIENTED_EDGE('',*,*,#24158,.T.) ;
#31561=ORIENTED_EDGE('',*,*,#24147,.F.) ;
#31562=ORIENTED_EDGE('',*,*,#24045,.T.) ;
#31563=ORIENTED_EDGE('',*,*,#24159,.T.) ;
#31564=ORIENTED_EDGE('',*,*,#24036,.T.) ;
#31565=ORIENTED_EDGE('',*,*,#24160,.T.) ;
#31566=ORIENTED_EDGE('',*,*,#23818,.T.) ;
#31567=ORIENTED_EDGE('',*,*,#24043,.T.) ;
#31568=ORIENTED_EDGE('',*,*,#24161,.T.) ;
#31569=ORIENTED_EDGE('',*,*,#24162,.T.) ;
#31570=ORIENTED_EDGE('',*,*,#24163,.T.) ;
#31571=ORIENTED_EDGE('',*,*,#24038,.T.) ;
#31572=ORIENTED_EDGE('',*,*,#23788,.T.) ;
#31573=ORIENTED_EDGE('',*,*,#24164,.T.) ;
#31574=ORIENTED_EDGE('',*,*,#24037,.T.) ;
#31575=ORIENTED_EDGE('',*,*,#24165,.T.) ;
#31576=ORIENTED_EDGE('',*,*,#24029,.T.) ;
#31577=ORIENTED_EDGE('',*,*,#23821,.T.) ;
#31578=ORIENTED_EDGE('',*,*,#24166,.T.) ;
#31579=ORIENTED_EDGE('',*,*,#24035,.T.) ;
#31580=ORIENTED_EDGE('',*,*,#23820,.T.) ;
#31581=ORIENTED_EDGE('',*,*,#24167,.T.) ;
#31582=ORIENTED_EDGE('',*,*,#23819,.T.) ;
#31583=ORIENTED_EDGE('',*,*,#24162,.F.) ;
#31584=ORIENTED_EDGE('',*,*,#24168,.T.) ;
#31585=ORIENTED_EDGE('',*,*,#24169,.T.) ;
#31586=ORIENTED_EDGE('',*,*,#24170,.T.) ;
#31587=ORIENTED_EDGE('',*,*,#24167,.F.) ;
#31588=ORIENTED_EDGE('',*,*,#23786,.T.) ;
#31589=ORIENTED_EDGE('',*,*,#24031,.T.) ;
#31590=ORIENTED_EDGE('',*,*,#24171,.T.) ;
#31591=ORIENTED_EDGE('',*,*,#24172,.T.) ;
#31592=ORIENTED_EDGE('',*,*,#23787,.T.) ;
#31593=ORIENTED_EDGE('',*,*,#24172,.F.) ;
#31594=ORIENTED_EDGE('',*,*,#24173,.T.) ;
#31595=ORIENTED_EDGE('',*,*,#24174,.T.) ;
#31596=ORIENTED_EDGE('',*,*,#24175,.T.) ;
#31597=ORIENTED_EDGE('',*,*,#24164,.F.) ;
#31598=ORIENTED_EDGE('',*,*,#24030,.T.) ;
#31599=ORIENTED_EDGE('',*,*,#24176,.T.) ;
#31600=ORIENTED_EDGE('',*,*,#24021,.T.) ;
#31601=ORIENTED_EDGE('',*,*,#24177,.T.) ;
#31602=ORIENTED_EDGE('',*,*,#23822,.T.) ;
#31603=ORIENTED_EDGE('',*,*,#24028,.T.) ;
#31604=ORIENTED_EDGE('',*,*,#24178,.T.) ;
#31605=ORIENTED_EDGE('',*,*,#24179,.T.) ;
#31606=ORIENTED_EDGE('',*,*,#24180,.T.) ;
#31607=ORIENTED_EDGE('',*,*,#24023,.T.) ;
#31608=ORIENTED_EDGE('',*,*,#23784,.T.) ;
#31609=ORIENTED_EDGE('',*,*,#24181,.T.) ;
#31610=ORIENTED_EDGE('',*,*,#24022,.T.) ;
#31611=ORIENTED_EDGE('',*,*,#24182,.T.) ;
#31612=ORIENTED_EDGE('',*,*,#24014,.T.) ;
#31613=ORIENTED_EDGE('',*,*,#23825,.T.) ;
#31614=ORIENTED_EDGE('',*,*,#24183,.T.) ;
#31615=ORIENTED_EDGE('',*,*,#24020,.T.) ;
#31616=ORIENTED_EDGE('',*,*,#23824,.T.) ;
#31617=ORIENTED_EDGE('',*,*,#24184,.T.) ;
#31618=ORIENTED_EDGE('',*,*,#23823,.T.) ;
#31619=ORIENTED_EDGE('',*,*,#24179,.F.) ;
#31620=ORIENTED_EDGE('',*,*,#24185,.T.) ;
#31621=ORIENTED_EDGE('',*,*,#24186,.T.) ;
#31622=ORIENTED_EDGE('',*,*,#24187,.T.) ;
#31623=ORIENTED_EDGE('',*,*,#24184,.F.) ;
#31624=ORIENTED_EDGE('',*,*,#23782,.T.) ;
#31625=ORIENTED_EDGE('',*,*,#24016,.T.) ;
#31626=ORIENTED_EDGE('',*,*,#24188,.T.) ;
#31627=ORIENTED_EDGE('',*,*,#24189,.T.) ;
#31628=ORIENTED_EDGE('',*,*,#23783,.T.) ;
#31629=ORIENTED_EDGE('',*,*,#24189,.F.) ;
#31630=ORIENTED_EDGE('',*,*,#24190,.T.) ;
#31631=ORIENTED_EDGE('',*,*,#24191,.T.) ;
#31632=ORIENTED_EDGE('',*,*,#24192,.T.) ;
#31633=ORIENTED_EDGE('',*,*,#24181,.F.) ;
#31634=ORIENTED_EDGE('',*,*,#24015,.T.) ;
#31635=ORIENTED_EDGE('',*,*,#24193,.T.) ;
#31636=ORIENTED_EDGE('',*,*,#24005,.T.) ;
#31637=ORIENTED_EDGE('',*,*,#24194,.T.) ;
#31638=ORIENTED_EDGE('',*,*,#23826,.T.) ;
#31639=ORIENTED_EDGE('',*,*,#24013,.T.) ;
#31640=ORIENTED_EDGE('',*,*,#24195,.T.) ;
#31641=ORIENTED_EDGE('',*,*,#24196,.T.) ;
#31642=ORIENTED_EDGE('',*,*,#24197,.T.) ;
#31643=ORIENTED_EDGE('',*,*,#24007,.T.) ;
#31644=ORIENTED_EDGE('',*,*,#23780,.T.) ;
#31645=ORIENTED_EDGE('',*,*,#24198,.T.) ;
#31646=ORIENTED_EDGE('',*,*,#24006,.T.) ;
#31647=ORIENTED_EDGE('',*,*,#24199,.T.) ;
#31648=ORIENTED_EDGE('',*,*,#23998,.T.) ;
#31649=ORIENTED_EDGE('',*,*,#23829,.T.) ;
#31650=ORIENTED_EDGE('',*,*,#24200,.T.) ;
#31651=ORIENTED_EDGE('',*,*,#24004,.T.) ;
#31652=ORIENTED_EDGE('',*,*,#23828,.T.) ;
#31653=ORIENTED_EDGE('',*,*,#24201,.T.) ;
#31654=ORIENTED_EDGE('',*,*,#23827,.T.) ;
#31655=ORIENTED_EDGE('',*,*,#24196,.F.) ;
#31656=ORIENTED_EDGE('',*,*,#24202,.T.) ;
#31657=ORIENTED_EDGE('',*,*,#24203,.T.) ;
#31658=ORIENTED_EDGE('',*,*,#24204,.T.) ;
#31659=ORIENTED_EDGE('',*,*,#24201,.F.) ;
#31660=ORIENTED_EDGE('',*,*,#23858,.T.) ;
#31661=ORIENTED_EDGE('',*,*,#24000,.T.) ;
#31662=ORIENTED_EDGE('',*,*,#24205,.T.) ;
#31663=ORIENTED_EDGE('',*,*,#24206,.T.) ;
#31664=ORIENTED_EDGE('',*,*,#23779,.T.) ;
#31665=ORIENTED_EDGE('',*,*,#23859,.T.) ;
#31666=ORIENTED_EDGE('',*,*,#24206,.F.) ;
#31667=ORIENTED_EDGE('',*,*,#24207,.T.) ;
#31668=ORIENTED_EDGE('',*,*,#24208,.T.) ;
#31669=ORIENTED_EDGE('',*,*,#24209,.T.) ;
#31670=ORIENTED_EDGE('',*,*,#24198,.F.) ;
#31671=ORIENTED_EDGE('',*,*,#23999,.T.) ;
#31672=ORIENTED_EDGE('',*,*,#24210,.T.) ;
#31673=ORIENTED_EDGE('',*,*,#23990,.T.) ;
#31674=ORIENTED_EDGE('',*,*,#24211,.T.) ;
#31675=ORIENTED_EDGE('',*,*,#23830,.T.) ;
#31676=ORIENTED_EDGE('',*,*,#23997,.T.) ;
#31677=ORIENTED_EDGE('',*,*,#24212,.T.) ;
#31678=ORIENTED_EDGE('',*,*,#24213,.T.) ;
#31679=ORIENTED_EDGE('',*,*,#24214,.T.) ;
#31680=ORIENTED_EDGE('',*,*,#23992,.T.) ;
#31681=ORIENTED_EDGE('',*,*,#23856,.T.) ;
#31682=ORIENTED_EDGE('',*,*,#24215,.T.) ;
#31683=ORIENTED_EDGE('',*,*,#23991,.T.) ;
#31684=ORIENTED_EDGE('',*,*,#24216,.T.) ;
#31685=ORIENTED_EDGE('',*,*,#23983,.T.) ;
#31686=ORIENTED_EDGE('',*,*,#23833,.T.) ;
#31687=ORIENTED_EDGE('',*,*,#24217,.T.) ;
#31688=ORIENTED_EDGE('',*,*,#23989,.T.) ;
#31689=ORIENTED_EDGE('',*,*,#23832,.T.) ;
#31690=ORIENTED_EDGE('',*,*,#24218,.T.) ;
#31691=ORIENTED_EDGE('',*,*,#23831,.T.) ;
#31692=ORIENTED_EDGE('',*,*,#24213,.F.) ;
#31693=ORIENTED_EDGE('',*,*,#24219,.T.) ;
#31694=ORIENTED_EDGE('',*,*,#24220,.T.) ;
#31695=ORIENTED_EDGE('',*,*,#24221,.T.) ;
#31696=ORIENTED_EDGE('',*,*,#24218,.F.) ;
#31697=ORIENTED_EDGE('',*,*,#23854,.T.) ;
#31698=ORIENTED_EDGE('',*,*,#23985,.T.) ;
#31699=ORIENTED_EDGE('',*,*,#24222,.T.) ;
#31700=ORIENTED_EDGE('',*,*,#24223,.T.) ;
#31701=ORIENTED_EDGE('',*,*,#23855,.T.) ;
#31702=ORIENTED_EDGE('',*,*,#24223,.F.) ;
#31703=ORIENTED_EDGE('',*,*,#24224,.T.) ;
#31704=ORIENTED_EDGE('',*,*,#24225,.T.) ;
#31705=ORIENTED_EDGE('',*,*,#24226,.T.) ;
#31706=ORIENTED_EDGE('',*,*,#24215,.F.) ;
#31707=ORIENTED_EDGE('',*,*,#23984,.T.) ;
#31708=ORIENTED_EDGE('',*,*,#24227,.T.) ;
#31709=ORIENTED_EDGE('',*,*,#23975,.T.) ;
#31710=ORIENTED_EDGE('',*,*,#24228,.T.) ;
#31711=ORIENTED_EDGE('',*,*,#23834,.T.) ;
#31712=ORIENTED_EDGE('',*,*,#23982,.T.) ;
#31713=ORIENTED_EDGE('',*,*,#24229,.T.) ;
#31714=ORIENTED_EDGE('',*,*,#24230,.T.) ;
#31715=ORIENTED_EDGE('',*,*,#24231,.T.) ;
#31716=ORIENTED_EDGE('',*,*,#23977,.T.) ;
#31717=ORIENTED_EDGE('',*,*,#23852,.T.) ;
#31718=ORIENTED_EDGE('',*,*,#24232,.T.) ;
#31719=ORIENTED_EDGE('',*,*,#23976,.T.) ;
#31720=ORIENTED_EDGE('',*,*,#24233,.T.) ;
#31721=ORIENTED_EDGE('',*,*,#23968,.T.) ;
#31722=ORIENTED_EDGE('',*,*,#23837,.T.) ;
#31723=ORIENTED_EDGE('',*,*,#24234,.T.) ;
#31724=ORIENTED_EDGE('',*,*,#23974,.T.) ;
#31725=ORIENTED_EDGE('',*,*,#23836,.T.) ;
#31726=ORIENTED_EDGE('',*,*,#24235,.T.) ;
#31727=ORIENTED_EDGE('',*,*,#23835,.T.) ;
#31728=ORIENTED_EDGE('',*,*,#24230,.F.) ;
#31729=ORIENTED_EDGE('',*,*,#24236,.T.) ;
#31730=ORIENTED_EDGE('',*,*,#24237,.T.) ;
#31731=ORIENTED_EDGE('',*,*,#24238,.T.) ;
#31732=ORIENTED_EDGE('',*,*,#24235,.F.) ;
#31733=ORIENTED_EDGE('',*,*,#23850,.T.) ;
#31734=ORIENTED_EDGE('',*,*,#23970,.T.) ;
#31735=ORIENTED_EDGE('',*,*,#24239,.T.) ;
#31736=ORIENTED_EDGE('',*,*,#24240,.T.) ;
#31737=ORIENTED_EDGE('',*,*,#23851,.T.) ;
#31738=ORIENTED_EDGE('',*,*,#24240,.F.) ;
#31739=ORIENTED_EDGE('',*,*,#24241,.T.) ;
#31740=ORIENTED_EDGE('',*,*,#24242,.T.) ;
#31741=ORIENTED_EDGE('',*,*,#24243,.T.) ;
#31742=ORIENTED_EDGE('',*,*,#24232,.F.) ;
#31743=ORIENTED_EDGE('',*,*,#23969,.T.) ;
#31744=ORIENTED_EDGE('',*,*,#24244,.T.) ;
#31745=ORIENTED_EDGE('',*,*,#23960,.T.) ;
#31746=ORIENTED_EDGE('',*,*,#24245,.T.) ;
#31747=ORIENTED_EDGE('',*,*,#23838,.T.) ;
#31748=ORIENTED_EDGE('',*,*,#23967,.T.) ;
#31749=ORIENTED_EDGE('',*,*,#24246,.T.) ;
#31750=ORIENTED_EDGE('',*,*,#24247,.T.) ;
#31751=ORIENTED_EDGE('',*,*,#24248,.T.) ;
#31752=ORIENTED_EDGE('',*,*,#23962,.T.) ;
#31753=ORIENTED_EDGE('',*,*,#23848,.T.) ;
#31754=ORIENTED_EDGE('',*,*,#24249,.T.) ;
#31755=ORIENTED_EDGE('',*,*,#23961,.T.) ;
#31756=ORIENTED_EDGE('',*,*,#24250,.T.) ;
#31757=ORIENTED_EDGE('',*,*,#23953,.T.) ;
#31758=ORIENTED_EDGE('',*,*,#23841,.T.) ;
#31759=ORIENTED_EDGE('',*,*,#24251,.T.) ;
#31760=ORIENTED_EDGE('',*,*,#23959,.T.) ;
#31761=ORIENTED_EDGE('',*,*,#23840,.T.) ;
#31762=ORIENTED_EDGE('',*,*,#24252,.T.) ;
#31763=ORIENTED_EDGE('',*,*,#23839,.T.) ;
#31764=ORIENTED_EDGE('',*,*,#24247,.F.) ;
#31765=ORIENTED_EDGE('',*,*,#24253,.T.) ;
#31766=ORIENTED_EDGE('',*,*,#24254,.T.) ;
#31767=ORIENTED_EDGE('',*,*,#24255,.T.) ;
#31768=ORIENTED_EDGE('',*,*,#24252,.F.) ;
#31769=ORIENTED_EDGE('',*,*,#23846,.T.) ;
#31770=ORIENTED_EDGE('',*,*,#23955,.T.) ;
#31771=ORIENTED_EDGE('',*,*,#24256,.T.) ;
#31772=ORIENTED_EDGE('',*,*,#24257,.T.) ;
#31773=ORIENTED_EDGE('',*,*,#23847,.T.) ;
#31774=ORIENTED_EDGE('',*,*,#24257,.F.) ;
#31775=ORIENTED_EDGE('',*,*,#24258,.T.) ;
#31776=ORIENTED_EDGE('',*,*,#24259,.T.) ;
#31777=ORIENTED_EDGE('',*,*,#24260,.T.) ;
#31778=ORIENTED_EDGE('',*,*,#24249,.F.) ;
#31779=ORIENTED_EDGE('',*,*,#23954,.T.) ;
#31780=ORIENTED_EDGE('',*,*,#24261,.T.) ;
#31781=ORIENTED_EDGE('',*,*,#23950,.T.) ;
#31782=ORIENTED_EDGE('',*,*,#24262,.T.) ;
#31783=ORIENTED_EDGE('',*,*,#23842,.T.) ;
#31784=ORIENTED_EDGE('',*,*,#23952,.T.) ;
#31785=ORIENTED_EDGE('',*,*,#24263,.T.) ;
#31786=ORIENTED_EDGE('',*,*,#24264,.T.) ;
#31787=ORIENTED_EDGE('',*,*,#24265,.T.) ;
#31788=ORIENTED_EDGE('',*,*,#23949,.T.) ;
#31789=ORIENTED_EDGE('',*,*,#23844,.T.) ;
#31790=ORIENTED_EDGE('',*,*,#24266,.T.) ;
#31791=ORIENTED_EDGE('',*,*,#23843,.T.) ;
#31792=ORIENTED_EDGE('',*,*,#24264,.F.) ;
#31793=ORIENTED_EDGE('',*,*,#24267,.T.) ;
#31794=ORIENTED_EDGE('',*,*,#24268,.T.) ;
#31795=ORIENTED_EDGE('',*,*,#24269,.T.) ;
#31796=ORIENTED_EDGE('',*,*,#24266,.F.) ;
#31797=ORIENTED_EDGE('',*,*,#24256,.F.) ;
#31798=ORIENTED_EDGE('',*,*,#23966,.F.) ;
#31799=ORIENTED_EDGE('',*,*,#24248,.F.) ;
#31800=ORIENTED_EDGE('',*,*,#24260,.F.) ;
#31801=ORIENTED_EDGE('',*,*,#24270,.F.) ;
#31802=ORIENTED_EDGE('',*,*,#24258,.F.) ;
#31803=ORIENTED_EDGE('',*,*,#24239,.F.) ;
#31804=ORIENTED_EDGE('',*,*,#23981,.F.) ;
#31805=ORIENTED_EDGE('',*,*,#24231,.F.) ;
#31806=ORIENTED_EDGE('',*,*,#24243,.F.) ;
#31807=ORIENTED_EDGE('',*,*,#24271,.F.) ;
#31808=ORIENTED_EDGE('',*,*,#24241,.F.) ;
#31809=ORIENTED_EDGE('',*,*,#24222,.F.) ;
#31810=ORIENTED_EDGE('',*,*,#23996,.F.) ;
#31811=ORIENTED_EDGE('',*,*,#24214,.F.) ;
#31812=ORIENTED_EDGE('',*,*,#24226,.F.) ;
#31813=ORIENTED_EDGE('',*,*,#24272,.F.) ;
#31814=ORIENTED_EDGE('',*,*,#24224,.F.) ;
#31815=ORIENTED_EDGE('',*,*,#24205,.F.) ;
#31816=ORIENTED_EDGE('',*,*,#24012,.F.) ;
#31817=ORIENTED_EDGE('',*,*,#24197,.F.) ;
#31818=ORIENTED_EDGE('',*,*,#24209,.F.) ;
#31819=ORIENTED_EDGE('',*,*,#24273,.F.) ;
#31820=ORIENTED_EDGE('',*,*,#24207,.F.) ;
#31821=ORIENTED_EDGE('',*,*,#24188,.F.) ;
#31822=ORIENTED_EDGE('',*,*,#24027,.F.) ;
#31823=ORIENTED_EDGE('',*,*,#24180,.F.) ;
#31824=ORIENTED_EDGE('',*,*,#24192,.F.) ;
#31825=ORIENTED_EDGE('',*,*,#24274,.F.) ;
#31826=ORIENTED_EDGE('',*,*,#24190,.F.) ;
#31827=ORIENTED_EDGE('',*,*,#24171,.F.) ;
#31828=ORIENTED_EDGE('',*,*,#24042,.F.) ;
#31829=ORIENTED_EDGE('',*,*,#24163,.F.) ;
#31830=ORIENTED_EDGE('',*,*,#24175,.F.) ;
#31831=ORIENTED_EDGE('',*,*,#24275,.F.) ;
#31832=ORIENTED_EDGE('',*,*,#24173,.F.) ;
#31833=ORIENTED_EDGE('',*,*,#24154,.F.) ;
#31834=ORIENTED_EDGE('',*,*,#24057,.F.) ;
#31835=ORIENTED_EDGE('',*,*,#24146,.F.) ;
#31836=ORIENTED_EDGE('',*,*,#24158,.F.) ;
#31837=ORIENTED_EDGE('',*,*,#24276,.F.) ;
#31838=ORIENTED_EDGE('',*,*,#24156,.F.) ;
#31839=ORIENTED_EDGE('',*,*,#24137,.F.) ;
#31840=ORIENTED_EDGE('',*,*,#24072,.F.) ;
#31841=ORIENTED_EDGE('',*,*,#24129,.F.) ;
#31842=ORIENTED_EDGE('',*,*,#24141,.F.) ;
#31843=ORIENTED_EDGE('',*,*,#24277,.F.) ;
#31844=ORIENTED_EDGE('',*,*,#24139,.F.) ;
#31845=ORIENTED_EDGE('',*,*,#24120,.F.) ;
#31846=ORIENTED_EDGE('',*,*,#24087,.F.) ;
#31847=ORIENTED_EDGE('',*,*,#24112,.F.) ;
#31848=ORIENTED_EDGE('',*,*,#24124,.F.) ;
#31849=ORIENTED_EDGE('',*,*,#24278,.F.) ;
#31850=ORIENTED_EDGE('',*,*,#24122,.F.) ;
#31851=ORIENTED_EDGE('',*,*,#24103,.F.) ;
#31852=ORIENTED_EDGE('',*,*,#24099,.F.) ;
#31853=ORIENTED_EDGE('',*,*,#24101,.F.) ;
#31854=ORIENTED_EDGE('',*,*,#24111,.F.) ;
#31855=ORIENTED_EDGE('',*,*,#24279,.F.) ;
#31856=ORIENTED_EDGE('',*,*,#24109,.F.) ;
#31857=ORIENTED_EDGE('',*,*,#24107,.F.) ;
#31858=ORIENTED_EDGE('',*,*,#24106,.F.) ;
#31859=ORIENTED_EDGE('',*,*,#24115,.F.) ;
#31860=ORIENTED_EDGE('',*,*,#24119,.F.) ;
#31861=ORIENTED_EDGE('',*,*,#24280,.F.) ;
#31862=ORIENTED_EDGE('',*,*,#24117,.F.) ;
#31863=ORIENTED_EDGE('',*,*,#24127,.F.) ;
#31864=ORIENTED_EDGE('',*,*,#24126,.F.) ;
#31865=ORIENTED_EDGE('',*,*,#24132,.F.) ;
#31866=ORIENTED_EDGE('',*,*,#24136,.F.) ;
#31867=ORIENTED_EDGE('',*,*,#24281,.F.) ;
#31868=ORIENTED_EDGE('',*,*,#24134,.F.) ;
#31869=ORIENTED_EDGE('',*,*,#24144,.F.) ;
#31870=ORIENTED_EDGE('',*,*,#24143,.F.) ;
#31871=ORIENTED_EDGE('',*,*,#24149,.F.) ;
#31872=ORIENTED_EDGE('',*,*,#24153,.F.) ;
#31873=ORIENTED_EDGE('',*,*,#24282,.F.) ;
#31874=ORIENTED_EDGE('',*,*,#24151,.F.) ;
#31875=ORIENTED_EDGE('',*,*,#24161,.F.) ;
#31876=ORIENTED_EDGE('',*,*,#24160,.F.) ;
#31877=ORIENTED_EDGE('',*,*,#24166,.F.) ;
#31878=ORIENTED_EDGE('',*,*,#24170,.F.) ;
#31879=ORIENTED_EDGE('',*,*,#24283,.F.) ;
#31880=ORIENTED_EDGE('',*,*,#24168,.F.) ;
#31881=ORIENTED_EDGE('',*,*,#24178,.F.) ;
#31882=ORIENTED_EDGE('',*,*,#24177,.F.) ;
#31883=ORIENTED_EDGE('',*,*,#24183,.F.) ;
#31884=ORIENTED_EDGE('',*,*,#24187,.F.) ;
#31885=ORIENTED_EDGE('',*,*,#24284,.F.) ;
#31886=ORIENTED_EDGE('',*,*,#24185,.F.) ;
#31887=ORIENTED_EDGE('',*,*,#24195,.F.) ;
#31888=ORIENTED_EDGE('',*,*,#24194,.F.) ;
#31889=ORIENTED_EDGE('',*,*,#24200,.F.) ;
#31890=ORIENTED_EDGE('',*,*,#24204,.F.) ;
#31891=ORIENTED_EDGE('',*,*,#24285,.F.) ;
#31892=ORIENTED_EDGE('',*,*,#24202,.F.) ;
#31893=ORIENTED_EDGE('',*,*,#24212,.F.) ;
#31894=ORIENTED_EDGE('',*,*,#24211,.F.) ;
#31895=ORIENTED_EDGE('',*,*,#24217,.F.) ;
#31896=ORIENTED_EDGE('',*,*,#24221,.F.) ;
#31897=ORIENTED_EDGE('',*,*,#24286,.F.) ;
#31898=ORIENTED_EDGE('',*,*,#24219,.F.) ;
#31899=ORIENTED_EDGE('',*,*,#24229,.F.) ;
#31900=ORIENTED_EDGE('',*,*,#24228,.F.) ;
#31901=ORIENTED_EDGE('',*,*,#24234,.F.) ;
#31902=ORIENTED_EDGE('',*,*,#24238,.F.) ;
#31903=ORIENTED_EDGE('',*,*,#24287,.F.) ;
#31904=ORIENTED_EDGE('',*,*,#24236,.F.) ;
#31905=ORIENTED_EDGE('',*,*,#24246,.F.) ;
#31906=ORIENTED_EDGE('',*,*,#24245,.F.) ;
#31907=ORIENTED_EDGE('',*,*,#24251,.F.) ;
#31908=ORIENTED_EDGE('',*,*,#24255,.F.) ;
#31909=ORIENTED_EDGE('',*,*,#24288,.F.) ;
#31910=ORIENTED_EDGE('',*,*,#24253,.F.) ;
#31911=ORIENTED_EDGE('',*,*,#24263,.F.) ;
#31912=ORIENTED_EDGE('',*,*,#24262,.F.) ;
#31913=ORIENTED_EDGE('',*,*,#24265,.F.) ;
#31914=ORIENTED_EDGE('',*,*,#24269,.F.) ;
#31915=ORIENTED_EDGE('',*,*,#24289,.F.) ;
#31916=ORIENTED_EDGE('',*,*,#24267,.F.) ;
#31917=ORIENTED_EDGE('',*,*,#24010,.F.) ;
#31918=ORIENTED_EDGE('',*,*,#24003,.F.) ;
#31919=ORIENTED_EDGE('',*,*,#23995,.F.) ;
#31920=ORIENTED_EDGE('',*,*,#23988,.F.) ;
#31921=ORIENTED_EDGE('',*,*,#23980,.F.) ;
#31922=ORIENTED_EDGE('',*,*,#23973,.F.) ;
#31923=ORIENTED_EDGE('',*,*,#23965,.F.) ;
#31924=ORIENTED_EDGE('',*,*,#23958,.F.) ;
#31925=ORIENTED_EDGE('',*,*,#24261,.F.) ;
#31926=ORIENTED_EDGE('',*,*,#24250,.F.) ;
#31927=ORIENTED_EDGE('',*,*,#24244,.F.) ;
#31928=ORIENTED_EDGE('',*,*,#24233,.F.) ;
#31929=ORIENTED_EDGE('',*,*,#24227,.F.) ;
#31930=ORIENTED_EDGE('',*,*,#24216,.F.) ;
#31931=ORIENTED_EDGE('',*,*,#24210,.F.) ;
#31932=ORIENTED_EDGE('',*,*,#24199,.F.) ;
#31933=ORIENTED_EDGE('',*,*,#24193,.F.) ;
#31934=ORIENTED_EDGE('',*,*,#24182,.F.) ;
#31935=ORIENTED_EDGE('',*,*,#24176,.F.) ;
#31936=ORIENTED_EDGE('',*,*,#24165,.F.) ;
#31937=ORIENTED_EDGE('',*,*,#24159,.F.) ;
#31938=ORIENTED_EDGE('',*,*,#24148,.F.) ;
#31939=ORIENTED_EDGE('',*,*,#24142,.F.) ;
#31940=ORIENTED_EDGE('',*,*,#24131,.F.) ;
#31941=ORIENTED_EDGE('',*,*,#24125,.F.) ;
#31942=ORIENTED_EDGE('',*,*,#24114,.F.) ;
#31943=ORIENTED_EDGE('',*,*,#24105,.F.) ;
#31944=ORIENTED_EDGE('',*,*,#24100,.F.) ;
#31945=ORIENTED_EDGE('',*,*,#24098,.F.) ;
#31946=ORIENTED_EDGE('',*,*,#24094,.F.) ;
#31947=ORIENTED_EDGE('',*,*,#24086,.F.) ;
#31948=ORIENTED_EDGE('',*,*,#24079,.F.) ;
#31949=ORIENTED_EDGE('',*,*,#24071,.F.) ;
#31950=ORIENTED_EDGE('',*,*,#24064,.F.) ;
#31951=ORIENTED_EDGE('',*,*,#24056,.F.) ;
#31952=ORIENTED_EDGE('',*,*,#24049,.F.) ;
#31953=ORIENTED_EDGE('',*,*,#24041,.F.) ;
#31954=ORIENTED_EDGE('',*,*,#24034,.F.) ;
#31955=ORIENTED_EDGE('',*,*,#24026,.F.) ;
#31956=ORIENTED_EDGE('',*,*,#24019,.F.) ;
#31957=ORIENTED_EDGE('',*,*,#24011,.F.) ;
#31958=ORIENTED_EDGE('',*,*,#24290,.T.) ;
#31959=ORIENTED_EDGE('',*,*,#24291,.F.) ;
#31960=ORIENTED_EDGE('',*,*,#24290,.F.) ;
#31961=ORIENTED_EDGE('',*,*,#24292,.T.) ;
#31962=ORIENTED_EDGE('',*,*,#24293,.T.) ;
#31963=ORIENTED_EDGE('',*,*,#24294,.T.) ;
#31964=ORIENTED_EDGE('',*,*,#23948,.T.) ;
#31965=ORIENTED_EDGE('',*,*,#24295,.F.) ;
#31966=ORIENTED_EDGE('',*,*,#24293,.F.) ;
#31967=ORIENTED_EDGE('',*,*,#24296,.F.) ;
#31968=ORIENTED_EDGE('',*,*,#24297,.F.) ;
#31969=ORIENTED_EDGE('',*,*,#24298,.F.) ;
#31970=ORIENTED_EDGE('',*,*,#24299,.F.) ;
#31971=ORIENTED_EDGE('',*,*,#24300,.F.) ;
#31972=ORIENTED_EDGE('',*,*,#24301,.F.) ;
#31973=ORIENTED_EDGE('',*,*,#24302,.F.) ;
#31974=ORIENTED_EDGE('',*,*,#24303,.F.) ;
#31975=ORIENTED_EDGE('',*,*,#24304,.F.) ;
#31976=ORIENTED_EDGE('',*,*,#24305,.F.) ;
#31977=ORIENTED_EDGE('',*,*,#24306,.F.) ;
#31978=ORIENTED_EDGE('',*,*,#24307,.F.) ;
#31979=ORIENTED_EDGE('',*,*,#24308,.F.) ;
#31980=ORIENTED_EDGE('',*,*,#24309,.F.) ;
#31981=ORIENTED_EDGE('',*,*,#24310,.F.) ;
#31982=ORIENTED_EDGE('',*,*,#24311,.F.) ;
#31983=ORIENTED_EDGE('',*,*,#24312,.F.) ;
#31984=ORIENTED_EDGE('',*,*,#24313,.F.) ;
#31985=ORIENTED_EDGE('',*,*,#24314,.F.) ;
#31986=ORIENTED_EDGE('',*,*,#24315,.F.) ;
#31987=ORIENTED_EDGE('',*,*,#24316,.F.) ;
#31988=ORIENTED_EDGE('',*,*,#24317,.F.) ;
#31989=ORIENTED_EDGE('',*,*,#24318,.F.) ;
#31990=ORIENTED_EDGE('',*,*,#24292,.F.) ;
#31991=ORIENTED_EDGE('',*,*,#24319,.T.) ;
#31992=ORIENTED_EDGE('',*,*,#24320,.T.) ;
#31993=ORIENTED_EDGE('',*,*,#24296,.T.) ;
#31994=ORIENTED_EDGE('',*,*,#23911,.F.) ;
#31995=ORIENTED_EDGE('',*,*,#24321,.F.) ;
#31996=ORIENTED_EDGE('',*,*,#24319,.F.) ;
#31997=ORIENTED_EDGE('',*,*,#23947,.F.) ;
#31998=ORIENTED_EDGE('',*,*,#24322,.T.) ;
#31999=ORIENTED_EDGE('',*,*,#24313,.T.) ;
#32000=ORIENTED_EDGE('',*,*,#24323,.T.) ;
#32001=ORIENTED_EDGE('',*,*,#23936,.T.) ;
#32002=ORIENTED_EDGE('',*,*,#24322,.F.) ;
#32003=ORIENTED_EDGE('',*,*,#23938,.T.) ;
#32004=ORIENTED_EDGE('',*,*,#24324,.T.) ;
#32005=ORIENTED_EDGE('',*,*,#24314,.T.) ;
#32006=ORIENTED_EDGE('',*,*,#24325,.T.) ;
#32007=ORIENTED_EDGE('',*,*,#24301,.T.) ;
#32008=ORIENTED_EDGE('',*,*,#24326,.T.) ;
#32009=ORIENTED_EDGE('',*,*,#24327,.T.) ;
#32010=ORIENTED_EDGE('',*,*,#23897,.F.) ;
#32011=ORIENTED_EDGE('',*,*,#24328,.T.) ;
#32012=ORIENTED_EDGE('',*,*,#24327,.F.) ;
#32013=ORIENTED_EDGE('',*,*,#24329,.T.) ;
#32014=ORIENTED_EDGE('',*,*,#24325,.F.) ;
#32015=ORIENTED_EDGE('',*,*,#24330,.T.) ;
#32016=ORIENTED_EDGE('',*,*,#24331,.T.) ;
#32017=ORIENTED_EDGE('',*,*,#24302,.T.) ;
#32018=ORIENTED_EDGE('',*,*,#23900,.F.) ;
#32019=ORIENTED_EDGE('',*,*,#24332,.F.) ;
#32020=ORIENTED_EDGE('',*,*,#24330,.F.) ;
#32021=ORIENTED_EDGE('',*,*,#24328,.F.) ;
#32022=ORIENTED_EDGE('',*,*,#24333,.T.) ;
#32023=ORIENTED_EDGE('',*,*,#24307,.T.) ;
#32024=ORIENTED_EDGE('',*,*,#24334,.T.) ;
#32025=ORIENTED_EDGE('',*,*,#24335,.T.) ;
#32026=ORIENTED_EDGE('',*,*,#23883,.F.) ;
#32027=ORIENTED_EDGE('',*,*,#23926,.T.) ;
#32028=ORIENTED_EDGE('',*,*,#24335,.F.) ;
#32029=ORIENTED_EDGE('',*,*,#24336,.T.) ;
#32030=ORIENTED_EDGE('',*,*,#24333,.F.) ;
#32031=ORIENTED_EDGE('',*,*,#23925,.T.) ;
#32032=ORIENTED_EDGE('',*,*,#24337,.T.) ;
#32033=ORIENTED_EDGE('',*,*,#24308,.T.) ;
#32034=ORIENTED_EDGE('',*,*,#24291,.T.) ;
#32035=ORIENTED_EDGE('',*,*,#24338,.T.) ;
#32036=ORIENTED_EDGE('',*,*,#24295,.T.) ;
#32037=ORIENTED_EDGE('',*,*,#24338,.F.) ;
#32038=ORIENTED_EDGE('',*,*,#24315,.T.) ;
#32039=ORIENTED_EDGE('',*,*,#24324,.F.) ;
#32040=ORIENTED_EDGE('',*,*,#23940,.F.) ;
#32041=ORIENTED_EDGE('',*,*,#24339,.F.) ;
#32042=ORIENTED_EDGE('',*,*,#24317,.T.) ;
#32043=ORIENTED_EDGE('',*,*,#24340,.F.) ;
#32044=ORIENTED_EDGE('',*,*,#23944,.F.) ;
#32045=ORIENTED_EDGE('',*,*,#24341,.F.) ;
#32046=ORIENTED_EDGE('',*,*,#24340,.T.) ;
#32047=ORIENTED_EDGE('',*,*,#24316,.T.) ;
#32048=ORIENTED_EDGE('',*,*,#24339,.T.) ;
#32049=ORIENTED_EDGE('',*,*,#23942,.T.) ;
#32050=ORIENTED_EDGE('',*,*,#23932,.F.) ;
#32051=ORIENTED_EDGE('',*,*,#24342,.F.) ;
#32052=ORIENTED_EDGE('',*,*,#24311,.T.) ;
#32053=ORIENTED_EDGE('',*,*,#24343,.F.) ;
#32054=ORIENTED_EDGE('',*,*,#24323,.F.) ;
#32055=ORIENTED_EDGE('',*,*,#24312,.T.) ;
#32056=ORIENTED_EDGE('',*,*,#24342,.T.) ;
#32057=ORIENTED_EDGE('',*,*,#23934,.T.) ;
#32058=ORIENTED_EDGE('',*,*,#24294,.F.) ;
#32059=ORIENTED_EDGE('',*,*,#24318,.T.) ;
#32060=ORIENTED_EDGE('',*,*,#24341,.T.) ;
#32061=ORIENTED_EDGE('',*,*,#23946,.T.) ;
#32062=ORIENTED_EDGE('',*,*,#24309,.T.) ;
#32063=ORIENTED_EDGE('',*,*,#24337,.F.) ;
#32064=ORIENTED_EDGE('',*,*,#23928,.F.) ;
#32065=ORIENTED_EDGE('',*,*,#24344,.F.) ;
#32066=ORIENTED_EDGE('',*,*,#24297,.T.) ;
#32067=ORIENTED_EDGE('',*,*,#24320,.F.) ;
#32068=ORIENTED_EDGE('',*,*,#24345,.F.) ;
#32069=ORIENTED_EDGE('',*,*,#24346,.F.) ;
#32070=ORIENTED_EDGE('',*,*,#23916,.F.) ;
#32071=ORIENTED_EDGE('',*,*,#24347,.T.) ;
#32072=ORIENTED_EDGE('',*,*,#24345,.T.) ;
#32073=ORIENTED_EDGE('',*,*,#24321,.T.) ;
#32074=ORIENTED_EDGE('',*,*,#24299,.T.) ;
#32075=ORIENTED_EDGE('',*,*,#24348,.F.) ;
#32076=ORIENTED_EDGE('',*,*,#24349,.F.) ;
#32077=ORIENTED_EDGE('',*,*,#24350,.F.) ;
#32078=ORIENTED_EDGE('',*,*,#24348,.T.) ;
#32079=ORIENTED_EDGE('',*,*,#24298,.T.) ;
#32080=ORIENTED_EDGE('',*,*,#24346,.T.) ;
#32081=ORIENTED_EDGE('',*,*,#24351,.T.) ;
#32082=ORIENTED_EDGE('',*,*,#23917,.F.) ;
#32083=ORIENTED_EDGE('',*,*,#24352,.T.) ;
#32084=ORIENTED_EDGE('',*,*,#24349,.T.) ;
#32085=ORIENTED_EDGE('',*,*,#24353,.T.) ;
#32086=ORIENTED_EDGE('',*,*,#24305,.T.) ;
#32087=ORIENTED_EDGE('',*,*,#24354,.F.) ;
#32088=ORIENTED_EDGE('',*,*,#24355,.F.) ;
#32089=ORIENTED_EDGE('',*,*,#24356,.F.) ;
#32090=ORIENTED_EDGE('',*,*,#24326,.F.) ;
#32091=ORIENTED_EDGE('',*,*,#24300,.T.) ;
#32092=ORIENTED_EDGE('',*,*,#24350,.T.) ;
#32093=ORIENTED_EDGE('',*,*,#24357,.T.) ;
#32094=ORIENTED_EDGE('',*,*,#24303,.T.) ;
#32095=ORIENTED_EDGE('',*,*,#24331,.F.) ;
#32096=ORIENTED_EDGE('',*,*,#24358,.F.) ;
#32097=ORIENTED_EDGE('',*,*,#24359,.F.) ;
#32098=ORIENTED_EDGE('',*,*,#23918,.F.) ;
#32099=ORIENTED_EDGE('',*,*,#24360,.T.) ;
#32100=ORIENTED_EDGE('',*,*,#24358,.T.) ;
#32101=ORIENTED_EDGE('',*,*,#24332,.T.) ;
#32102=ORIENTED_EDGE('',*,*,#24354,.T.) ;
#32103=ORIENTED_EDGE('',*,*,#24304,.T.) ;
#32104=ORIENTED_EDGE('',*,*,#24359,.T.) ;
#32105=ORIENTED_EDGE('',*,*,#24361,.T.) ;
#32106=ORIENTED_EDGE('',*,*,#23919,.F.) ;
#32107=ORIENTED_EDGE('',*,*,#24362,.T.) ;
#32108=ORIENTED_EDGE('',*,*,#24355,.T.) ;
#32109=ORIENTED_EDGE('',*,*,#24363,.T.) ;
#32110=ORIENTED_EDGE('',*,*,#24334,.F.) ;
#32111=ORIENTED_EDGE('',*,*,#24306,.T.) ;
#32112=ORIENTED_EDGE('',*,*,#24356,.T.) ;
#32113=ORIENTED_EDGE('',*,*,#24364,.T.) ;
#32114=ORIENTED_EDGE('',*,*,#24343,.T.) ;
#32115=ORIENTED_EDGE('',*,*,#24310,.T.) ;
#32116=ORIENTED_EDGE('',*,*,#24344,.T.) ;
#32117=ORIENTED_EDGE('',*,*,#23930,.T.) ;
#32118=ORIENTED_EDGE('',*,*,#24110,.F.) ;
#32119=ORIENTED_EDGE('',*,*,#24279,.T.) ;
#32120=ORIENTED_EDGE('',*,*,#24118,.F.) ;
#32121=ORIENTED_EDGE('',*,*,#24280,.T.) ;
#32122=ORIENTED_EDGE('',*,*,#24135,.F.) ;
#32123=ORIENTED_EDGE('',*,*,#24281,.T.) ;
#32124=ORIENTED_EDGE('',*,*,#24152,.F.) ;
#32125=ORIENTED_EDGE('',*,*,#24282,.T.) ;
#32126=ORIENTED_EDGE('',*,*,#24169,.F.) ;
#32127=ORIENTED_EDGE('',*,*,#24283,.T.) ;
#32128=ORIENTED_EDGE('',*,*,#24186,.F.) ;
#32129=ORIENTED_EDGE('',*,*,#24284,.T.) ;
#32130=ORIENTED_EDGE('',*,*,#24203,.F.) ;
#32131=ORIENTED_EDGE('',*,*,#24285,.T.) ;
#32132=ORIENTED_EDGE('',*,*,#24220,.F.) ;
#32133=ORIENTED_EDGE('',*,*,#24286,.T.) ;
#32134=ORIENTED_EDGE('',*,*,#24237,.F.) ;
#32135=ORIENTED_EDGE('',*,*,#24287,.T.) ;
#32136=ORIENTED_EDGE('',*,*,#24254,.F.) ;
#32137=ORIENTED_EDGE('',*,*,#24288,.T.) ;
#32138=ORIENTED_EDGE('',*,*,#24268,.F.) ;
#32139=ORIENTED_EDGE('',*,*,#24289,.T.) ;
#32140=ORIENTED_EDGE('',*,*,#24259,.F.) ;
#32141=ORIENTED_EDGE('',*,*,#24270,.T.) ;
#32142=ORIENTED_EDGE('',*,*,#24242,.F.) ;
#32143=ORIENTED_EDGE('',*,*,#24271,.T.) ;
#32144=ORIENTED_EDGE('',*,*,#24225,.F.) ;
#32145=ORIENTED_EDGE('',*,*,#24272,.T.) ;
#32146=ORIENTED_EDGE('',*,*,#24208,.F.) ;
#32147=ORIENTED_EDGE('',*,*,#24273,.T.) ;
#32148=ORIENTED_EDGE('',*,*,#24191,.F.) ;
#32149=ORIENTED_EDGE('',*,*,#24274,.T.) ;
#32150=ORIENTED_EDGE('',*,*,#24174,.F.) ;
#32151=ORIENTED_EDGE('',*,*,#24275,.T.) ;
#32152=ORIENTED_EDGE('',*,*,#24157,.F.) ;
#32153=ORIENTED_EDGE('',*,*,#24276,.T.) ;
#32154=ORIENTED_EDGE('',*,*,#24140,.F.) ;
#32155=ORIENTED_EDGE('',*,*,#24277,.T.) ;
#32156=ORIENTED_EDGE('',*,*,#24123,.F.) ;
#32157=ORIENTED_EDGE('',*,*,#24278,.T.) ;
#32158=ORIENTED_EDGE('',*,*,#23895,.F.) ;
#32159=ORIENTED_EDGE('',*,*,#24329,.F.) ;
#32160=ORIENTED_EDGE('',*,*,#24357,.F.) ;
#32161=ORIENTED_EDGE('',*,*,#24352,.F.) ;
#32162=ORIENTED_EDGE('',*,*,#23891,.F.) ;
#32163=ORIENTED_EDGE('',*,*,#24363,.F.) ;
#32164=ORIENTED_EDGE('',*,*,#24361,.F.) ;
#32165=ORIENTED_EDGE('',*,*,#24360,.F.) ;
#32166=ORIENTED_EDGE('',*,*,#23881,.F.) ;
#32167=ORIENTED_EDGE('',*,*,#24336,.F.) ;
#32168=ORIENTED_EDGE('',*,*,#24364,.F.) ;
#32169=ORIENTED_EDGE('',*,*,#24362,.F.) ;
#32170=ORIENTED_EDGE('',*,*,#23905,.F.) ;
#32171=ORIENTED_EDGE('',*,*,#24353,.F.) ;
#32172=ORIENTED_EDGE('',*,*,#24351,.F.) ;
#32173=ORIENTED_EDGE('',*,*,#24347,.F.) ;
#45432=TOROIDAL_SURFACE('',#49312,5.8,0.2) ;
#45433=TOROIDAL_SURFACE('',#49365,1.15,0.2) ;
#45434=TOROIDAL_SURFACE('',#49377,1.15,0.2) ;
#45435=TOROIDAL_SURFACE('',#49389,1.15,0.2) ;
#45436=TOROIDAL_SURFACE('',#49398,1.15,0.2) ;
#45437=TOROIDAL_SURFACE('',#49454,5.8,0.2) ;
#45438=TOROIDAL_SURFACE('',#49472,5.8,0.2) ;
#45439=TOROIDAL_SURFACE('',#49490,5.8,0.2) ;
#45440=TOROIDAL_SURFACE('',#49508,5.8,0.2) ;
#45441=TOROIDAL_SURFACE('',#49526,5.8,0.2) ;
#45442=TOROIDAL_SURFACE('',#49544,5.8,0.2) ;
#45443=TOROIDAL_SURFACE('',#49562,5.8,0.2) ;
#45444=TOROIDAL_SURFACE('',#49580,5.8,0.2) ;
#45445=TOROIDAL_SURFACE('',#49598,5.8,0.2) ;
#45446=TOROIDAL_SURFACE('',#49616,5.8,0.2) ;
#45447=TOROIDAL_SURFACE('',#49622,5.8,0.2) ;
#45448=TOROIDAL_SURFACE('',#49627,5.8,0.2) ;
#45449=TOROIDAL_SURFACE('',#49630,5.8,0.2) ;
#45450=TOROIDAL_SURFACE('',#49633,5.8,0.2) ;
#45451=TOROIDAL_SURFACE('',#49636,5.8,0.2) ;
#45452=TOROIDAL_SURFACE('',#49640,5.8,0.2) ;
#45453=TOROIDAL_SURFACE('',#49643,5.8,0.2) ;
#45454=TOROIDAL_SURFACE('',#49646,5.8,0.2) ;
#45455=TOROIDAL_SURFACE('',#49650,5.8,0.2) ;
#45456=TOROIDAL_SURFACE('',#49653,5.8,0.2) ;
#45457=TOROIDAL_SURFACE('',#49656,5.8,0.2) ;
#45458=TOROIDAL_SURFACE('',#49660,5.8,0.2) ;
#45459=TOROIDAL_SURFACE('',#49663,5.8,0.2) ;
#45460=TOROIDAL_SURFACE('',#49666,5.8,0.2) ;
#45461=TOROIDAL_SURFACE('',#49670,5.8,0.2) ;
#45462=TOROIDAL_SURFACE('',#49673,5.8,0.2) ;
#45463=TOROIDAL_SURFACE('',#49676,5.8,0.2) ;
#45464=TOROIDAL_SURFACE('',#49680,5.8,0.2) ;
#45465=TOROIDAL_SURFACE('',#49683,5.8,0.2) ;
#45466=TOROIDAL_SURFACE('',#49686,5.8,0.2) ;
#45467=TOROIDAL_SURFACE('',#49690,5.8,0.2) ;
#45468=TOROIDAL_SURFACE('',#49693,5.8,0.2) ;
#45469=TOROIDAL_SURFACE('',#49696,5.8,0.2) ;
#45470=TOROIDAL_SURFACE('',#49700,5.8,0.2) ;
#45471=TOROIDAL_SURFACE('',#49703,5.8,0.2) ;
#45472=TOROIDAL_SURFACE('',#49706,5.8,0.2) ;
#45473=TOROIDAL_SURFACE('',#49710,5.8,0.2) ;
#45474=TOROIDAL_SURFACE('',#49713,5.8,0.2) ;
#45475=TOROIDAL_SURFACE('',#49716,5.8,0.2) ;
#45476=TOROIDAL_SURFACE('',#49720,5.8,0.2) ;
#45477=TOROIDAL_SURFACE('',#49764,0.75,0.2) ;
#45478=TOROIDAL_SURFACE('',#49784,0.75,0.2) ;
#45479=TOROIDAL_SURFACE('',#49789,0.75,0.2) ;
#45480=TOROIDAL_SURFACE('',#49797,0.75,0.2) ;
#45481=TOROIDAL_SURFACE('',#49804,5.13915047169858,0.2) ;
#45482=TOROIDAL_SURFACE('',#49806,0.399999999999991,0.2) ;
#45483=TOROIDAL_SURFACE('',#49808,0.399999999999991,0.2) ;
#45484=TOROIDAL_SURFACE('',#49812,0.399999999999956,0.199999999999996) ;
#45485=TOROIDAL_SURFACE('',#49817,0.399999999999991,0.2) ;
#45486=TOROIDAL_SURFACE('',#49819,0.399999999999991,0.2) ;
#45487=TOROIDAL_SURFACE('',#49823,0.399999999999991,0.2) ;
#45488=TOROIDAL_SURFACE('',#49829,0.399999999999991,0.2) ;
#45489=TOROIDAL_SURFACE('',#49834,0.399999999999991,0.2) ;
#45965=ADVANCED_FACE('',(#10747),#45432,.T.) ;
#45966=ADVANCED_FACE('',(#10748),#9460,.T.) ;
#45967=ADVANCED_FACE('',(#10749),#2216,.F.) ;
#45968=ADVANCED_FACE('',(#10750),#9461,.F.) ;
#45969=ADVANCED_FACE('',(#10751),#9462,.F.) ;
#45970=ADVANCED_FACE('',(#10752),#45433,.F.) ;
#45971=ADVANCED_FACE('',(#10753),#9463,.F.) ;
#45972=ADVANCED_FACE('',(#10754),#9464,.F.) ;
#45973=ADVANCED_FACE('',(#10755),#9465,.F.) ;
#45974=ADVANCED_FACE('',(#10756),#45434,.F.) ;
#45975=ADVANCED_FACE('',(#10757),#9466,.F.) ;
#45976=ADVANCED_FACE('',(#10758),#9467,.F.) ;
#45977=ADVANCED_FACE('',(#10759),#9468,.F.) ;
#45978=ADVANCED_FACE('',(#10760),#45435,.F.) ;
#45979=ADVANCED_FACE('',(#10761),#9469,.F.) ;
#45980=ADVANCED_FACE('',(#10762),#9470,.F.) ;
#45981=ADVANCED_FACE('',(#10763),#45436,.F.) ;
#45982=ADVANCED_FACE('',(#10764),#9471,.F.) ;
#45983=ADVANCED_FACE('',(#10765),#9472,.F.) ;
#45984=ADVANCED_FACE('',(#10766),#2119,.F.) ;
#45985=ADVANCED_FACE('',(#10767),#2120,.F.) ;
#45986=ADVANCED_FACE('',(#10768),#2121,.F.) ;
#45987=ADVANCED_FACE('',(#10769),#2122,.F.) ;
#45988=ADVANCED_FACE('',(#10770),#2123,.F.) ;
#45989=ADVANCED_FACE('',(#10771),#2124,.F.) ;
#45990=ADVANCED_FACE('',(#10772),#2125,.F.) ;
#45991=ADVANCED_FACE('',(#10773),#2126,.F.) ;
#45992=ADVANCED_FACE('',(#10774),#2217,.F.) ;
#45993=ADVANCED_FACE('',(#10775),#9473,.F.) ;
#45994=ADVANCED_FACE('',(#10776),#2218,.F.) ;
#45995=ADVANCED_FACE('',(#10777),#9474,.F.) ;
#45996=ADVANCED_FACE('',(#10778),#2219,.F.) ;
#45997=ADVANCED_FACE('',(#10779),#9475,.T.) ;
#45998=ADVANCED_FACE('',(#10780),#2220,.F.) ;
#45999=ADVANCED_FACE('',(#10781),#9476,.F.) ;
#46000=ADVANCED_FACE('',(#10782),#2221,.F.) ;
#46001=ADVANCED_FACE('',(#10783),#9477,.F.) ;
#46002=ADVANCED_FACE('',(#10784),#2222,.F.) ;
#46003=ADVANCED_FACE('',(#10785),#9478,.T.) ;
#46004=ADVANCED_FACE('',(#10786),#2223,.T.) ;
#46005=ADVANCED_FACE('',(#10787),#2127,.T.) ;
#46006=ADVANCED_FACE('',(#10788),#2128,.T.) ;
#46007=ADVANCED_FACE('',(#10789),#2129,.T.) ;
#46008=ADVANCED_FACE('',(#10790),#45437,.T.) ;
#46009=ADVANCED_FACE('',(#10791),#2130,.T.) ;
#46010=ADVANCED_FACE('',(#10792),#2131,.T.) ;
#46011=ADVANCED_FACE('',(#10793),#1769,.F.) ;
#46012=ADVANCED_FACE('',(#10794),#2132,.T.) ;
#46013=ADVANCED_FACE('',(#10795),#2133,.T.) ;
#46014=ADVANCED_FACE('',(#10796),#45438,.T.) ;
#46015=ADVANCED_FACE('',(#10797),#2134,.T.) ;
#46016=ADVANCED_FACE('',(#10798),#2135,.T.) ;
#46017=ADVANCED_FACE('',(#10799),#1770,.F.) ;
#46018=ADVANCED_FACE('',(#10800),#2136,.T.) ;
#46019=ADVANCED_FACE('',(#10801),#2137,.T.) ;
#46020=ADVANCED_FACE('',(#10802),#45439,.T.) ;
#46021=ADVANCED_FACE('',(#10803),#2138,.T.) ;
#46022=ADVANCED_FACE('',(#10804),#2139,.T.) ;
#46023=ADVANCED_FACE('',(#10805),#1771,.F.) ;
#46024=ADVANCED_FACE('',(#10806),#2140,.T.) ;
#46025=ADVANCED_FACE('',(#10807),#2141,.T.) ;
#46026=ADVANCED_FACE('',(#10808),#45440,.T.) ;
#46027=ADVANCED_FACE('',(#10809),#2142,.T.) ;
#46028=ADVANCED_FACE('',(#10810),#2143,.T.) ;
#46029=ADVANCED_FACE('',(#10811),#1772,.F.) ;
#46030=ADVANCED_FACE('',(#10812),#2144,.T.) ;
#46031=ADVANCED_FACE('',(#10813),#2145,.T.) ;
#46032=ADVANCED_FACE('',(#10814),#45441,.T.) ;
#46033=ADVANCED_FACE('',(#10815),#2146,.T.) ;
#46034=ADVANCED_FACE('',(#10816),#2147,.T.) ;
#46035=ADVANCED_FACE('',(#10817),#1773,.F.) ;
#46036=ADVANCED_FACE('',(#10818),#2148,.T.) ;
#46037=ADVANCED_FACE('',(#10819),#2149,.T.) ;
#46038=ADVANCED_FACE('',(#10820),#45442,.T.) ;
#46039=ADVANCED_FACE('',(#10821),#2150,.T.) ;
#46040=ADVANCED_FACE('',(#10822),#2151,.T.) ;
#46041=ADVANCED_FACE('',(#10823),#1774,.F.) ;
#46042=ADVANCED_FACE('',(#10824),#2152,.T.) ;
#46043=ADVANCED_FACE('',(#10825),#2153,.T.) ;
#46044=ADVANCED_FACE('',(#10826),#45443,.T.) ;
#46045=ADVANCED_FACE('',(#10827),#2154,.T.) ;
#46046=ADVANCED_FACE('',(#10828),#2155,.T.) ;
#46047=ADVANCED_FACE('',(#10829),#1775,.F.) ;
#46048=ADVANCED_FACE('',(#10830),#2156,.T.) ;
#46049=ADVANCED_FACE('',(#10831),#2157,.T.) ;
#46050=ADVANCED_FACE('',(#10832),#45444,.T.) ;
#46051=ADVANCED_FACE('',(#10833),#2158,.T.) ;
#46052=ADVANCED_FACE('',(#10834),#2159,.T.) ;
#46053=ADVANCED_FACE('',(#10835),#1776,.F.) ;
#46054=ADVANCED_FACE('',(#10836),#2160,.T.) ;
#46055=ADVANCED_FACE('',(#10837),#2161,.T.) ;
#46056=ADVANCED_FACE('',(#10838),#45445,.T.) ;
#46057=ADVANCED_FACE('',(#10839),#2162,.T.) ;
#46058=ADVANCED_FACE('',(#10840),#2163,.T.) ;
#46059=ADVANCED_FACE('',(#10841),#1777,.F.) ;
#46060=ADVANCED_FACE('',(#10842),#2164,.T.) ;
#46061=ADVANCED_FACE('',(#10843),#2165,.T.) ;
#46062=ADVANCED_FACE('',(#10844),#45446,.T.) ;
#46063=ADVANCED_FACE('',(#10845),#2166,.T.) ;
#46064=ADVANCED_FACE('',(#10846),#1778,.F.) ;
#46065=ADVANCED_FACE('',(#10847),#45447,.T.) ;
#46066=ADVANCED_FACE('',(#10848),#9479,.T.) ;
#46067=ADVANCED_FACE('',(#10849),#9480,.T.) ;
#46068=ADVANCED_FACE('',(#10850),#1779,.F.) ;
#46069=ADVANCED_FACE('',(#10851),#9481,.T.) ;
#46070=ADVANCED_FACE('',(#10852),#45448,.T.) ;
#46071=ADVANCED_FACE('',(#10853),#9482,.T.) ;
#46072=ADVANCED_FACE('',(#10854),#45449,.T.) ;
#46073=ADVANCED_FACE('',(#10855),#9483,.T.) ;
#46074=ADVANCED_FACE('',(#10856),#45450,.T.) ;
#46075=ADVANCED_FACE('',(#10857),#9484,.T.) ;
#46076=ADVANCED_FACE('',(#10858),#45451,.T.) ;
#46077=ADVANCED_FACE('',(#10859),#1780,.F.) ;
#46078=ADVANCED_FACE('',(#10860),#9485,.T.) ;
#46079=ADVANCED_FACE('',(#10861),#9486,.T.) ;
#46080=ADVANCED_FACE('',(#10862),#45452,.T.) ;
#46081=ADVANCED_FACE('',(#10863),#9487,.T.) ;
#46082=ADVANCED_FACE('',(#10864),#45453,.T.) ;
#46083=ADVANCED_FACE('',(#10865),#9488,.T.) ;
#46084=ADVANCED_FACE('',(#10866),#45454,.T.) ;
#46085=ADVANCED_FACE('',(#10867),#1781,.F.) ;
#46086=ADVANCED_FACE('',(#10868),#9489,.T.) ;
#46087=ADVANCED_FACE('',(#10869),#9490,.T.) ;
#46088=ADVANCED_FACE('',(#10870),#45455,.T.) ;
#46089=ADVANCED_FACE('',(#10871),#9491,.T.) ;
#46090=ADVANCED_FACE('',(#10872),#45456,.T.) ;
#46091=ADVANCED_FACE('',(#10873),#9492,.T.) ;
#46092=ADVANCED_FACE('',(#10874),#45457,.T.) ;
#46093=ADVANCED_FACE('',(#10875),#1782,.F.) ;
#46094=ADVANCED_FACE('',(#10876),#9493,.T.) ;
#46095=ADVANCED_FACE('',(#10877),#9494,.T.) ;
#46096=ADVANCED_FACE('',(#10878),#45458,.T.) ;
#46097=ADVANCED_FACE('',(#10879),#9495,.T.) ;
#46098=ADVANCED_FACE('',(#10880),#45459,.T.) ;
#46099=ADVANCED_FACE('',(#10881),#9496,.T.) ;
#46100=ADVANCED_FACE('',(#10882),#45460,.T.) ;
#46101=ADVANCED_FACE('',(#10883),#1783,.F.) ;
#46102=ADVANCED_FACE('',(#10884),#9497,.T.) ;
#46103=ADVANCED_FACE('',(#10885),#9498,.T.) ;
#46104=ADVANCED_FACE('',(#10886),#45461,.T.) ;
#46105=ADVANCED_FACE('',(#10887),#9499,.T.) ;
#46106=ADVANCED_FACE('',(#10888),#45462,.T.) ;
#46107=ADVANCED_FACE('',(#10889),#9500,.T.) ;
#46108=ADVANCED_FACE('',(#10890),#45463,.T.) ;
#46109=ADVANCED_FACE('',(#10891),#1784,.F.) ;
#46110=ADVANCED_FACE('',(#10892),#9501,.T.) ;
#46111=ADVANCED_FACE('',(#10893),#9502,.T.) ;
#46112=ADVANCED_FACE('',(#10894),#45464,.T.) ;
#46113=ADVANCED_FACE('',(#10895),#9503,.T.) ;
#46114=ADVANCED_FACE('',(#10896),#45465,.T.) ;
#46115=ADVANCED_FACE('',(#10897),#9504,.T.) ;
#46116=ADVANCED_FACE('',(#10898),#45466,.T.) ;
#46117=ADVANCED_FACE('',(#10899),#1785,.F.) ;
#46118=ADVANCED_FACE('',(#10900),#9505,.T.) ;
#46119=ADVANCED_FACE('',(#10901),#9506,.T.) ;
#46120=ADVANCED_FACE('',(#10902),#45467,.T.) ;
#46121=ADVANCED_FACE('',(#10903),#9507,.T.) ;
#46122=ADVANCED_FACE('',(#10904),#45468,.T.) ;
#46123=ADVANCED_FACE('',(#10905),#9508,.T.) ;
#46124=ADVANCED_FACE('',(#10906),#45469,.T.) ;
#46125=ADVANCED_FACE('',(#10907),#1786,.F.) ;
#46126=ADVANCED_FACE('',(#10908),#9509,.T.) ;
#46127=ADVANCED_FACE('',(#10909),#9510,.T.) ;
#46128=ADVANCED_FACE('',(#10910),#45470,.T.) ;
#46129=ADVANCED_FACE('',(#10911),#9511,.T.) ;
#46130=ADVANCED_FACE('',(#10912),#45471,.T.) ;
#46131=ADVANCED_FACE('',(#10913),#9512,.T.) ;
#46132=ADVANCED_FACE('',(#10914),#45472,.T.) ;
#46133=ADVANCED_FACE('',(#10915),#1787,.F.) ;
#46134=ADVANCED_FACE('',(#10916),#9513,.T.) ;
#46135=ADVANCED_FACE('',(#10917),#9514,.T.) ;
#46136=ADVANCED_FACE('',(#10918),#45473,.T.) ;
#46137=ADVANCED_FACE('',(#10919),#9515,.T.) ;
#46138=ADVANCED_FACE('',(#10920),#45474,.T.) ;
#46139=ADVANCED_FACE('',(#10921),#9516,.T.) ;
#46140=ADVANCED_FACE('',(#10922),#45475,.T.) ;
#46141=ADVANCED_FACE('',(#10923),#1788,.F.) ;
#46142=ADVANCED_FACE('',(#10924),#9517,.T.) ;
#46143=ADVANCED_FACE('',(#10925),#9518,.T.) ;
#46144=ADVANCED_FACE('',(#10926),#45476,.T.) ;
#46145=ADVANCED_FACE('',(#10927),#9519,.F.) ;
#46146=ADVANCED_FACE('',(#10928),#9520,.F.) ;
#46147=ADVANCED_FACE('',(#10929),#9521,.F.) ;
#46148=ADVANCED_FACE('',(#10930),#9522,.F.) ;
#46149=ADVANCED_FACE('',(#10931),#9523,.F.) ;
#46150=ADVANCED_FACE('',(#10932),#9524,.F.) ;
#46151=ADVANCED_FACE('',(#10933),#9525,.F.) ;
#46152=ADVANCED_FACE('',(#10934),#9526,.F.) ;
#46153=ADVANCED_FACE('',(#10935),#9527,.F.) ;
#46154=ADVANCED_FACE('',(#10936),#9528,.F.) ;
#46155=ADVANCED_FACE('',(#10937),#9529,.F.) ;
#46156=ADVANCED_FACE('',(#10938),#9530,.F.) ;
#46157=ADVANCED_FACE('',(#10939),#9531,.F.) ;
#46158=ADVANCED_FACE('',(#10940),#9532,.F.) ;
#46159=ADVANCED_FACE('',(#10941),#9533,.F.) ;
#46160=ADVANCED_FACE('',(#10942),#9534,.F.) ;
#46161=ADVANCED_FACE('',(#10943),#9535,.F.) ;
#46162=ADVANCED_FACE('',(#10944),#9536,.F.) ;
#46163=ADVANCED_FACE('',(#10945),#9537,.F.) ;
#46164=ADVANCED_FACE('',(#10946),#9538,.F.) ;
#46165=ADVANCED_FACE('',(#10947),#773,.T.) ;
#46166=ADVANCED_FACE('',(#10948),#45477,.T.) ;
#46167=ADVANCED_FACE('',(#10949,#670),#2224,.T.) ;
#46168=ADVANCED_FACE('',(#10950),#9539,.T.) ;
#46169=ADVANCED_FACE('',(#10951),#2225,.F.) ;
#46170=ADVANCED_FACE('',(#10952),#45478,.T.) ;
#46171=ADVANCED_FACE('',(#10953),#9540,.T.) ;
#46172=ADVANCED_FACE('',(#10954),#45479,.T.) ;
#46173=ADVANCED_FACE('',(#10955),#9541,.T.) ;
#46174=ADVANCED_FACE('',(#10956),#9542,.T.) ;
#46175=ADVANCED_FACE('',(#10957),#2226,.F.) ;
#46176=ADVANCED_FACE('',(#10958),#45480,.T.) ;
#46177=ADVANCED_FACE('',(#10959),#9543,.T.) ;
#46178=ADVANCED_FACE('',(#10960),#9544,.T.) ;
#46179=ADVANCED_FACE('',(#10961),#45481,.T.) ;
#46180=ADVANCED_FACE('',(#10962),#45482,.T.) ;
#46181=ADVANCED_FACE('',(#10963),#45483,.T.) ;
#46182=ADVANCED_FACE('',(#10964),#9545,.T.) ;
#46183=ADVANCED_FACE('',(#10965),#45484,.T.) ;
#46184=ADVANCED_FACE('',(#10966),#9546,.T.) ;
#46185=ADVANCED_FACE('',(#10967),#9547,.T.) ;
#46186=ADVANCED_FACE('',(#10968),#45485,.T.) ;
#46187=ADVANCED_FACE('',(#10969),#45486,.T.) ;
#46188=ADVANCED_FACE('',(#10970),#9548,.F.) ;
#46189=ADVANCED_FACE('',(#10971),#45487,.T.) ;
#46190=ADVANCED_FACE('',(#10972),#9549,.T.) ;
#46191=ADVANCED_FACE('',(#10973),#9550,.F.) ;
#46192=ADVANCED_FACE('',(#10974),#45488,.T.) ;
#46193=ADVANCED_FACE('',(#10975),#9551,.T.) ;
#46194=ADVANCED_FACE('',(#10976),#45489,.T.) ;
#46195=ADVANCED_FACE('',(#10977),#9552,.F.) ;
#46196=ADVANCED_FACE('',(#10978),#9553,.T.) ;
#46197=ADVANCED_FACE('',(#10979),#9554,.F.) ;
#46198=ADVANCED_FACE('',(#10980),#9555,.T.) ;
#46199=ADVANCED_FACE('',(#10981),#9556,.T.) ;
#46200=ADVANCED_FACE('',(#10982),#2227,.T.) ;
#46201=ADVANCED_FACE('',(#10983),#2228,.T.) ;
#46202=ADVANCED_FACE('',(#10984),#2229,.T.) ;
#46203=ADVANCED_FACE('',(#10985),#2230,.T.) ;
#46204=ADVANCED_FACE('',(#10986),#2231,.T.) ;
#46205=ADVANCED_FACE('',(#10987),#2232,.T.) ;
#46206=ADVANCED_FACE('',(#10988),#2233,.T.) ;
#46207=ADVANCED_FACE('',(#10989),#2234,.T.) ;
#46208=ADVANCED_FACE('',(#10990),#2235,.T.) ;
#46209=ADVANCED_FACE('',(#10991),#2236,.T.) ;
#46210=ADVANCED_FACE('',(#10992),#2237,.T.) ;
#46211=ADVANCED_FACE('',(#10993),#2238,.T.) ;
#46212=ADVANCED_FACE('',(#10994),#2239,.T.) ;
#46213=ADVANCED_FACE('',(#10995),#2240,.T.) ;
#46214=ADVANCED_FACE('',(#10996),#2241,.T.) ;
#46215=ADVANCED_FACE('',(#10997),#2242,.T.) ;
#46216=ADVANCED_FACE('',(#10998),#2243,.T.) ;
#46217=ADVANCED_FACE('',(#10999),#2244,.T.) ;
#46218=ADVANCED_FACE('',(#11000),#2245,.T.) ;
#46219=ADVANCED_FACE('',(#11001),#2246,.T.) ;
#46220=ADVANCED_FACE('',(#11002),#2247,.F.) ;
#46221=ADVANCED_FACE('',(#11003),#2248,.F.) ;
#46222=ADVANCED_FACE('',(#11004),#2249,.F.) ;
#46223=ADVANCED_FACE('',(#11005),#2250,.F.) ;
#49057=CLOSED_SHELL('',(#45965,#45966,#45967,#45968,#45969,#45970,#45971,
#45972,#45973,#45974,#45975,#45976,#45977,#45978,#45979,#45980,#45981,#45982,
#45983,#45984,#45985,#45986,#45987,#45988,#45989,#45990,#45991,#45992,#45993,
#45994,#45995,#45996,#45997,#45998,#45999,#46000,#46001,#46002,#46003,#46004,
#46005,#46006,#46007,#46008,#46009,#46010,#46011,#46012,#46013,#46014,#46015,
#46016,#46017,#46018,#46019,#46020,#46021,#46022,#46023,#46024,#46025,#46026,
#46027,#46028,#46029,#46030,#46031,#46032,#46033,#46034,#46035,#46036,#46037,
#46038,#46039,#46040,#46041,#46042,#46043,#46044,#46045,#46046,#46047,#46048,
#46049,#46050,#46051,#46052,#46053,#46054,#46055,#46056,#46057,#46058,#46059,
#46060,#46061,#46062,#46063,#46064,#46065,#46066,#46067,#46068,#46069,#46070,
#46071,#46072,#46073,#46074,#46075,#46076,#46077,#46078,#46079,#46080,#46081,
#46082,#46083,#46084,#46085,#46086,#46087,#46088,#46089,#46090,#46091,#46092,
#46093,#46094,#46095,#46096,#46097,#46098,#46099,#46100,#46101,#46102,#46103,
#46104,#46105,#46106,#46107,#46108,#46109,#46110,#46111,#46112,#46113,#46114,
#46115,#46116,#46117,#46118,#46119,#46120,#46121,#46122,#46123,#46124,#46125,
#46126,#46127,#46128,#46129,#46130,#46131,#46132,#46133,#46134,#46135,#46136,
#46137,#46138,#46139,#46140,#46141,#46142,#46143,#46144,#46145,#46146,#46147,
#46148,#46149,#46150,#46151,#46152,#46153,#46154,#46155,#46156,#46157,#46158,
#46159,#46160,#46161,#46162,#46163,#46164,#46165,#46166,#46167,#46168,#46169,
#46170,#46171,#46172,#46173,#46174,#46175,#46176,#46177,#46178,#46179,#46180,
#46181,#46182,#46183,#46184,#46185,#46186,#46187,#46188,#46189,#46190,#46191,
#46192,#46193,#46194,#46195,#46196,#46197,#46198,#46199,#46200,#46201,#46202,
#46203,#46204,#46205,#46206,#46207,#46208,#46209,#46210,#46211,#46212,#46213,
#46214,#46215,#46216,#46217,#46218,#46219,#46220,#46221,#46222,#46223)) ;
#49311=AXIS2_PLACEMENT_3D('',#69886,#55099,#55100) ;
#49312=AXIS2_PLACEMENT_3D('',#69887,#55101,#55102) ;
#49313=AXIS2_PLACEMENT_3D('',#69889,#55103,#55104) ;
#49314=AXIS2_PLACEMENT_3D('',#69891,#55105,#55106) ;
#49315=AXIS2_PLACEMENT_3D('',#69892,#55107,#55108) ;
#49316=AXIS2_PLACEMENT_3D('',#69893,#55109,#55110) ;
#49317=AXIS2_PLACEMENT_3D('',#69897,#55112,#55113) ;
#49318=AXIS2_PLACEMENT_3D('',#69901,#55115,#55116) ;
#49319=AXIS2_PLACEMENT_3D('',#69905,#55118,#55119) ;
#49320=AXIS2_PLACEMENT_3D('',#69909,#55121,#55122) ;
#49321=AXIS2_PLACEMENT_3D('',#69913,#55124,#55125) ;
#49322=AXIS2_PLACEMENT_3D('',#69917,#55127,#55128) ;
#49323=AXIS2_PLACEMENT_3D('',#69921,#55130,#55131) ;
#49324=AXIS2_PLACEMENT_3D('',#69925,#55133,#55134) ;
#49325=AXIS2_PLACEMENT_3D('',#69929,#55136,#55137) ;
#49326=AXIS2_PLACEMENT_3D('',#69933,#55139,#55140) ;
#49327=AXIS2_PLACEMENT_3D('',#69937,#55142,#55143) ;
#49328=AXIS2_PLACEMENT_3D('',#69941,#55145,#55146) ;
#49329=AXIS2_PLACEMENT_3D('',#69945,#55148,#55149) ;
#49330=AXIS2_PLACEMENT_3D('',#69949,#55151,#55152) ;
#49331=AXIS2_PLACEMENT_3D('',#69953,#55154,#55155) ;
#49332=AXIS2_PLACEMENT_3D('',#69957,#55157,#55158) ;
#49333=AXIS2_PLACEMENT_3D('',#69961,#55160,#55161) ;
#49334=AXIS2_PLACEMENT_3D('',#69965,#55163,#55164) ;
#49335=AXIS2_PLACEMENT_3D('',#69969,#55166,#55167) ;
#49336=AXIS2_PLACEMENT_3D('',#69973,#55169,#55170) ;
#49337=AXIS2_PLACEMENT_3D('',#69977,#55172,#55173) ;
#49338=AXIS2_PLACEMENT_3D('',#69981,#55175,#55176) ;
#49339=AXIS2_PLACEMENT_3D('',#69985,#55178,#55179) ;
#49340=AXIS2_PLACEMENT_3D('',#69989,#55181,#55182) ;
#49341=AXIS2_PLACEMENT_3D('',#69993,#55184,#55185) ;
#49342=AXIS2_PLACEMENT_3D('',#69997,#55187,#55188) ;
#49343=AXIS2_PLACEMENT_3D('',#70001,#55190,#55191) ;
#49344=AXIS2_PLACEMENT_3D('',#70005,#55193,#55194) ;
#49345=AXIS2_PLACEMENT_3D('',#70009,#55196,#55197) ;
#49346=AXIS2_PLACEMENT_3D('',#70013,#55199,#55200) ;
#49347=AXIS2_PLACEMENT_3D('',#70017,#55202,#55203) ;
#49348=AXIS2_PLACEMENT_3D('',#70021,#55205,#55206) ;
#49349=AXIS2_PLACEMENT_3D('',#70025,#55208,#55209) ;
#49350=AXIS2_PLACEMENT_3D('',#70029,#55211,#55212) ;
#49351=AXIS2_PLACEMENT_3D('',#70033,#55214,#55215) ;
#49352=AXIS2_PLACEMENT_3D('',#70037,#55217,#55218) ;
#49353=AXIS2_PLACEMENT_3D('',#70041,#55220,#55221) ;
#49354=AXIS2_PLACEMENT_3D('',#70045,#55223,#55224) ;
#49355=AXIS2_PLACEMENT_3D('',#70049,#55226,#55227) ;
#49356=AXIS2_PLACEMENT_3D('',#70053,#55229,#55230) ;
#49357=AXIS2_PLACEMENT_3D('',#70056,#55232,#55233) ;
#49358=AXIS2_PLACEMENT_3D('',#70057,#55234,#55235) ;
#49359=AXIS2_PLACEMENT_3D('',#70058,#55236,#55237) ;
#49360=AXIS2_PLACEMENT_3D('',#70061,#55238,#55239) ;
#49361=AXIS2_PLACEMENT_3D('',#70065,#55241,#55242) ;
#49362=AXIS2_PLACEMENT_3D('',#70067,#55244,#55245) ;
#49363=AXIS2_PLACEMENT_3D('',#70070,#55246,#55247) ;
#49364=AXIS2_PLACEMENT_3D('',#70074,#55249,#55250) ;
#49365=AXIS2_PLACEMENT_3D('',#70076,#55252,#55253) ;
#49366=AXIS2_PLACEMENT_3D('',#70079,#55254,#55255) ;
#49367=AXIS2_PLACEMENT_3D('',#70080,#55256,#55257) ;
#49368=AXIS2_PLACEMENT_3D('',#70081,#55258,#55259) ;
#49369=AXIS2_PLACEMENT_3D('',#70082,#55260,#55261) ;
#49370=AXIS2_PLACEMENT_3D('',#70084,#55262,#55263) ;
#49371=AXIS2_PLACEMENT_3D('',#70087,#55266,#55267) ;
#49372=AXIS2_PLACEMENT_3D('',#70090,#55268,#55269) ;
#49373=AXIS2_PLACEMENT_3D('',#70093,#55271,#55272) ;
#49374=AXIS2_PLACEMENT_3D('',#70095,#55274,#55275) ;
#49375=AXIS2_PLACEMENT_3D('',#70098,#55276,#55277) ;
#49376=AXIS2_PLACEMENT_3D('',#70102,#55279,#55280) ;
#49377=AXIS2_PLACEMENT_3D('',#70104,#55282,#55283) ;
#49378=AXIS2_PLACEMENT_3D('',#70107,#55284,#55285) ;
#49379=AXIS2_PLACEMENT_3D('',#70108,#55286,#55287) ;
#49380=AXIS2_PLACEMENT_3D('',#70109,#55288,#55289) ;
#49381=AXIS2_PLACEMENT_3D('',#70110,#55290,#55291) ;
#49382=AXIS2_PLACEMENT_3D('',#70112,#55292,#55293) ;
#49383=AXIS2_PLACEMENT_3D('',#70115,#55296,#55297) ;
#49384=AXIS2_PLACEMENT_3D('',#70118,#55298,#55299) ;
#49385=AXIS2_PLACEMENT_3D('',#70121,#55301,#55302) ;
#49386=AXIS2_PLACEMENT_3D('',#70123,#55304,#55305) ;
#49387=AXIS2_PLACEMENT_3D('',#70126,#55306,#55307) ;
#49388=AXIS2_PLACEMENT_3D('',#70130,#55309,#55310) ;
#49389=AXIS2_PLACEMENT_3D('',#70132,#55312,#55313) ;
#49390=AXIS2_PLACEMENT_3D('',#70135,#55314,#55315) ;
#49391=AXIS2_PLACEMENT_3D('',#70136,#55316,#55317) ;
#49392=AXIS2_PLACEMENT_3D('',#70137,#55318,#55319) ;
#49393=AXIS2_PLACEMENT_3D('',#70138,#55320,#55321) ;
#49394=AXIS2_PLACEMENT_3D('',#70140,#55322,#55323) ;
#49395=AXIS2_PLACEMENT_3D('',#70143,#55326,#55327) ;
#49396=AXIS2_PLACEMENT_3D('',#70146,#55328,#55329) ;
#49397=AXIS2_PLACEMENT_3D('',#70149,#55331,#55332) ;
#49398=AXIS2_PLACEMENT_3D('',#70151,#55334,#55335) ;
#49399=AXIS2_PLACEMENT_3D('',#70154,#55336,#55337) ;
#49400=AXIS2_PLACEMENT_3D('',#70156,#55338,#55339) ;
#49401=AXIS2_PLACEMENT_3D('',#70158,#55340,#55341) ;
#49402=AXIS2_PLACEMENT_3D('',#70159,#55342,#55343) ;
#49403=AXIS2_PLACEMENT_3D('',#70160,#55344,#55345) ;
#49404=AXIS2_PLACEMENT_3D('',#70162,#55346,#55347) ;
#49405=AXIS2_PLACEMENT_3D('',#70165,#55350,#55351) ;
#49406=AXIS2_PLACEMENT_3D('',#70167,#55352,#55353) ;
#49407=AXIS2_PLACEMENT_3D('',#70170,#55356,#55357) ;
#49408=AXIS2_PLACEMENT_3D('',#70171,#55358,#55359) ;
#49409=AXIS2_PLACEMENT_3D('',#70172,#55360,#55361) ;
#49410=AXIS2_PLACEMENT_3D('',#70173,#55362,#55363) ;
#49411=AXIS2_PLACEMENT_3D('',#70174,#55364,#55365) ;
#49412=AXIS2_PLACEMENT_3D('',#70175,#55366,#55367) ;
#49413=AXIS2_PLACEMENT_3D('',#70176,#55368,#55369) ;
#49414=AXIS2_PLACEMENT_3D('',#70177,#55370,#55371) ;
#49415=AXIS2_PLACEMENT_3D('',#70178,#55372,#55373) ;
#49416=AXIS2_PLACEMENT_3D('',#70179,#55374,#55375) ;
#49417=AXIS2_PLACEMENT_3D('',#70180,#55376,#55377) ;
#49418=AXIS2_PLACEMENT_3D('',#70181,#55378,#55379) ;
#49419=AXIS2_PLACEMENT_3D('',#70182,#55380,#55381) ;
#49420=AXIS2_PLACEMENT_3D('',#70183,#55382,#55383) ;
#49421=AXIS2_PLACEMENT_3D('',#70184,#55384,#55385) ;
#49422=AXIS2_PLACEMENT_3D('',#70185,#55386,#55387) ;
#49423=AXIS2_PLACEMENT_3D('',#70186,#55388,#55389) ;
#49424=AXIS2_PLACEMENT_3D('',#70192,#55393,#55394) ;
#49425=AXIS2_PLACEMENT_3D('',#70195,#55396,#55397) ;
#49426=AXIS2_PLACEMENT_3D('',#70196,#55398,#55399) ;
#49427=AXIS2_PLACEMENT_3D('',#70200,#55402,#55403) ;
#49428=AXIS2_PLACEMENT_3D('',#70203,#55405,#55406) ;
#49429=AXIS2_PLACEMENT_3D('',#70204,#55407,#55408) ;
#49430=AXIS2_PLACEMENT_3D('',#70208,#55411,#55412) ;
#49431=AXIS2_PLACEMENT_3D('',#70211,#55414,#55415) ;
#49432=AXIS2_PLACEMENT_3D('',#70212,#55416,#55417) ;
#49433=AXIS2_PLACEMENT_3D('',#70216,#55420,#55421) ;
#49434=AXIS2_PLACEMENT_3D('',#70219,#55423,#55424) ;
#49435=AXIS2_PLACEMENT_3D('',#70220,#55425,#55426) ;
#49436=AXIS2_PLACEMENT_3D('',#70224,#55429,#55430) ;
#49437=AXIS2_PLACEMENT_3D('',#70227,#55432,#55433) ;
#49438=AXIS2_PLACEMENT_3D('',#70228,#55434,#55435) ;
#49439=AXIS2_PLACEMENT_3D('',#70232,#55438,#55439) ;
#49440=AXIS2_PLACEMENT_3D('',#70235,#55441,#55442) ;
#49441=AXIS2_PLACEMENT_3D('',#70236,#55443,#55444) ;
#49442=AXIS2_PLACEMENT_3D('',#70237,#55445,#55446) ;
#49443=AXIS2_PLACEMENT_3D('',#70239,#55447,#55448) ;
#49444=AXIS2_PLACEMENT_3D('',#70241,#55449,#55450) ;
#49445=AXIS2_PLACEMENT_3D('',#70242,#55451,#55452) ;
#49446=AXIS2_PLACEMENT_3D('',#70243,#55453,#55454) ;
#49447=AXIS2_PLACEMENT_3D('',#70245,#55455,#55456) ;
#49448=AXIS2_PLACEMENT_3D('',#70247,#55457,#55458) ;
#49449=AXIS2_PLACEMENT_3D('',#70248,#55459,#55460) ;
#49450=AXIS2_PLACEMENT_3D('',#70249,#55461,#55462) ;
#49451=AXIS2_PLACEMENT_3D('',#70251,#55463,#55464) ;
#49452=AXIS2_PLACEMENT_3D('',#70253,#55465,#55466) ;
#49453=AXIS2_PLACEMENT_3D('',#70254,#55467,#55468) ;
#49454=AXIS2_PLACEMENT_3D('',#70255,#55469,#55470) ;
#49455=AXIS2_PLACEMENT_3D('',#70256,#55471,#55472) ;
#49456=AXIS2_PLACEMENT_3D('',#70257,#55473,#55474) ;
#49457=AXIS2_PLACEMENT_3D('',#70259,#55475,#55476) ;
#49458=AXIS2_PLACEMENT_3D('',#70261,#55477,#55478) ;
#49459=AXIS2_PLACEMENT_3D('',#70262,#55479,#55480) ;
#49460=AXIS2_PLACEMENT_3D('',#70263,#55481,#55482) ;
#49461=AXIS2_PLACEMENT_3D('',#70265,#55483,#55484) ;
#49462=AXIS2_PLACEMENT_3D('',#70267,#55485,#55486) ;
#49463=AXIS2_PLACEMENT_3D('',#70268,#55487,#55488) ;
#49464=AXIS2_PLACEMENT_3D('',#70535,#55489,#55490) ;
#49465=AXIS2_PLACEMENT_3D('',#70537,#55491,#55492) ;
#49466=AXIS2_PLACEMENT_3D('',#70539,#55493,#55494) ;
#49467=AXIS2_PLACEMENT_3D('',#70540,#55495,#55496) ;
#49468=AXIS2_PLACEMENT_3D('',#70541,#55497,#55498) ;
#49469=AXIS2_PLACEMENT_3D('',#70543,#55499,#55500) ;
#49470=AXIS2_PLACEMENT_3D('',#70545,#55501,#55502) ;
#49471=AXIS2_PLACEMENT_3D('',#70546,#55503,#55504) ;
#49472=AXIS2_PLACEMENT_3D('',#70547,#55505,#55506) ;
#49473=AXIS2_PLACEMENT_3D('',#70548,#55507,#55508) ;
#49474=AXIS2_PLACEMENT_3D('',#70549,#55509,#55510) ;
#49475=AXIS2_PLACEMENT_3D('',#70551,#55511,#55512) ;
#49476=AXIS2_PLACEMENT_3D('',#70553,#55513,#55514) ;
#49477=AXIS2_PLACEMENT_3D('',#70554,#55515,#55516) ;
#49478=AXIS2_PLACEMENT_3D('',#70555,#55517,#55518) ;
#49479=AXIS2_PLACEMENT_3D('',#70557,#55519,#55520) ;
#49480=AXIS2_PLACEMENT_3D('',#70559,#55521,#55522) ;
#49481=AXIS2_PLACEMENT_3D('',#70560,#55523,#55524) ;
#49482=AXIS2_PLACEMENT_3D('',#70754,#55525,#55526) ;
#49483=AXIS2_PLACEMENT_3D('',#70756,#55527,#55528) ;
#49484=AXIS2_PLACEMENT_3D('',#70758,#55529,#55530) ;
#49485=AXIS2_PLACEMENT_3D('',#70759,#55531,#55532) ;
#49486=AXIS2_PLACEMENT_3D('',#70760,#55533,#55534) ;
#49487=AXIS2_PLACEMENT_3D('',#70762,#55535,#55536) ;
#49488=AXIS2_PLACEMENT_3D('',#70764,#55537,#55538) ;
#49489=AXIS2_PLACEMENT_3D('',#70765,#55539,#55540) ;
#49490=AXIS2_PLACEMENT_3D('',#70766,#55541,#55542) ;
#49491=AXIS2_PLACEMENT_3D('',#70767,#55543,#55544) ;
#49492=AXIS2_PLACEMENT_3D('',#70768,#55545,#55546) ;
#49493=AXIS2_PLACEMENT_3D('',#70770,#55547,#55548) ;
#49494=AXIS2_PLACEMENT_3D('',#70772,#55549,#55550) ;
#49495=AXIS2_PLACEMENT_3D('',#70773,#55551,#55552) ;
#49496=AXIS2_PLACEMENT_3D('',#70774,#55553,#55554) ;
#49497=AXIS2_PLACEMENT_3D('',#70776,#55555,#55556) ;
#49498=AXIS2_PLACEMENT_3D('',#70778,#55557,#55558) ;
#49499=AXIS2_PLACEMENT_3D('',#70779,#55559,#55560) ;
#49500=AXIS2_PLACEMENT_3D('',#70973,#55561,#55562) ;
#49501=AXIS2_PLACEMENT_3D('',#70975,#55563,#55564) ;
#49502=AXIS2_PLACEMENT_3D('',#70977,#55565,#55566) ;
#49503=AXIS2_PLACEMENT_3D('',#70978,#55567,#55568) ;
#49504=AXIS2_PLACEMENT_3D('',#70979,#55569,#55570) ;
#49505=AXIS2_PLACEMENT_3D('',#70981,#55571,#55572) ;
#49506=AXIS2_PLACEMENT_3D('',#70983,#55573,#55574) ;
#49507=AXIS2_PLACEMENT_3D('',#70984,#55575,#55576) ;
#49508=AXIS2_PLACEMENT_3D('',#70985,#55577,#55578) ;
#49509=AXIS2_PLACEMENT_3D('',#70986,#55579,#55580) ;
#49510=AXIS2_PLACEMENT_3D('',#70987,#55581,#55582) ;
#49511=AXIS2_PLACEMENT_3D('',#70989,#55583,#55584) ;
#49512=AXIS2_PLACEMENT_3D('',#70991,#55585,#55586) ;
#49513=AXIS2_PLACEMENT_3D('',#70992,#55587,#55588) ;
#49514=AXIS2_PLACEMENT_3D('',#70993,#55589,#55590) ;
#49515=AXIS2_PLACEMENT_3D('',#70995,#55591,#55592) ;
#49516=AXIS2_PLACEMENT_3D('',#70997,#55593,#55594) ;
#49517=AXIS2_PLACEMENT_3D('',#70998,#55595,#55596) ;
#49518=AXIS2_PLACEMENT_3D('',#71197,#55597,#55598) ;
#49519=AXIS2_PLACEMENT_3D('',#71199,#55599,#55600) ;
#49520=AXIS2_PLACEMENT_3D('',#71201,#55601,#55602) ;
#49521=AXIS2_PLACEMENT_3D('',#71202,#55603,#55604) ;
#49522=AXIS2_PLACEMENT_3D('',#71203,#55605,#55606) ;
#49523=AXIS2_PLACEMENT_3D('',#71205,#55607,#55608) ;
#49524=AXIS2_PLACEMENT_3D('',#71207,#55609,#55610) ;
#49525=AXIS2_PLACEMENT_3D('',#71208,#55611,#55612) ;
#49526=AXIS2_PLACEMENT_3D('',#71209,#55613,#55614) ;
#49527=AXIS2_PLACEMENT_3D('',#71210,#55615,#55616) ;
#49528=AXIS2_PLACEMENT_3D('',#71211,#55617,#55618) ;
#49529=AXIS2_PLACEMENT_3D('',#71213,#55619,#55620) ;
#49530=AXIS2_PLACEMENT_3D('',#71215,#55621,#55622) ;
#49531=AXIS2_PLACEMENT_3D('',#71216,#55623,#55624) ;
#49532=AXIS2_PLACEMENT_3D('',#71217,#55625,#55626) ;
#49533=AXIS2_PLACEMENT_3D('',#71219,#55627,#55628) ;
#49534=AXIS2_PLACEMENT_3D('',#71221,#55629,#55630) ;
#49535=AXIS2_PLACEMENT_3D('',#71222,#55631,#55632) ;
#49536=AXIS2_PLACEMENT_3D('',#71425,#55633,#55634) ;
#49537=AXIS2_PLACEMENT_3D('',#71427,#55635,#55636) ;
#49538=AXIS2_PLACEMENT_3D('',#71429,#55637,#55638) ;
#49539=AXIS2_PLACEMENT_3D('',#71430,#55639,#55640) ;
#49540=AXIS2_PLACEMENT_3D('',#71431,#55641,#55642) ;
#49541=AXIS2_PLACEMENT_3D('',#71433,#55643,#55644) ;
#49542=AXIS2_PLACEMENT_3D('',#71435,#55645,#55646) ;
#49543=AXIS2_PLACEMENT_3D('',#71436,#55647,#55648) ;
#49544=AXIS2_PLACEMENT_3D('',#71437,#55649,#55650) ;
#49545=AXIS2_PLACEMENT_3D('',#71438,#55651,#55652) ;
#49546=AXIS2_PLACEMENT_3D('',#71439,#55653,#55654) ;
#49547=AXIS2_PLACEMENT_3D('',#71441,#55655,#55656) ;
#49548=AXIS2_PLACEMENT_3D('',#71443,#55657,#55658) ;
#49549=AXIS2_PLACEMENT_3D('',#71444,#55659,#55660) ;
#49550=AXIS2_PLACEMENT_3D('',#71445,#55661,#55662) ;
#49551=AXIS2_PLACEMENT_3D('',#71447,#55663,#55664) ;
#49552=AXIS2_PLACEMENT_3D('',#71449,#55665,#55666) ;
#49553=AXIS2_PLACEMENT_3D('',#71450,#55667,#55668) ;
#49554=AXIS2_PLACEMENT_3D('',#71644,#55669,#55670) ;
#49555=AXIS2_PLACEMENT_3D('',#71646,#55671,#55672) ;
#49556=AXIS2_PLACEMENT_3D('',#71648,#55673,#55674) ;
#49557=AXIS2_PLACEMENT_3D('',#71649,#55675,#55676) ;
#49558=AXIS2_PLACEMENT_3D('',#71650,#55677,#55678) ;
#49559=AXIS2_PLACEMENT_3D('',#71652,#55679,#55680) ;
#49560=AXIS2_PLACEMENT_3D('',#71654,#55681,#55682) ;
#49561=AXIS2_PLACEMENT_3D('',#71655,#55683,#55684) ;
#49562=AXIS2_PLACEMENT_3D('',#71656,#55685,#55686) ;
#49563=AXIS2_PLACEMENT_3D('',#71657,#55687,#55688) ;
#49564=AXIS2_PLACEMENT_3D('',#71658,#55689,#55690) ;
#49565=AXIS2_PLACEMENT_3D('',#71660,#55691,#55692) ;
#49566=AXIS2_PLACEMENT_3D('',#71662,#55693,#55694) ;
#49567=AXIS2_PLACEMENT_3D('',#71663,#55695,#55696) ;
#49568=AXIS2_PLACEMENT_3D('',#71664,#55697,#55698) ;
#49569=AXIS2_PLACEMENT_3D('',#71666,#55699,#55700) ;
#49570=AXIS2_PLACEMENT_3D('',#71668,#55701,#55702) ;
#49571=AXIS2_PLACEMENT_3D('',#71669,#55703,#55704) ;
#49572=AXIS2_PLACEMENT_3D('',#71863,#55705,#55706) ;
#49573=AXIS2_PLACEMENT_3D('',#71865,#55707,#55708) ;
#49574=AXIS2_PLACEMENT_3D('',#71867,#55709,#55710) ;
#49575=AXIS2_PLACEMENT_3D('',#71868,#55711,#55712) ;
#49576=AXIS2_PLACEMENT_3D('',#71869,#55713,#55714) ;
#49577=AXIS2_PLACEMENT_3D('',#71871,#55715,#55716) ;
#49578=AXIS2_PLACEMENT_3D('',#71873,#55717,#55718) ;
#49579=AXIS2_PLACEMENT_3D('',#71874,#55719,#55720) ;
#49580=AXIS2_PLACEMENT_3D('',#71875,#55721,#55722) ;
#49581=AXIS2_PLACEMENT_3D('',#71876,#55723,#55724) ;
#49582=AXIS2_PLACEMENT_3D('',#71877,#55725,#55726) ;
#49583=AXIS2_PLACEMENT_3D('',#71879,#55727,#55728) ;
#49584=AXIS2_PLACEMENT_3D('',#71881,#55729,#55730) ;
#49585=AXIS2_PLACEMENT_3D('',#71882,#55731,#55732) ;
#49586=AXIS2_PLACEMENT_3D('',#71883,#55733,#55734) ;
#49587=AXIS2_PLACEMENT_3D('',#71885,#55735,#55736) ;
#49588=AXIS2_PLACEMENT_3D('',#71887,#55737,#55738) ;
#49589=AXIS2_PLACEMENT_3D('',#71888,#55739,#55740) ;
#49590=AXIS2_PLACEMENT_3D('',#72070,#55741,#55742) ;
#49591=AXIS2_PLACEMENT_3D('',#72072,#55743,#55744) ;
#49592=AXIS2_PLACEMENT_3D('',#72074,#55745,#55746) ;
#49593=AXIS2_PLACEMENT_3D('',#72075,#55747,#55748) ;
#49594=AXIS2_PLACEMENT_3D('',#72076,#55749,#55750) ;
#49595=AXIS2_PLACEMENT_3D('',#72078,#55751,#55752) ;
#49596=AXIS2_PLACEMENT_3D('',#72080,#55753,#55754) ;
#49597=AXIS2_PLACEMENT_3D('',#72081,#55755,#55756) ;
#49598=AXIS2_PLACEMENT_3D('',#72082,#55757,#55758) ;
#49599=AXIS2_PLACEMENT_3D('',#72083,#55759,#55760) ;
#49600=AXIS2_PLACEMENT_3D('',#72084,#55761,#55762) ;
#49601=AXIS2_PLACEMENT_3D('',#72086,#55763,#55764) ;
#49602=AXIS2_PLACEMENT_3D('',#72088,#55765,#55766) ;
#49603=AXIS2_PLACEMENT_3D('',#72089,#55767,#55768) ;
#49604=AXIS2_PLACEMENT_3D('',#72090,#55769,#55770) ;
#49605=AXIS2_PLACEMENT_3D('',#72092,#55771,#55772) ;
#49606=AXIS2_PLACEMENT_3D('',#72094,#55773,#55774) ;
#49607=AXIS2_PLACEMENT_3D('',#72095,#55775,#55776) ;
#49608=AXIS2_PLACEMENT_3D('',#72201,#55777,#55778) ;
#49609=AXIS2_PLACEMENT_3D('',#72203,#55779,#55780) ;
#49610=AXIS2_PLACEMENT_3D('',#72205,#55781,#55782) ;
#49611=AXIS2_PLACEMENT_3D('',#72206,#55783,#55784) ;
#49612=AXIS2_PLACEMENT_3D('',#72207,#55785,#55786) ;
#49613=AXIS2_PLACEMENT_3D('',#72209,#55787,#55788) ;
#49614=AXIS2_PLACEMENT_3D('',#72211,#55789,#55790) ;
#49615=AXIS2_PLACEMENT_3D('',#72212,#55791,#55792) ;
#49616=AXIS2_PLACEMENT_3D('',#72213,#55793,#55794) ;
#49617=AXIS2_PLACEMENT_3D('',#72214,#55795,#55796) ;
#49618=AXIS2_PLACEMENT_3D('',#72215,#55797,#55798) ;
#49619=AXIS2_PLACEMENT_3D('',#72217,#55799,#55800) ;
#49620=AXIS2_PLACEMENT_3D('',#72219,#55801,#55802) ;
#49621=AXIS2_PLACEMENT_3D('',#72220,#55803,#55804) ;
#49622=AXIS2_PLACEMENT_3D('',#72399,#55805,#55806) ;
#49623=AXIS2_PLACEMENT_3D('',#72400,#55807,#55808) ;
#49624=AXIS2_PLACEMENT_3D('',#72401,#55809,#55810) ;
#49625=AXIS2_PLACEMENT_3D('',#72418,#55812,#55813) ;
#49626=AXIS2_PLACEMENT_3D('',#72629,#55815,#55816) ;
#49627=AXIS2_PLACEMENT_3D('',#72644,#55818,#55819) ;
#49628=AXIS2_PLACEMENT_3D('',#72653,#55820,#55821) ;
#49629=AXIS2_PLACEMENT_3D('',#72660,#55822,#55823) ;
#49630=AXIS2_PLACEMENT_3D('',#72677,#55825,#55826) ;
#49631=AXIS2_PLACEMENT_3D('',#72678,#55827,#55828) ;
#49632=AXIS2_PLACEMENT_3D('',#72679,#55829,#55830) ;
#49633=AXIS2_PLACEMENT_3D('',#72696,#55832,#55833) ;
#49634=AXIS2_PLACEMENT_3D('',#72705,#55834,#55835) ;
#49635=AXIS2_PLACEMENT_3D('',#72712,#55836,#55837) ;
#49636=AXIS2_PLACEMENT_3D('',#72727,#55839,#55840) ;
#49637=AXIS2_PLACEMENT_3D('',#72736,#55841,#55842) ;
#49638=AXIS2_PLACEMENT_3D('',#72939,#55843,#55844) ;
#49639=AXIS2_PLACEMENT_3D('',#72954,#55846,#55847) ;
#49640=AXIS2_PLACEMENT_3D('',#72971,#55849,#55850) ;
#49641=AXIS2_PLACEMENT_3D('',#72972,#55851,#55852) ;
#49642=AXIS2_PLACEMENT_3D('',#72973,#55853,#55854) ;
#49643=AXIS2_PLACEMENT_3D('',#72990,#55856,#55857) ;
#49644=AXIS2_PLACEMENT_3D('',#72999,#55858,#55859) ;
#49645=AXIS2_PLACEMENT_3D('',#73006,#55860,#55861) ;
#49646=AXIS2_PLACEMENT_3D('',#73021,#55863,#55864) ;
#49647=AXIS2_PLACEMENT_3D('',#73030,#55865,#55866) ;
#49648=AXIS2_PLACEMENT_3D('',#73230,#55867,#55868) ;
#49649=AXIS2_PLACEMENT_3D('',#73245,#55870,#55871) ;
#49650=AXIS2_PLACEMENT_3D('',#73262,#55873,#55874) ;
#49651=AXIS2_PLACEMENT_3D('',#73263,#55875,#55876) ;
#49652=AXIS2_PLACEMENT_3D('',#73264,#55877,#55878) ;
#49653=AXIS2_PLACEMENT_3D('',#73281,#55880,#55881) ;
#49654=AXIS2_PLACEMENT_3D('',#73290,#55882,#55883) ;
#49655=AXIS2_PLACEMENT_3D('',#73297,#55884,#55885) ;
#49656=AXIS2_PLACEMENT_3D('',#73312,#55887,#55888) ;
#49657=AXIS2_PLACEMENT_3D('',#73321,#55889,#55890) ;
#49658=AXIS2_PLACEMENT_3D('',#73433,#55891,#55892) ;
#49659=AXIS2_PLACEMENT_3D('',#73448,#55894,#55895) ;
#49660=AXIS2_PLACEMENT_3D('',#73465,#55897,#55898) ;
#49661=AXIS2_PLACEMENT_3D('',#73466,#55899,#55900) ;
#49662=AXIS2_PLACEMENT_3D('',#73467,#55901,#55902) ;
#49663=AXIS2_PLACEMENT_3D('',#73484,#55904,#55905) ;
#49664=AXIS2_PLACEMENT_3D('',#73493,#55906,#55907) ;
#49665=AXIS2_PLACEMENT_3D('',#73500,#55908,#55909) ;
#49666=AXIS2_PLACEMENT_3D('',#73515,#55911,#55912) ;
#49667=AXIS2_PLACEMENT_3D('',#73524,#55913,#55914) ;
#49668=AXIS2_PLACEMENT_3D('',#73709,#55915,#55916) ;
#49669=AXIS2_PLACEMENT_3D('',#73724,#55918,#55919) ;
#49670=AXIS2_PLACEMENT_3D('',#73741,#55921,#55922) ;
#49671=AXIS2_PLACEMENT_3D('',#73742,#55923,#55924) ;
#49672=AXIS2_PLACEMENT_3D('',#73743,#55925,#55926) ;
#49673=AXIS2_PLACEMENT_3D('',#73760,#55928,#55929) ;
#49674=AXIS2_PLACEMENT_3D('',#73769,#55930,#55931) ;
#49675=AXIS2_PLACEMENT_3D('',#73776,#55932,#55933) ;
#49676=AXIS2_PLACEMENT_3D('',#73791,#55935,#55936) ;
#49677=AXIS2_PLACEMENT_3D('',#73800,#55937,#55938) ;
#49678=AXIS2_PLACEMENT_3D('',#74000,#55939,#55940) ;
#49679=AXIS2_PLACEMENT_3D('',#74015,#55942,#55943) ;
#49680=AXIS2_PLACEMENT_3D('',#74032,#55945,#55946) ;
#49681=AXIS2_PLACEMENT_3D('',#74033,#55947,#55948) ;
#49682=AXIS2_PLACEMENT_3D('',#74034,#55949,#55950) ;
#49683=AXIS2_PLACEMENT_3D('',#74051,#55952,#55953) ;
#49684=AXIS2_PLACEMENT_3D('',#74060,#55954,#55955) ;
#49685=AXIS2_PLACEMENT_3D('',#74067,#55956,#55957) ;
#49686=AXIS2_PLACEMENT_3D('',#74082,#55959,#55960) ;
#49687=AXIS2_PLACEMENT_3D('',#74091,#55961,#55962) ;
#49688=AXIS2_PLACEMENT_3D('',#74294,#55963,#55964) ;
#49689=AXIS2_PLACEMENT_3D('',#74309,#55966,#55967) ;
#49690=AXIS2_PLACEMENT_3D('',#74326,#55969,#55970) ;
#49691=AXIS2_PLACEMENT_3D('',#74327,#55971,#55972) ;
#49692=AXIS2_PLACEMENT_3D('',#74328,#55973,#55974) ;
#49693=AXIS2_PLACEMENT_3D('',#74345,#55976,#55977) ;
#49694=AXIS2_PLACEMENT_3D('',#74354,#55978,#55979) ;
#49695=AXIS2_PLACEMENT_3D('',#74361,#55980,#55981) ;
#49696=AXIS2_PLACEMENT_3D('',#74376,#55983,#55984) ;
#49697=AXIS2_PLACEMENT_3D('',#74385,#55985,#55986) ;
#49698=AXIS2_PLACEMENT_3D('',#74570,#55987,#55988) ;
#49699=AXIS2_PLACEMENT_3D('',#74585,#55990,#55991) ;
#49700=AXIS2_PLACEMENT_3D('',#74602,#55993,#55994) ;
#49701=AXIS2_PLACEMENT_3D('',#74603,#55995,#55996) ;
#49702=AXIS2_PLACEMENT_3D('',#74604,#55997,#55998) ;
#49703=AXIS2_PLACEMENT_3D('',#74621,#56000,#56001) ;
#49704=AXIS2_PLACEMENT_3D('',#74630,#56002,#56003) ;
#49705=AXIS2_PLACEMENT_3D('',#74637,#56004,#56005) ;
#49706=AXIS2_PLACEMENT_3D('',#74652,#56007,#56008) ;
#49707=AXIS2_PLACEMENT_3D('',#74661,#56009,#56010) ;
#49708=AXIS2_PLACEMENT_3D('',#74773,#56011,#56012) ;
#49709=AXIS2_PLACEMENT_3D('',#74788,#56014,#56015) ;
#49710=AXIS2_PLACEMENT_3D('',#74805,#56017,#56018) ;
#49711=AXIS2_PLACEMENT_3D('',#74806,#56019,#56020) ;
#49712=AXIS2_PLACEMENT_3D('',#74807,#56021,#56022) ;
#49713=AXIS2_PLACEMENT_3D('',#74824,#56024,#56025) ;
#49714=AXIS2_PLACEMENT_3D('',#74833,#56026,#56027) ;
#49715=AXIS2_PLACEMENT_3D('',#74840,#56028,#56029) ;
#49716=AXIS2_PLACEMENT_3D('',#74855,#56031,#56032) ;
#49717=AXIS2_PLACEMENT_3D('',#74864,#56033,#56034) ;
#49718=AXIS2_PLACEMENT_3D('',#75052,#56035,#56036) ;
#49719=AXIS2_PLACEMENT_3D('',#75067,#56038,#56039) ;
#49720=AXIS2_PLACEMENT_3D('',#75084,#56041,#56042) ;
#49721=AXIS2_PLACEMENT_3D('',#75093,#56043,#56044) ;
#49722=AXIS2_PLACEMENT_3D('',#75100,#56045,#56046) ;
#49723=AXIS2_PLACEMENT_3D('',#75101,#56047,#56048) ;
#49724=AXIS2_PLACEMENT_3D('',#75102,#56049,#56050) ;
#49725=AXIS2_PLACEMENT_3D('',#75103,#56051,#56052) ;
#49726=AXIS2_PLACEMENT_3D('',#75104,#56053,#56054) ;
#49727=AXIS2_PLACEMENT_3D('',#75105,#56055,#56056) ;
#49728=AXIS2_PLACEMENT_3D('',#75106,#56057,#56058) ;
#49729=AXIS2_PLACEMENT_3D('',#75107,#56059,#56060) ;
#49730=AXIS2_PLACEMENT_3D('',#75108,#56061,#56062) ;
#49731=AXIS2_PLACEMENT_3D('',#75109,#56063,#56064) ;
#49732=AXIS2_PLACEMENT_3D('',#75110,#56065,#56066) ;
#49733=AXIS2_PLACEMENT_3D('',#75111,#56067,#56068) ;
#49734=AXIS2_PLACEMENT_3D('',#75112,#56069,#56070) ;
#49735=AXIS2_PLACEMENT_3D('',#75113,#56071,#56072) ;
#49736=AXIS2_PLACEMENT_3D('',#75114,#56073,#56074) ;
#49737=AXIS2_PLACEMENT_3D('',#75115,#56075,#56076) ;
#49738=AXIS2_PLACEMENT_3D('',#75116,#56077,#56078) ;
#49739=AXIS2_PLACEMENT_3D('',#75117,#56079,#56080) ;
#49740=AXIS2_PLACEMENT_3D('',#75118,#56081,#56082) ;
#49741=AXIS2_PLACEMENT_3D('',#75119,#56083,#56084) ;
#49742=AXIS2_PLACEMENT_3D('',#75120,#56085,#56086) ;
#49743=AXIS2_PLACEMENT_3D('',#75121,#56087,#56088) ;
#49744=AXIS2_PLACEMENT_3D('',#75122,#56089,#56090) ;
#49745=AXIS2_PLACEMENT_3D('',#75123,#56091,#56092) ;
#49746=AXIS2_PLACEMENT_3D('',#75124,#56093,#56094) ;
#49747=AXIS2_PLACEMENT_3D('',#75125,#56095,#56096) ;
#49748=AXIS2_PLACEMENT_3D('',#75126,#56097,#56098) ;
#49749=AXIS2_PLACEMENT_3D('',#75127,#56099,#56100) ;
#49750=AXIS2_PLACEMENT_3D('',#75128,#56101,#56102) ;
#49751=AXIS2_PLACEMENT_3D('',#75129,#56103,#56104) ;
#49752=AXIS2_PLACEMENT_3D('',#75130,#56105,#56106) ;
#49753=AXIS2_PLACEMENT_3D('',#75131,#56107,#56108) ;
#49754=AXIS2_PLACEMENT_3D('',#75132,#56109,#56110) ;
#49755=AXIS2_PLACEMENT_3D('',#75133,#56111,#56112) ;
#49756=AXIS2_PLACEMENT_3D('',#75134,#56113,#56114) ;
#49757=AXIS2_PLACEMENT_3D('',#75135,#56115,#56116) ;
#49758=AXIS2_PLACEMENT_3D('',#75136,#56117,#56118) ;
#49759=AXIS2_PLACEMENT_3D('',#75137,#56119,#56120) ;
#49760=AXIS2_PLACEMENT_3D('',#75138,#56121,#56122) ;
#49761=AXIS2_PLACEMENT_3D('',#75139,#56123,#56124) ;
#49762=AXIS2_PLACEMENT_3D('',#75140,#56125,#56126) ;
#49763=AXIS2_PLACEMENT_3D('',#75143,#56128,#56129) ;
#49764=AXIS2_PLACEMENT_3D('',#75144,#56130,#56131) ;
#49765=AXIS2_PLACEMENT_3D('',#75146,#56132,#56133) ;
#49766=AXIS2_PLACEMENT_3D('',#75148,#56134,#56135) ;
#49767=AXIS2_PLACEMENT_3D('',#75149,#56136,#56137) ;
#49768=AXIS2_PLACEMENT_3D('',#75150,#56138,#56139) ;
#49769=AXIS2_PLACEMENT_3D('',#75152,#56140,#56141) ;
#49770=AXIS2_PLACEMENT_3D('',#75156,#56143,#56144) ;
#49771=AXIS2_PLACEMENT_3D('',#75160,#56146,#56147) ;
#49772=AXIS2_PLACEMENT_3D('',#75164,#56149,#56150) ;
#49773=AXIS2_PLACEMENT_3D('',#75168,#56152,#56153) ;
#49774=AXIS2_PLACEMENT_3D('',#75172,#56155,#56156) ;
#49775=AXIS2_PLACEMENT_3D('',#75176,#56158,#56159) ;
#49776=AXIS2_PLACEMENT_3D('',#75180,#56161,#56162) ;
#49777=AXIS2_PLACEMENT_3D('',#75184,#56164,#56165) ;
#49778=AXIS2_PLACEMENT_3D('',#75188,#56167,#56168) ;
#49779=AXIS2_PLACEMENT_3D('',#75192,#56170,#56171) ;
#49780=AXIS2_PLACEMENT_3D('',#75196,#56173,#56174) ;
#49781=AXIS2_PLACEMENT_3D('',#75198,#56176,#56177) ;
#49782=AXIS2_PLACEMENT_3D('',#75201,#56179,#56180) ;
#49783=AXIS2_PLACEMENT_3D('',#75202,#56181,#56182) ;
#49784=AXIS2_PLACEMENT_3D('',#75204,#56184,#56185) ;
#49785=AXIS2_PLACEMENT_3D('',#75205,#56186,#56187) ;
#49786=AXIS2_PLACEMENT_3D('',#75206,#56188,#56189) ;
#49787=AXIS2_PLACEMENT_3D('',#75207,#56190,#56191) ;
#49788=AXIS2_PLACEMENT_3D('',#75208,#56192,#56193) ;
#49789=AXIS2_PLACEMENT_3D('',#75209,#56194,#56195) ;
#49790=AXIS2_PLACEMENT_3D('',#75211,#56196,#56197) ;
#49791=AXIS2_PLACEMENT_3D('',#75213,#56198,#56199) ;
#49792=AXIS2_PLACEMENT_3D('',#75214,#56200,#56201) ;
#49793=AXIS2_PLACEMENT_3D('',#75215,#56202,#56203) ;
#49794=AXIS2_PLACEMENT_3D('',#75218,#56206,#56207) ;
#49795=AXIS2_PLACEMENT_3D('',#75221,#56209,#56210) ;
#49796=AXIS2_PLACEMENT_3D('',#75222,#56211,#56212) ;
#49797=AXIS2_PLACEMENT_3D('',#75224,#56214,#56215) ;
#49798=AXIS2_PLACEMENT_3D('',#75225,#56216,#56217) ;
#49799=AXIS2_PLACEMENT_3D('',#75227,#56218,#56219) ;
#49800=AXIS2_PLACEMENT_3D('',#75228,#56220,#56221) ;
#49801=AXIS2_PLACEMENT_3D('',#75229,#56222,#56223) ;
#49802=AXIS2_PLACEMENT_3D('',#75231,#56225,#56226) ;
#49803=AXIS2_PLACEMENT_3D('',#75232,#56227,#56228) ;
#49804=AXIS2_PLACEMENT_3D('',#75233,#56229,#56230) ;
#49805=AXIS2_PLACEMENT_3D('',#75234,#56231,#56232) ;
#49806=AXIS2_PLACEMENT_3D('',#75235,#56233,#56234) ;
#49807=AXIS2_PLACEMENT_3D('',#75236,#56235,#56236) ;
#49808=AXIS2_PLACEMENT_3D('',#75237,#56237,#56238) ;
#49809=AXIS2_PLACEMENT_3D('',#75238,#56239,#56240) ;
#49810=AXIS2_PLACEMENT_3D('',#75239,#56241,#56242) ;
#49811=AXIS2_PLACEMENT_3D('',#75240,#56243,#56244) ;
#49812=AXIS2_PLACEMENT_3D('',#75241,#56245,#56246) ;
#49813=AXIS2_PLACEMENT_3D('',#75242,#56247,#56248) ;
#49814=AXIS2_PLACEMENT_3D('',#75243,#56249,#56250) ;
#49815=AXIS2_PLACEMENT_3D('',#75244,#56251,#56252) ;
#49816=AXIS2_PLACEMENT_3D('',#75245,#56253,#56254) ;
#49817=AXIS2_PLACEMENT_3D('',#75246,#56255,#56256) ;
#49818=AXIS2_PLACEMENT_3D('',#75247,#56257,#56258) ;
#49819=AXIS2_PLACEMENT_3D('',#75248,#56259,#56260) ;
#49820=AXIS2_PLACEMENT_3D('',#75250,#56261,#56262) ;
#49821=AXIS2_PLACEMENT_3D('',#75251,#56263,#56264) ;
#49822=AXIS2_PLACEMENT_3D('',#75252,#56265,#56266) ;
#49823=AXIS2_PLACEMENT_3D('',#75254,#56268,#56269) ;
#49824=AXIS2_PLACEMENT_3D('',#75256,#56270,#56271) ;
#49825=AXIS2_PLACEMENT_3D('',#75258,#56272,#56273) ;
#49826=AXIS2_PLACEMENT_3D('',#75259,#56274,#56275) ;
#49827=AXIS2_PLACEMENT_3D('',#75260,#56276,#56277) ;
#49828=AXIS2_PLACEMENT_3D('',#75262,#56279,#56280) ;
#49829=AXIS2_PLACEMENT_3D('',#75265,#56283,#56284) ;
#49830=AXIS2_PLACEMENT_3D('',#75267,#56285,#56286) ;
#49831=AXIS2_PLACEMENT_3D('',#75269,#56287,#56288) ;
#49832=AXIS2_PLACEMENT_3D('',#75270,#56289,#56290) ;
#49833=AXIS2_PLACEMENT_3D('',#75271,#56291,#56292) ;
#49834=AXIS2_PLACEMENT_3D('',#75273,#56294,#56295) ;
#49835=AXIS2_PLACEMENT_3D('',#75275,#56296,#56297) ;
#49836=AXIS2_PLACEMENT_3D('',#75276,#56298,#56299) ;
#49837=AXIS2_PLACEMENT_3D('',#75277,#56300,#56301) ;
#49838=AXIS2_PLACEMENT_3D('',#75279,#56303,#56304) ;
#49839=AXIS2_PLACEMENT_3D('',#75281,#56306,#56307) ;
#49840=AXIS2_PLACEMENT_3D('',#75284,#56310,#56311) ;
#49841=AXIS2_PLACEMENT_3D('',#75286,#56313,#56314) ;
#49842=AXIS2_PLACEMENT_3D('',#75287,#56315,#56316) ;
#49843=AXIS2_PLACEMENT_3D('',#75288,#56317,#56318) ;
#49844=AXIS2_PLACEMENT_3D('',#75289,#56319,#56320) ;
#49845=AXIS2_PLACEMENT_3D('',#75290,#56321,#56322) ;
#49846=AXIS2_PLACEMENT_3D('',#75291,#56323,#56324) ;
#49847=AXIS2_PLACEMENT_3D('',#75292,#56325,#56326) ;
#49848=AXIS2_PLACEMENT_3D('',#75293,#56327,#56328) ;
#49849=AXIS2_PLACEMENT_3D('',#75294,#56329,#56330) ;
#49850=AXIS2_PLACEMENT_3D('',#75295,#56331,#56332) ;
#49851=AXIS2_PLACEMENT_3D('',#75296,#56333,#56334) ;
#49852=AXIS2_PLACEMENT_3D('',#75297,#56335,#56336) ;
#49853=AXIS2_PLACEMENT_3D('',#75298,#56337,#56338) ;
#49854=AXIS2_PLACEMENT_3D('',#75299,#56339,#56340) ;
#49855=AXIS2_PLACEMENT_3D('',#75300,#56341,#56342) ;
#49856=AXIS2_PLACEMENT_3D('',#75301,#56343,#56344) ;
#49857=AXIS2_PLACEMENT_3D('',#75302,#56345,#56346) ;
#49858=AXIS2_PLACEMENT_3D('',#75303,#56347,#56348) ;
#49859=AXIS2_PLACEMENT_3D('',#75304,#56349,#56350) ;
#49860=AXIS2_PLACEMENT_3D('',#75305,#56351,#56352) ;
#49861=AXIS2_PLACEMENT_3D('',#75306,#56353,#56354) ;
#49862=AXIS2_PLACEMENT_3D('',#75307,#56355,#56356) ;
#49863=AXIS2_PLACEMENT_3D('',#75308,#56357,#56358) ;
#49864=AXIS2_PLACEMENT_3D('',#75309,#56359,#56360) ;
#49865=AXIS2_PLACEMENT_3D('',#75310,#56361,#56362) ;
#55099=DIRECTION('axis',(0.,0.,1.)) ;
#55100=DIRECTION('refdir',(1.,0.,0.)) ;
#55101=DIRECTION('center_axis',(0.,0.,1.)) ;
#55102=DIRECTION('ref_axis',(1.,0.,0.)) ;
#55103=DIRECTION('center_axis',(0.,0.,-1.)) ;
#55104=DIRECTION('ref_axis',(1.,0.,0.)) ;
#55105=DIRECTION('center_axis',(0.,-1.,0.)) ;
#55106=DIRECTION('ref_axis',(-1.,0.,0.)) ;
#55107=DIRECTION('center_axis',(0.,0.,1.)) ;
#55108=DIRECTION('ref_axis',(1.,0.,0.)) ;
#55109=DIRECTION('center_axis',(0.,0.,1.)) ;
#55110=DIRECTION('ref_axis',(1.,0.,0.)) ;
#55111=DIRECTION('',(0.,0.,-1.)) ;
#55112=DIRECTION('center_axis',(0.,0.,-1.)) ;
#55113=DIRECTION('ref_axis',(-1.,-5.9211894646675E-15,0.)) ;
#55114=DIRECTION('',(0.,0.,1.)) ;
#55115=DIRECTION('center_axis',(0.,0.,-1.)) ;
#55116=DIRECTION('ref_axis',(-0.987688340595137,-0.156434465040233,0.)) ;
#55117=DIRECTION('',(0.,0.,-1.)) ;
#55118=DIRECTION('center_axis',(0.,0.,-1.)) ;
#55119=DIRECTION('ref_axis',(-0.951056516295152,-0.309016994374953,0.)) ;
#55120=DIRECTION('',(0.,0.,1.)) ;
#55121=DIRECTION('center_axis',(0.,0.,-1.)) ;
#55122=DIRECTION('ref_axis',(-0.89100652418837,-0.453990499739543,0.)) ;
#55123=DIRECTION('',(0.,0.,-1.)) ;
#55124=DIRECTION('center_axis',(0.,0.,-1.)) ;
#55125=DIRECTION('ref_axis',(-0.809016994374946,-0.587785252292475,0.)) ;
#55126=DIRECTION('',(0.,0.,1.)) ;
#55127=DIRECTION('center_axis',(0.,0.,-1.)) ;
#55128=DIRECTION('ref_axis',(-0.707106781186549,-0.707106781186546,0.)) ;
#55129=DIRECTION('',(0.,0.,-1.)) ;
#55130=DIRECTION('center_axis',(0.,0.,-1.)) ;
#55131=DIRECTION('ref_axis',(-0.587785252292474,-0.809016994374947,0.)) ;
#55132=DIRECTION('',(0.,0.,1.)) ;
#55133=DIRECTION('center_axis',(0.,0.,-1.)) ;
#55134=DIRECTION('ref_axis',(-0.453990499739548,-0.891006524188367,0.)) ;
#55135=DIRECTION('',(0.,0.,-1.)) ;
#55136=DIRECTION('center_axis',(0.,0.,-1.)) ;
#55137=DIRECTION('ref_axis',(-0.309016994374946,-0.951056516295154,0.)) ;
#55138=DIRECTION('',(0.,0.,1.)) ;
#55139=DIRECTION('center_axis',(0.,0.,-1.)) ;
#55140=DIRECTION('ref_axis',(-0.156434465040232,-0.987688340595138,0.)) ;
#55141=DIRECTION('',(0.,0.,-1.)) ;
#55142=DIRECTION('center_axis',(0.,0.,-1.)) ;
#55143=DIRECTION('ref_axis',(0.,-1.,0.)) ;
#55144=DIRECTION('',(0.,0.,1.)) ;
#55145=DIRECTION('center_axis',(0.,0.,-1.)) ;
#55146=DIRECTION('ref_axis',(0.156434465040235,-0.987688340595137,0.)) ;
#55147=DIRECTION('',(0.,0.,-1.)) ;
#55148=DIRECTION('center_axis',(0.,0.,-1.)) ;
#55149=DIRECTION('ref_axis',(0.309016994374953,-0.951056516295152,0.)) ;
#55150=DIRECTION('',(0.,0.,1.)) ;
#55151=DIRECTION('center_axis',(0.,0.,-1.)) ;
#55152=DIRECTION('ref_axis',(0.453990499739551,-0.891006524188366,0.)) ;
#55153=DIRECTION('',(0.,0.,-1.)) ;
#55154=DIRECTION('center_axis',(0.,0.,-1.)) ;
#55155=DIRECTION('ref_axis',(0.587785252292479,-0.809016994374943,0.)) ;
#55156=DIRECTION('',(0.,0.,1.)) ;
#55157=DIRECTION('center_axis',(0.,0.,-1.)) ;
#55158=DIRECTION('ref_axis',(0.70710678118655,-0.707106781186545,0.)) ;
#55159=DIRECTION('',(0.,0.,-1.)) ;
#55160=DIRECTION('center_axis',(0.,0.,-1.)) ;
#55161=DIRECTION('ref_axis',(0.809016994374954,-0.587785252292464,0.)) ;
#55162=DIRECTION('',(0.,0.,1.)) ;
#55163=DIRECTION('center_axis',(0.,0.,-1.)) ;
#55164=DIRECTION('ref_axis',(0.891006524188373,-0.453990499739537,0.)) ;
#55165=DIRECTION('',(0.,0.,-1.)) ;
#55166=DIRECTION('center_axis',(0.,0.,-1.)) ;
#55167=DIRECTION('ref_axis',(0.951056516295156,-0.309016994374941,0.)) ;
#55168=DIRECTION('',(0.,0.,1.)) ;
#55169=DIRECTION('center_axis',(0.,0.,-1.)) ;
#55170=DIRECTION('ref_axis',(0.987688340595139,-0.156434465040226,0.)) ;
#55171=DIRECTION('',(0.,0.,-1.)) ;
#55172=DIRECTION('center_axis',(0.,0.,-1.)) ;
#55173=DIRECTION('ref_axis',(1.,0.,0.)) ;
#55174=DIRECTION('',(0.,0.,1.)) ;
#55175=DIRECTION('center_axis',(0.,0.,-1.)) ;
#55176=DIRECTION('ref_axis',(0.987688340595137,0.156434465040233,0.)) ;
#55177=DIRECTION('',(0.,0.,-1.)) ;
#55178=DIRECTION('center_axis',(0.,0.,-1.)) ;
#55179=DIRECTION('ref_axis',(0.951056516295154,0.309016994374947,0.)) ;
#55180=DIRECTION('',(0.,0.,1.)) ;
#55181=DIRECTION('center_axis',(0.,0.,-1.)) ;
#55182=DIRECTION('ref_axis',(0.891006524188367,0.453990499739548,0.)) ;
#55183=DIRECTION('',(0.,0.,-1.)) ;
#55184=DIRECTION('center_axis',(0.,0.,-1.)) ;
#55185=DIRECTION('ref_axis',(0.809016994374945,0.587785252292477,0.)) ;
#55186=DIRECTION('',(0.,0.,1.)) ;
#55187=DIRECTION('center_axis',(0.,0.,-1.)) ;
#55188=DIRECTION('ref_axis',(0.707106781186547,0.707106781186547,0.)) ;
#55189=DIRECTION('',(0.,0.,-1.)) ;
#55190=DIRECTION('center_axis',(0.,0.,-1.)) ;
#55191=DIRECTION('ref_axis',(0.587785252292479,0.809016994374943,0.)) ;
#55192=DIRECTION('',(0.,0.,1.)) ;
#55193=DIRECTION('center_axis',(0.,0.,-1.)) ;
#55194=DIRECTION('ref_axis',(0.453990499739548,0.891006524188367,0.)) ;
#55195=DIRECTION('',(0.,0.,-1.)) ;
#55196=DIRECTION('center_axis',(0.,0.,-1.)) ;
#55197=DIRECTION('ref_axis',(0.30901699437495,0.951056516295153,0.)) ;
#55198=DIRECTION('',(0.,0.,1.)) ;
#55199=DIRECTION('center_axis',(0.,0.,-1.)) ;
#55200=DIRECTION('ref_axis',(0.156434465040232,0.987688340595138,0.)) ;
#55201=DIRECTION('',(0.,0.,-1.)) ;
#55202=DIRECTION('center_axis',(0.,0.,-1.)) ;
#55203=DIRECTION('ref_axis',(4.44089209850062E-15,1.,0.)) ;
#55204=DIRECTION('',(0.,0.,1.)) ;
#55205=DIRECTION('center_axis',(0.,0.,-1.)) ;
#55206=DIRECTION('ref_axis',(-0.156434465040226,0.987688340595139,0.)) ;
#55207=DIRECTION('',(0.,0.,-1.)) ;
#55208=DIRECTION('center_axis',(0.,0.,-1.)) ;
#55209=DIRECTION('ref_axis',(-0.309016994374939,0.951056516295156,0.)) ;
#55210=DIRECTION('',(0.,0.,1.)) ;
#55211=DIRECTION('center_axis',(0.,0.,-1.)) ;
#55212=DIRECTION('ref_axis',(-0.453990499739542,0.89100652418837,0.)) ;
#55213=DIRECTION('',(0.,0.,-1.)) ;
#55214=DIRECTION('center_axis',(0.,0.,-1.)) ;
#55215=DIRECTION('ref_axis',(-0.587785252292473,0.809016994374948,0.)) ;
#55216=DIRECTION('',(0.,0.,1.)) ;
#55217=DIRECTION('center_axis',(0.,0.,-1.)) ;
#55218=DIRECTION('ref_axis',(-0.707106781186542,0.707106781186554,0.)) ;
#55219=DIRECTION('',(0.,0.,-1.)) ;
#55220=DIRECTION('center_axis',(0.,0.,-1.)) ;
#55221=DIRECTION('ref_axis',(-0.809016994374941,0.587785252292481,0.)) ;
#55222=DIRECTION('',(0.,0.,1.)) ;
#55223=DIRECTION('center_axis',(0.,0.,-1.)) ;
#55224=DIRECTION('ref_axis',(-0.891006524188364,0.453990499739554,0.)) ;
#55225=DIRECTION('',(0.,0.,-1.)) ;
#55226=DIRECTION('center_axis',(0.,0.,-1.)) ;
#55227=DIRECTION('ref_axis',(-0.95105651629515,0.309016994374958,0.)) ;
#55228=DIRECTION('',(0.,0.,1.)) ;
#55229=DIRECTION('center_axis',(0.,0.,-1.)) ;
#55230=DIRECTION('ref_axis',(-0.987688340595137,0.156434465040233,0.)) ;
#55231=DIRECTION('',(0.,0.,-1.)) ;
#55232=DIRECTION('center_axis',(0.,0.,-1.)) ;
#55233=DIRECTION('ref_axis',(-1.,-5.9211894646675E-15,0.)) ;
#55234=DIRECTION('center_axis',(0.,0.,-1.)) ;
#55235=DIRECTION('ref_axis',(1.,0.,0.)) ;
#55236=DIRECTION('center_axis',(0.,1.,0.)) ;
#55237=DIRECTION('ref_axis',(0.70710678118654,0.,0.707106781186555)) ;
#55238=DIRECTION('center_axis',(0.,-1.,0.)) ;
#55239=DIRECTION('ref_axis',(1.,0.,0.)) ;
#55240=DIRECTION('',(0.,1.,0.)) ;
#55241=DIRECTION('center_axis',(0.,1.,0.)) ;
#55242=DIRECTION('ref_axis',(0.,0.,1.)) ;
#55243=DIRECTION('',(0.,-1.,0.)) ;
#55244=DIRECTION('center_axis',(-1.26882631385732E-15,1.,0.)) ;
#55245=DIRECTION('ref_axis',(0.70710678118654,8.97195690676432E-16,0.707106781186555)) ;
#55246=DIRECTION('center_axis',(0.,-1.,0.)) ;
#55247=DIRECTION('ref_axis',(1.,0.,0.)) ;
#55248=DIRECTION('',(-1.26882631385732E-15,1.,0.)) ;
#55249=DIRECTION('center_axis',(0.,1.,0.)) ;
#55250=DIRECTION('ref_axis',(0.,0.,1.)) ;
#55251=DIRECTION('',(1.26882631385732E-15,-1.,0.)) ;
#55252=DIRECTION('center_axis',(0.,0.,-1.)) ;
#55253=DIRECTION('ref_axis',(-1.,0.,0.)) ;
#55254=DIRECTION('center_axis',(1.,0.,0.)) ;
#55255=DIRECTION('ref_axis',(0.,0.,1.)) ;
#55256=DIRECTION('center_axis',(0.,0.,1.)) ;
#55257=DIRECTION('ref_axis',(-0.707106781186543,0.707106781186552,0.)) ;
#55258=DIRECTION('center_axis',(0.,0.,-1.)) ;
#55259=DIRECTION('ref_axis',(-0.707106781186543,0.707106781186552,0.)) ;
#55260=DIRECTION('center_axis',(1.,0.,0.)) ;
#55261=DIRECTION('ref_axis',(0.,-0.707106781186602,0.707106781186493)) ;
#55262=DIRECTION('center_axis',(1.,0.,0.)) ;
#55263=DIRECTION('ref_axis',(0.,0.,1.)) ;
#55264=DIRECTION('',(-1.,0.,0.)) ;
#55265=DIRECTION('',(1.,0.,0.)) ;
#55266=DIRECTION('center_axis',(1.,2.96059473233375E-14,0.)) ;
#55267=DIRECTION('ref_axis',(2.09345661157853E-14,-0.707106781186602,0.707106781186493)) ;
#55268=DIRECTION('center_axis',(-1.,-4.44089209850072E-14,0.)) ;
#55269=DIRECTION('ref_axis',(4.44089209850072E-14,-1.,0.)) ;
#55270=DIRECTION('',(1.,2.96059473233375E-14,0.)) ;
#55271=DIRECTION('center_axis',(1.,4.44089209850072E-14,0.)) ;
#55272=DIRECTION('ref_axis',(0.,0.,1.)) ;
#55273=DIRECTION('',(-1.,-2.96059473233375E-14,0.)) ;
#55274=DIRECTION('center_axis',(1.,0.,0.)) ;
#55275=DIRECTION('ref_axis',(0.,-0.707106781186602,0.707106781186493)) ;
#55276=DIRECTION('center_axis',(-1.,0.,0.)) ;
#55277=DIRECTION('ref_axis',(0.,-1.,0.)) ;
#55278=DIRECTION('',(1.,0.,0.)) ;
#55279=DIRECTION('center_axis',(1.,0.,0.)) ;
#55280=DIRECTION('ref_axis',(0.,0.,1.)) ;
#55281=DIRECTION('',(-1.,0.,0.)) ;
#55282=DIRECTION('center_axis',(0.,0.,-1.)) ;
#55283=DIRECTION('ref_axis',(-1.,0.,0.)) ;
#55284=DIRECTION('center_axis',(0.,-1.,0.)) ;
#55285=DIRECTION('ref_axis',(0.,0.,1.)) ;
#55286=DIRECTION('center_axis',(0.,0.,1.)) ;
#55287=DIRECTION('ref_axis',(0.707106781186548,0.707106781186548,0.)) ;
#55288=DIRECTION('center_axis',(0.,0.,-1.)) ;
#55289=DIRECTION('ref_axis',(0.707106781186547,0.707106781186547,0.)) ;
#55290=DIRECTION('center_axis',(0.,-1.,0.)) ;
#55291=DIRECTION('ref_axis',(-0.70710678118654,0.,0.707106781186555)) ;
#55292=DIRECTION('center_axis',(0.,-1.,0.)) ;
#55293=DIRECTION('ref_axis',(0.,0.,1.)) ;
#55294=DIRECTION('',(0.,1.,0.)) ;
#55295=DIRECTION('',(0.,-1.,0.)) ;
#55296=DIRECTION('center_axis',(-7.40148683083432E-15,-1.,0.)) ;
#55297=DIRECTION('ref_axis',(-0.70710678118654,5.23364152894582E-15,0.707106781186555)) ;
#55298=DIRECTION('center_axis',(0.,1.,0.)) ;
#55299=DIRECTION('ref_axis',(-1.,0.,0.)) ;
#55300=DIRECTION('',(-7.40148683083432E-15,-1.,0.)) ;
#55301=DIRECTION('center_axis',(0.,-1.,0.)) ;
#55302=DIRECTION('ref_axis',(0.,0.,1.)) ;
#55303=DIRECTION('',(7.40148683083432E-15,1.,0.)) ;
#55304=DIRECTION('center_axis',(0.,-1.,0.)) ;
#55305=DIRECTION('ref_axis',(-0.70710678118654,0.,0.707106781186555)) ;
#55306=DIRECTION('center_axis',(0.,1.,0.)) ;
#55307=DIRECTION('ref_axis',(-1.,0.,0.)) ;
#55308=DIRECTION('',(0.,-1.,0.)) ;
#55309=DIRECTION('center_axis',(0.,-1.,0.)) ;
#55310=DIRECTION('ref_axis',(0.,0.,1.)) ;
#55311=DIRECTION('',(0.,1.,0.)) ;
#55312=DIRECTION('center_axis',(0.,0.,-1.)) ;
#55313=DIRECTION('ref_axis',(-1.,0.,0.)) ;
#55314=DIRECTION('center_axis',(-1.,0.,0.)) ;
#55315=DIRECTION('ref_axis',(0.,0.,1.)) ;
#55316=DIRECTION('center_axis',(0.,0.,1.)) ;
#55317=DIRECTION('ref_axis',(0.707106781186548,-0.707106781186548,0.)) ;
#55318=DIRECTION('center_axis',(0.,0.,-1.)) ;
#55319=DIRECTION('ref_axis',(0.707106781186547,-0.707106781186547,0.)) ;
#55320=DIRECTION('center_axis',(-1.,0.,0.)) ;
#55321=DIRECTION('ref_axis',(0.,0.707106781186477,0.707106781186618)) ;
#55322=DIRECTION('center_axis',(-1.,0.,0.)) ;
#55323=DIRECTION('ref_axis',(0.,0.,1.)) ;
#55324=DIRECTION('',(1.,0.,0.)) ;
#55325=DIRECTION('',(-1.,0.,0.)) ;
#55326=DIRECTION('center_axis',(-1.,0.,0.)) ;
#55327=DIRECTION('ref_axis',(0.,0.707106781186477,0.707106781186618)) ;
#55328=DIRECTION('center_axis',(1.,0.,0.)) ;
#55329=DIRECTION('ref_axis',(0.,1.,0.)) ;
#55330=DIRECTION('',(-1.,0.,0.)) ;
#55331=DIRECTION('center_axis',(-1.,0.,0.)) ;
#55332=DIRECTION('ref_axis',(0.,0.,1.)) ;
#55333=DIRECTION('',(1.,0.,0.)) ;
#55334=DIRECTION('center_axis',(0.,0.,-1.)) ;
#55335=DIRECTION('ref_axis',(-1.,0.,0.)) ;
#55336=DIRECTION('center_axis',(1.,0.,0.)) ;
#55337=DIRECTION('ref_axis',(0.,1.,0.)) ;
#55338=DIRECTION('center_axis',(0.,0.,-1.)) ;
#55339=DIRECTION('ref_axis',(-0.707106781186547,-0.707106781186547,0.)) ;
#55340=DIRECTION('center_axis',(0.,1.,0.)) ;
#55341=DIRECTION('ref_axis',(0.,0.,1.)) ;
#55342=DIRECTION('center_axis',(0.,0.,1.)) ;
#55343=DIRECTION('ref_axis',(-0.707106781186548,-0.707106781186548,0.)) ;
#55344=DIRECTION('center_axis',(-1.26882631385732E-15,1.,0.)) ;
#55345=DIRECTION('ref_axis',(0.70710678118654,8.97195690676432E-16,0.707106781186555)) ;
#55346=DIRECTION('center_axis',(0.,1.,0.)) ;
#55347=DIRECTION('ref_axis',(0.,0.,1.)) ;
#55348=DIRECTION('',(1.26882631385732E-15,-1.,0.)) ;
#55349=DIRECTION('',(-1.26882631385732E-15,1.,0.)) ;
#55350=DIRECTION('center_axis',(-1.,0.,0.)) ;
#55351=DIRECTION('ref_axis',(0.,0.707106781186477,0.707106781186618)) ;
#55352=DIRECTION('center_axis',(1.,0.,0.)) ;
#55353=DIRECTION('ref_axis',(0.,1.,0.)) ;
#55354=DIRECTION('',(-1.,0.,0.)) ;
#55355=DIRECTION('',(1.,0.,0.)) ;
#55356=DIRECTION('center_axis',(0.408248290463862,-0.816496580927723,0.40824829046387)) ;
#55357=DIRECTION('ref_axis',(0.577350269189623,0.577350269189623,0.577350269189632)) ;
#55358=DIRECTION('center_axis',(0.,0.,-1.)) ;
#55359=DIRECTION('ref_axis',(0.707106781186636,0.707106781186459,0.)) ;
#55360=DIRECTION('center_axis',(-0.40824829046386,-0.81649658092772,0.408248290463878)) ;
#55361=DIRECTION('ref_axis',(-0.577350269189623,0.577350269189623,0.577350269189632)) ;
#55362=DIRECTION('center_axis',(0.,0.,-1.)) ;
#55363=DIRECTION('ref_axis',(-0.707106781186636,0.707106781186459,0.)) ;
#55364=DIRECTION('center_axis',(-0.408248290463862,-0.816496580927723,0.40824829046387)) ;
#55365=DIRECTION('ref_axis',(-0.577350269189623,0.577350269189623,0.577350269189632)) ;
#55366=DIRECTION('center_axis',(0.,0.,-1.)) ;
#55367=DIRECTION('ref_axis',(-0.707106781186636,0.707106781186459,0.)) ;
#55368=DIRECTION('center_axis',(0.408248290463862,-0.816496580927723,-0.40824829046387)) ;
#55369=DIRECTION('ref_axis',(-0.577350269189623,-0.577350269189623,0.577350269189632)) ;
#55370=DIRECTION('center_axis',(0.,0.,-1.)) ;
#55371=DIRECTION('ref_axis',(-0.707106781186481,-0.707106781186614,0.)) ;
#55372=DIRECTION('center_axis',(0.40824829046386,-0.81649658092772,-0.408248290463878)) ;
#55373=DIRECTION('ref_axis',(-0.577350269189623,-0.577350269189623,0.577350269189632)) ;
#55374=DIRECTION('center_axis',(0.,0.,-1.)) ;
#55375=DIRECTION('ref_axis',(-0.707106781186614,-0.707106781186481,0.)) ;
#55376=DIRECTION('center_axis',(0.408248290463928,-0.408248290463857,-0.816496580927697)) ;
#55377=DIRECTION('ref_axis',(0.577350269189706,-0.577350269189493,0.577350269189679)) ;
#55378=DIRECTION('center_axis',(0.,0.,-1.)) ;
#55379=DIRECTION('ref_axis',(0.707106781186636,-0.707106781186459,0.)) ;
#55380=DIRECTION('center_axis',(0.40824829046386,-0.40824829046386,-0.816496580927729)) ;
#55381=DIRECTION('ref_axis',(0.577350269189626,-0.577350269189626,0.577350269189626)) ;
#55382=DIRECTION('center_axis',(0.,0.,-1.)) ;
#55383=DIRECTION('ref_axis',(0.707106781186481,-0.707106781186614,0.)) ;
#55384=DIRECTION('center_axis',(0.408248290463862,-0.816496580927723,0.40824829046387)) ;
#55385=DIRECTION('ref_axis',(0.577350269189623,0.577350269189623,0.577350269189632)) ;
#55386=DIRECTION('center_axis',(0.,0.,-1.)) ;
#55387=DIRECTION('ref_axis',(0.707106781186636,0.707106781186459,0.)) ;
#55388=DIRECTION('center_axis',(-1.,0.,0.)) ;
#55389=DIRECTION('ref_axis',(0.,1.,0.)) ;
#55390=DIRECTION('',(0.,0.,1.)) ;
#55391=DIRECTION('',(0.,-1.,0.)) ;
#55392=DIRECTION('',(0.,0.,-1.)) ;
#55393=DIRECTION('center_axis',(0.,0.,-1.)) ;
#55394=DIRECTION('ref_axis',(-0.707106781186579,-0.707106781186516,0.)) ;
#55395=DIRECTION('',(0.,0.,-1.)) ;
#55396=DIRECTION('center_axis',(0.,0.,1.)) ;
#55397=DIRECTION('ref_axis',(4.44089209850072E-14,-1.,0.)) ;
#55398=DIRECTION('center_axis',(2.96059473233375E-14,-1.,0.)) ;
#55399=DIRECTION('ref_axis',(-1.,-2.96059473233375E-14,0.)) ;
#55400=DIRECTION('',(0.,0.,1.)) ;
#55401=DIRECTION('',(1.,2.96059473233375E-14,0.)) ;
#55402=DIRECTION('center_axis',(0.,0.,-1.)) ;
#55403=DIRECTION('ref_axis',(0.70710678118661,-0.707106781186485,0.)) ;
#55404=DIRECTION('',(0.,0.,-1.)) ;
#55405=DIRECTION('center_axis',(0.,0.,1.)) ;
#55406=DIRECTION('ref_axis',(1.,0.,0.)) ;
#55407=DIRECTION('center_axis',(1.,1.26882631385732E-15,0.)) ;
#55408=DIRECTION('ref_axis',(1.26882631385732E-15,-1.,0.)) ;
#55409=DIRECTION('',(0.,0.,1.)) ;
#55410=DIRECTION('',(-1.26882631385732E-15,1.,0.)) ;
#55411=DIRECTION('center_axis',(0.,0.,-1.)) ;
#55412=DIRECTION('ref_axis',(-0.707106781186554,0.707106781186541,0.)) ;
#55413=DIRECTION('',(0.,0.,-1.)) ;
#55414=DIRECTION('center_axis',(0.,0.,-1.)) ;
#55415=DIRECTION('ref_axis',(-0.707106781186539,0.707106781186556,0.)) ;
#55416=DIRECTION('center_axis',(0.,-1.,0.)) ;
#55417=DIRECTION('ref_axis',(-1.,0.,0.)) ;
#55418=DIRECTION('',(0.,0.,1.)) ;
#55419=DIRECTION('',(1.,0.,0.)) ;
#55420=DIRECTION('center_axis',(0.,0.,-1.)) ;
#55421=DIRECTION('ref_axis',(0.707106781186485,-0.70710678118661,0.)) ;
#55422=DIRECTION('',(0.,0.,-1.)) ;
#55423=DIRECTION('center_axis',(0.,0.,1.)) ;
#55424=DIRECTION('ref_axis',(1.,0.,0.)) ;
#55425=DIRECTION('center_axis',(1.,0.,0.)) ;
#55426=DIRECTION('ref_axis',(0.,-1.,0.)) ;
#55427=DIRECTION('',(0.,0.,1.)) ;
#55428=DIRECTION('',(0.,1.,0.)) ;
#55429=DIRECTION('center_axis',(0.,0.,-1.)) ;
#55430=DIRECTION('ref_axis',(0.70710678118661,0.707106781186485,0.)) ;
#55431=DIRECTION('',(0.,0.,-1.)) ;
#55432=DIRECTION('center_axis',(0.,0.,1.)) ;
#55433=DIRECTION('ref_axis',(0.,1.,0.)) ;
#55434=DIRECTION('center_axis',(0.,1.,0.)) ;
#55435=DIRECTION('ref_axis',(1.,0.,0.)) ;
#55436=DIRECTION('',(0.,0.,1.)) ;
#55437=DIRECTION('',(-1.,0.,0.)) ;
#55438=DIRECTION('center_axis',(0.,0.,-1.)) ;
#55439=DIRECTION('ref_axis',(-0.707106781186548,-0.707106781186548,0.)) ;
#55440=DIRECTION('',(0.,0.,-1.)) ;
#55441=DIRECTION('center_axis',(0.,0.,-1.)) ;
#55442=DIRECTION('ref_axis',(-0.707106781186564,-0.707106781186531,0.)) ;
#55443=DIRECTION('center_axis',(0.,0.,-1.)) ;
#55444=DIRECTION('ref_axis',(1.,0.,0.)) ;
#55445=DIRECTION('center_axis',(0.,0.,1.)) ;
#55446=DIRECTION('ref_axis',(1.,0.,0.)) ;
#55447=DIRECTION('center_axis',(-1.31682711760943E-11,1.79856020404298E-11,
-1.)) ;
#55448=DIRECTION('ref_axis',(0.806857664468129,0.590745892316684,4.62568615494041E-26)) ;
#55449=DIRECTION('center_axis',(-0.317035052983307,0.433015558388784,0.843792807135212)) ;
#55450=DIRECTION('ref_axis',(-0.365456287528658,0.765207700889935,-0.529998940003196)) ;
#55451=DIRECTION('center_axis',(0.902369376537521,0.4309634651421,-4.58229759167643E-13)) ;
#55452=DIRECTION('ref_axis',(-0.4309634651421,0.902369376537521,2.6214339396372E-29)) ;
#55453=DIRECTION('center_axis',(0.,0.,1.)) ;
#55454=DIRECTION('ref_axis',(1.,0.,0.)) ;
#55455=DIRECTION('center_axis',(2.16808315015822E-11,4.00706478615926E-12,
-1.)) ;
#55456=DIRECTION('ref_axis',(-0.181742644394422,0.98334612990977,-7.78466561773078E-27)) ;
#55457=DIRECTION('center_axis',(-0.983346129909754,-0.181742644394508,-2.43498486700547E-13)) ;
#55458=DIRECTION('ref_axis',(-0.154117454211813,0.83387585041345,-0.5299989400032)) ;
#55459=DIRECTION('center_axis',(0.00196658646623397,0.536665474150936,0.843792807146412)) ;
#55460=DIRECTION('ref_axis',(-0.999993285952489,0.00366443037087552,-1.17624957867241E-19)) ;
#55461=DIRECTION('center_axis',(0.,0.,1.)) ;
#55462=DIRECTION('ref_axis',(-0.928035724969788,0.372491198795086,0.)) ;
#55463=DIRECTION('center_axis',(1.9734015444057E-11,1.07018918516592E-11,
-1.)) ;
#55464=DIRECTION('ref_axis',(-0.476718191734985,0.879056178903787,-9.54822769938885E-27)) ;
#55465=DIRECTION('center_axis',(-0.879056178903635,-0.476718191735265,-3.46485113656339E-13)) ;
#55466=DIRECTION('ref_axis',(-0.404256218079704,0.745438148835541,-0.52999894000322)) ;
#55467=DIRECTION('center_axis',(-0.163968416933248,0.511006904900617,0.843792807146574)) ;
#55468=DIRECTION('ref_axis',(-0.952182502115841,-0.305529839237374,-1.20183483998926E-16)) ;
#55469=DIRECTION('center_axis',(0.,0.,-1.)) ;
#55470=DIRECTION('ref_axis',(-1.,0.,0.)) ;
#55471=DIRECTION('center_axis',(8.28544638211486E-16,4.22164579210903E-16,
1.)) ;
#55472=DIRECTION('ref_axis',(-0.453990499739544,0.891006524188369,1.49459261390817E-31)) ;
#55473=DIRECTION('center_axis',(0.,0.,1.)) ;
#55474=DIRECTION('ref_axis',(1.,0.,0.)) ;
#55475=DIRECTION('center_axis',(-6.99415838648067E-12,2.1260400847229E-11,
-1.)) ;
#55476=DIRECTION('ref_axis',(0.949917759598147,0.312500000000059,8.11578044958985E-27)) ;
#55477=DIRECTION('center_axis',(-0.167709086662903,0.509791487647221,0.843792807135216)) ;
#55478=DIRECTION('ref_axis',(-0.111107399873594,0.840687973798145,-0.529998940003183)) ;
#55479=DIRECTION('center_axis',(0.991379310344833,0.131023139254877,-1.92356772507714E-13)) ;
#55480=DIRECTION('ref_axis',(-0.131023139254877,0.991379310344833,2.71194847215894E-32)) ;
#55481=DIRECTION('center_axis',(0.,0.,1.)) ;
#55482=DIRECTION('ref_axis',(1.,0.,0.)) ;
#55483=DIRECTION('center_axis',(-2.9576381803503E-9,2.13233469821874E-9,
-1.)) ;
#55484=DIRECTION('ref_axis',(0.584816719432152,0.811165460724639,-3.75440385536796E-24)) ;
#55485=DIRECTION('center_axis',(-0.435327416839363,0.31385305198745,0.843792807451054)) ;
#55486=DIRECTION('ref_axis',(-0.584031767477094,0.614823566702723,-0.529998940003208)) ;
#55487=DIRECTION('center_axis',(0.725029240977556,0.688718084362179,-4.33368493355678E-11)) ;
#55488=DIRECTION('ref_axis',(-0.688718084362179,0.725029240977556,4.25223242774214E-27)) ;
#55489=DIRECTION('center_axis',(0.,0.,1.)) ;
#55490=DIRECTION('ref_axis',(1.,0.,0.)) ;
#55491=DIRECTION('center_axis',(2.1947551897582E-11,-2.90064268900393E-12,
-1.)) ;
#55492=DIRECTION('ref_axis',(0.13102313925492,0.991379310344828,-1.27623067668808E-26)) ;
#55493=DIRECTION('center_axis',(-0.991379310344839,0.131023139254833,-1.40543823316144E-13)) ;
#55494=DIRECTION('ref_axis',(0.111107399873597,0.840687973798168,-0.529998940003147)) ;
#55495=DIRECTION('center_axis',(0.16770908668058,0.509791487623121,0.843792807146263)) ;
#55496=DIRECTION('ref_axis',(-0.949917759597208,0.312500000002913,1.29384740635467E-16)) ;
#55497=DIRECTION('center_axis',(0.,0.,1.)) ;
#55498=DIRECTION('ref_axis',(-0.997720534269979,0.0674813714741176,0.)) ;
#55499=DIRECTION('center_axis',(1.55778144178567E-11,1.63991206560649E-11,
-1.)) ;
#55500=DIRECTION('ref_axis',(-0.725029240977598,0.688718084362135,9.07425119548907E-27)) ;
#55501=DIRECTION('center_axis',(-0.688718084362041,-0.725029240977687,-3.15160813713268E-13)) ;
#55502=DIRECTION('ref_axis',(-0.614823566703066,0.584031767476771,-0.529998940003165)) ;
#55503=DIRECTION('center_axis',(-0.313853049248083,0.435327419404426,0.843792807146614)) ;
#55504=DIRECTION('ref_axis',(-0.811165460726608,-0.584816719429421,2.43009916984589E-17)) ;
#55505=DIRECTION('center_axis',(0.,0.,-1.)) ;
#55506=DIRECTION('ref_axis',(-1.,0.,0.)) ;
#55507=DIRECTION('center_axis',(0.,0.,1.)) ;
#55508=DIRECTION('ref_axis',(-0.70710678118654,0.707106781186555,0.)) ;
#55509=DIRECTION('center_axis',(0.,0.,1.)) ;
#55510=DIRECTION('ref_axis',(1.,0.,0.)) ;
#55511=DIRECTION('center_axis',(-8.18284374038753E-14,2.2330315979718E-11,
-1.)) ;
#55512=DIRECTION('ref_axis',(0.9999932859525,0.00366443036803338,-2.0111893130656E-29)) ;
#55513=DIRECTION('center_axis',(-0.00196658644184458,0.536665474168601,
0.843792807135234)) ;
#55514=DIRECTION('ref_axis',(0.154117454211902,0.833875850413451,-0.529998940003172)) ;
#55515=DIRECTION('center_axis',(0.983346129909768,-0.181742644394433,-2.0434311177167E-13)) ;
#55516=DIRECTION('ref_axis',(0.181742644394433,0.983346129909768,1.81948992375041E-30)) ;
#55517=DIRECTION('center_axis',(0.,0.,1.)) ;
#55518=DIRECTION('ref_axis',(1.,0.,0.)) ;
#55519=DIRECTION('center_axis',(-3.47159356885201E-9,1.11394131129615E-9,
-1.)) ;
#55520=DIRECTION('ref_axis',(0.30552983924033,0.952182502114893,-5.05335281096018E-24)) ;
#55521=DIRECTION('center_axis',(-0.511006903307709,0.163968420330768,0.843792807451035)) ;
#55522=DIRECTION('ref_axis',(-0.745438148835789,0.404256218079294,-0.529998940003184)) ;
#55523=DIRECTION('center_axis',(0.476718191734985,0.879056178903787,-4.318892192726E-11)) ;
#55524=DIRECTION('ref_axis',(-0.879056178903787,0.476718191734985,-2.44707824205826E-27)) ;
#55525=DIRECTION('center_axis',(0.,0.,1.)) ;
#55526=DIRECTION('ref_axis',(1.,0.,0.)) ;
#55527=DIRECTION('center_axis',(2.04816646369444E-11,-9.78185806535746E-12,
-1.)) ;
#55528=DIRECTION('ref_axis',(0.430963465142067,0.902369376537536,1.52695952366941E-26)) ;
#55529=DIRECTION('center_axis',(-0.902369376537554,0.430963465142031,1.0484051409526E-14)) ;
#55530=DIRECTION('ref_axis',(0.365456287528609,0.765207700890011,-0.52999894000312)) ;
#55531=DIRECTION('center_axis',(0.317035052992538,0.433015558359767,0.843792807146635)) ;
#55532=DIRECTION('ref_axis',(-0.806857664466093,0.590745892319466,-1.0919610983098E-14)) ;
#55533=DIRECTION('center_axis',(0.,0.,1.)) ;
#55534=DIRECTION('ref_axis',(-0.969741506148218,-0.244134002657118,0.)) ;
#55535=DIRECTION('center_axis',(9.63335300264386E-12,2.01707185088096E-11,
-1.)) ;
#55536=DIRECTION('ref_axis',(-0.902369376537538,0.430963465142064,-8.19822425960458E-27)) ;
#55537=DIRECTION('center_axis',(-0.430963465142029,-0.902369376537555,-4.78686444844716E-13)) ;
#55538=DIRECTION('ref_axis',(-0.76520770088988,0.365456287528832,-0.529998940003155)) ;
#55539=DIRECTION('center_axis',(-0.433015558360072,0.317035052992619,0.843792807146448)) ;
#55540=DIRECTION('ref_axis',(-0.590745892319279,-0.806857664466229,4.35385268996785E-16)) ;
#55541=DIRECTION('center_axis',(0.,0.,-1.)) ;
#55542=DIRECTION('ref_axis',(-1.,0.,0.)) ;
#55543=DIRECTION('center_axis',(-4.22164579210917E-16,-8.28544638211483E-16,
1.)) ;
#55544=DIRECTION('ref_axis',(-0.891006524188363,0.453990499739557,-3.67890034138173E-31)) ;
#55545=DIRECTION('center_axis',(0.,0.,1.)) ;
#55546=DIRECTION('ref_axis',(1.,0.,0.)) ;
#55547=DIRECTION('center_axis',(1.1139654743955E-9,3.47166887305239E-9,
-1.)) ;
#55548=DIRECTION('ref_axis',(0.95218250211488,-0.30552983924037,3.12386086939447E-24)) ;
#55549=DIRECTION('center_axis',(0.163968420330646,0.511006903307724,0.843792807451049)) ;
#55550=DIRECTION('ref_axis',(0.404256218079267,0.745438148835828,-0.529998940003149)) ;
#55551=DIRECTION('center_axis',(0.879056178903768,-0.476718191735019,-4.35521559523163E-11)) ;
#55552=DIRECTION('ref_axis',(0.476718191735019,0.879056178903768,1.19542347053691E-27)) ;
#55553=DIRECTION('center_axis',(0.,0.,1.)) ;
#55554=DIRECTION('ref_axis',(1.,0.,0.)) ;
#55555=DIRECTION('center_axis',(-2.2505433560128E-11,-8.24701478889645E-14,
-1.)) ;
#55556=DIRECTION('ref_axis',(-0.00366443036789935,0.9999932859525,-6.10256549266988E-30)) ;
#55557=DIRECTION('center_axis',(-0.536665474168608,-0.00196658644177862,
0.843792807135229)) ;
#55558=DIRECTION('ref_axis',(-0.833875850413441,0.154117454211901,-0.529998940003188)) ;
#55559=DIRECTION('center_axis',(0.181742644394586,0.98334612990974,1.24050620488944E-13)) ;
#55560=DIRECTION('ref_axis',(-0.98334612990974,0.181742644394586,4.16361191750322E-31)) ;
#55561=DIRECTION('center_axis',(0.,0.,1.)) ;
#55562=DIRECTION('ref_axis',(1.,0.,0.)) ;
#55563=DIRECTION('center_axis',(1.63294940199106E-11,-1.55116748461524E-11,
-1.)) ;
#55564=DIRECTION('ref_axis',(0.688718084362179,0.725029240977556,-3.72638284961352E-26)) ;
#55565=DIRECTION('center_axis',(-0.725029240977534,0.688718084362202,3.31781870825906E-13)) ;
#55566=DIRECTION('ref_axis',(0.584031767476678,0.614823566703193,-0.529998940003121)) ;
#55567=DIRECTION('center_axis',(0.435327419404398,0.313853049248157,0.843792807146601)) ;
#55568=DIRECTION('ref_axis',(-0.584816719429501,0.81116546072655,-2.76706225236514E-14)) ;
#55569=DIRECTION('center_axis',(0.,0.,1.)) ;
#55570=DIRECTION('ref_axis',(-0.846837422818252,-0.531851839626921,0.)) ;
#55571=DIRECTION('center_axis',(2.95467354287013E-12,2.23563733542085E-11,
-1.)) ;
#55572=DIRECTION('ref_axis',(-0.99137931034482,0.131023139254975,-2.37981664476678E-27)) ;
#55573=DIRECTION('center_axis',(-0.13102313925497,-0.991379310344821,-2.30233604581775E-13)) ;
#55574=DIRECTION('ref_axis',(-0.840687973798143,0.11110739987376,-0.529998940003153)) ;
#55575=DIRECTION('center_axis',(-0.509791487622676,0.167709086680539,0.84379280714654)) ;
#55576=DIRECTION('ref_axis',(-0.3125000000031,-0.949917759597147,-6.06868932102577E-15)) ;
#55577=DIRECTION('center_axis',(0.,0.,-1.)) ;
#55578=DIRECTION('ref_axis',(-1.,0.,0.)) ;
#55579=DIRECTION('center_axis',(-4.07310400565444E-16,-2.57165665851294E-15,
1.)) ;
#55580=DIRECTION('ref_axis',(-0.987688340595137,0.156434465040233,1.02208220263746E-30)) ;
#55581=DIRECTION('center_axis',(0.,0.,1.)) ;
#55582=DIRECTION('ref_axis',(1.,0.,0.)) ;
#55583=DIRECTION('center_axis',(2.13219594596649E-9,2.95744572512378E-9,
-1.)) ;
#55584=DIRECTION('ref_axis',(0.811165460724706,-0.584816719432059,2.16408345829625E-24)) ;
#55585=DIRECTION('center_axis',(0.31385305198712,0.435327416839625,0.843792807451041)) ;
#55586=DIRECTION('ref_axis',(0.614823566702783,0.584031767477069,-0.529998940003167)) ;
#55587=DIRECTION('center_axis',(0.688718084362157,-0.725029240977577,-4.29727203305136E-11)) ;
#55588=DIRECTION('ref_axis',(0.725029240977577,0.688718084362157,-2.82507373973619E-28)) ;
#55589=DIRECTION('center_axis',(0.,0.,1.)) ;
#55590=DIRECTION('ref_axis',(-0.846837422818128,0.531851839627119,0.)) ;
#55591=DIRECTION('center_axis',(-2.13516241724208E-11,-7.02416865719327E-12,
-1.)) ;
#55592=DIRECTION('ref_axis',(-0.312499999999965,0.949917759598178,-2.13901517135901E-26)) ;
#55593=DIRECTION('center_axis',(-0.509791487647294,-0.167709086662617,0.843792807135229)) ;
#55594=DIRECTION('ref_axis',(-0.840687973798133,-0.111107399873593,-0.529998940003203)) ;
#55595=DIRECTION('center_axis',(-0.131023139254975,0.99137931034482,1.00333650532032E-13)) ;
#55596=DIRECTION('ref_axis',(-0.99137931034482,-0.131023139254975,-1.54140930935766E-30)) ;
#55597=DIRECTION('center_axis',(0.,0.,1.)) ;
#55598=DIRECTION('ref_axis',(1.,0.,0.)) ;
#55599=DIRECTION('center_axis',(1.06076376456186E-11,-1.95602130936441E-11,
-1.)) ;
#55600=DIRECTION('ref_axis',(0.879056178903777,0.476718191735003,-1.06012529608883E-27)) ;
#55601=DIRECTION('center_axis',(-0.476718191735159,0.879056178903692,-5.28038199040795E-14)) ;
#55602=DIRECTION('ref_axis',(0.745438148835549,0.404256218079769,-0.529998940003159)) ;
#55603=DIRECTION('center_axis',(0.511006904900899,0.163968416933291,0.843792807146396)) ;
#55604=DIRECTION('ref_axis',(-0.305529839237293,0.952182502115867,-3.36895286441765E-16)) ;
#55605=DIRECTION('center_axis',(0.,0.,1.)) ;
#55606=DIRECTION('ref_axis',(1.,0.,0.)) ;
#55607=DIRECTION('center_axis',(-4.09946443533915E-12,2.21807738113741E-11,
-1.)) ;
#55608=DIRECTION('ref_axis',(-0.983346129909772,-0.181742644394414,7.99870886518743E-27)) ;
#55609=DIRECTION('center_axis',(0.181742644394235,-0.983346129909805,3.51119831505045E-13)) ;
#55610=DIRECTION('ref_axis',(-0.833875850413454,-0.154117454211895,-0.529998940003169)) ;
#55611=DIRECTION('center_axis',(-0.536665474150717,0.00196658646630492,
0.843792807146551)) ;
#55612=DIRECTION('ref_axis',(-0.00366443037100923,-0.999993285952489,-4.49392882749049E-18)) ;
#55613=DIRECTION('center_axis',(0.,0.,-1.)) ;
#55614=DIRECTION('ref_axis',(-1.,0.,0.)) ;
#55615=DIRECTION('center_axis',(4.07310400565444E-16,-2.57165665851294E-15,
1.)) ;
#55616=DIRECTION('ref_axis',(-0.987688340595137,-0.156434465040233,-1.02208220263746E-30)) ;
#55617=DIRECTION('center_axis',(0.,0.,1.)) ;
#55618=DIRECTION('ref_axis',(1.,0.,0.)) ;
#55619=DIRECTION('center_axis',(1.7935464781828E-11,1.31315628682055E-11,
-1.)) ;
#55620=DIRECTION('ref_axis',(0.590745892316729,-0.806857664468097,-2.56130688849362E-26)) ;
#55621=DIRECTION('center_axis',(0.433015558388759,0.317035052983428,0.84379280713518)) ;
#55622=DIRECTION('ref_axis',(0.765207700889972,0.365456287528543,-0.529998940003221)) ;
#55623=DIRECTION('center_axis',(0.430963465142209,-0.902369376537469,2.13644511040471E-13)) ;
#55624=DIRECTION('ref_axis',(0.902369376537469,0.430963465142209,1.03035559199192E-29)) ;
#55625=DIRECTION('center_axis',(0.,0.,1.)) ;
#55626=DIRECTION('ref_axis',(-0.969741506148105,0.244134002657569,0.)) ;
#55627=DIRECTION('center_axis',(-1.81360138162381E-11,-1.32783960997652E-11,
-1.)) ;
#55628=DIRECTION('ref_axis',(-0.590745892316613,0.806857664468181,4.5131152795346E-26)) ;
#55629=DIRECTION('center_axis',(-0.433015558388868,-0.317035052983152,0.843792807135227)) ;
#55630=DIRECTION('ref_axis',(-0.765207700889916,-0.365456287528693,-0.529998940003199)) ;
#55631=DIRECTION('center_axis',(-0.430963465142191,0.902369376537477,-1.55470811146141E-13)) ;
#55632=DIRECTION('ref_axis',(-0.902369376537477,-0.430963465142191,-2.56005574118538E-30)) ;
#55633=DIRECTION('center_axis',(0.,0.,1.)) ;
#55634=DIRECTION('ref_axis',(1.,0.,0.)) ;
#55635=DIRECTION('center_axis',(4.10254442364617E-12,-2.21974385550383E-11,
-1.)) ;
#55636=DIRECTION('ref_axis',(0.98334612990977,0.181742644394422,1.01873606893427E-26)) ;
#55637=DIRECTION('center_axis',(-0.181742644394422,0.98334612990977,6.10504213176762E-14)) ;
#55638=DIRECTION('ref_axis',(0.833875850413441,0.154117454211901,-0.529998940003189)) ;
#55639=DIRECTION('center_axis',(0.536665474150816,-0.00196658646632877,
0.843792807146488)) ;
#55640=DIRECTION('ref_axis',(0.00366443037105299,0.999993285952489,-2.34126876451944E-18)) ;
#55641=DIRECTION('center_axis',(0.,0.,1.)) ;
#55642=DIRECTION('ref_axis',(1.,0.,0.)) ;
#55643=DIRECTION('center_axis',(-1.06507252826682E-11,1.96396655966931E-11,
-1.)) ;
#55644=DIRECTION('ref_axis',(-0.879056178903767,-0.476718191735022,-5.02209139854702E-27)) ;
#55645=DIRECTION('center_axis',(0.476718191735315,-0.879056178903608,-3.76403016459087E-13)) ;
#55646=DIRECTION('ref_axis',(-0.745438148835569,-0.404256218079756,-0.529998940003141)) ;
#55647=DIRECTION('center_axis',(-0.51100690490078,-0.163968416933259,0.843792807146473)) ;
#55648=DIRECTION('ref_axis',(0.305529839237304,-0.952182502115864,-1.10174364593412E-16)) ;
#55649=DIRECTION('center_axis',(0.,0.,-1.)) ;
#55650=DIRECTION('ref_axis',(-1.,0.,0.)) ;
#55651=DIRECTION('center_axis',(4.22164579210906E-16,-8.28544638211488E-16,
1.)) ;
#55652=DIRECTION('ref_axis',(-0.891006524188369,-0.453990499739545,8.13162959031963E-31)) ;
#55653=DIRECTION('center_axis',(0.,0.,1.)) ;
#55654=DIRECTION('ref_axis',(1.,0.,0.)) ;
#55655=DIRECTION('center_axis',(2.14643118094183E-11,7.06124016807633E-12,
-1.)) ;
#55656=DIRECTION('ref_axis',(0.312500000000018,-0.94991775959816,2.99169651445016E-27)) ;
#55657=DIRECTION('center_axis',(0.509791487647313,0.167709086662475,0.843792807135246)) ;
#55658=DIRECTION('ref_axis',(0.840687973798138,0.111107399873593,-0.529998940003195)) ;
#55659=DIRECTION('center_axis',(0.131023139254964,-0.991379310344822,-5.71828291818378E-13)) ;
#55660=DIRECTION('ref_axis',(0.991379310344822,0.131023139254964,4.17162583323648E-30)) ;
#55661=DIRECTION('center_axis',(0.,0.,1.)) ;
#55662=DIRECTION('ref_axis',(-0.997720534324265,-0.0674813706714934,0.)) ;
#55663=DIRECTION('center_axis',(-2.13215299884117E-9,-2.95738615564921E-9,
-1.)) ;
#55664=DIRECTION('ref_axis',(-0.811165460724706,0.584816719432059,1.39233222030208E-24)) ;
#55665=DIRECTION('center_axis',(-0.313853051987107,-0.435327416839706,0.843792807451004)) ;
#55666=DIRECTION('ref_axis',(-0.614823566702853,-0.584031767476959,-0.529998940003206)) ;
#55667=DIRECTION('center_axis',(-0.688718084362157,0.725029240977577,-4.33310958927125E-11)) ;
#55668=DIRECTION('ref_axis',(-0.725029240977577,-0.688718084362157,1.5461825750629E-27)) ;
#55669=DIRECTION('center_axis',(0.,0.,1.)) ;
#55670=DIRECTION('ref_axis',(1.,0.,0.)) ;
#55671=DIRECTION('center_axis',(-2.94653190735649E-12,-2.22947701210221E-11,
-1.)) ;
#55672=DIRECTION('ref_axis',(0.991379310344822,-0.131023139254964,-6.81534253461201E-28)) ;
#55673=DIRECTION('center_axis',(0.131023139254789,0.991379310344845,-5.43252859013157E-13)) ;
#55674=DIRECTION('ref_axis',(0.840687973798117,-0.111107399873768,-0.529998940003192)) ;
#55675=DIRECTION('center_axis',(0.509791487622542,-0.167709086680493,0.84379280714663)) ;
#55676=DIRECTION('ref_axis',(0.312500000003087,0.949917759597151,1.58736934972717E-16)) ;
#55677=DIRECTION('center_axis',(0.,0.,1.)) ;
#55678=DIRECTION('ref_axis',(1.,0.,0.)) ;
#55679=DIRECTION('center_axis',(-1.62352932768802E-11,1.54221918961996E-11,
-1.)) ;
#55680=DIRECTION('ref_axis',(-0.688718084362202,-0.725029240977533,1.19191244840782E-26)) ;
#55681=DIRECTION('center_axis',(0.725029240977534,-0.688718084362202,2.10320299617929E-13)) ;
#55682=DIRECTION('ref_axis',(-0.58403176747671,-0.614823566703132,-0.529998940003157)) ;
#55683=DIRECTION('center_axis',(-0.435327419404505,-0.313853049248141,0.843792807146552)) ;
#55684=DIRECTION('ref_axis',(0.584816719429358,-0.811165460726653,-5.01043326805999E-14)) ;
#55685=DIRECTION('center_axis',(0.,0.,-1.)) ;
#55686=DIRECTION('ref_axis',(-1.,0.,0.)) ;
#55687=DIRECTION('center_axis',(1.44658084518888E-15,-1.70959554431413E-15,
1.)) ;
#55688=DIRECTION('ref_axis',(-0.707106781186548,-0.707106781186548,-1.85979477303204E-16)) ;
#55689=DIRECTION('center_axis',(0.,0.,1.)) ;
#55690=DIRECTION('ref_axis',(1.,0.,0.)) ;
#55691=DIRECTION('center_axis',(2.24206992470253E-11,8.21596428150777E-14,
-1.)) ;
#55692=DIRECTION('ref_axis',(0.00366443036794375,-0.9999932859525,-1.73167550995323E-28)) ;
#55693=DIRECTION('center_axis',(0.536665474168609,0.00196658644184461,0.843792807135228)) ;
#55694=DIRECTION('ref_axis',(0.833875850413446,-0.154117454211902,-0.529998940003181)) ;
#55695=DIRECTION('center_axis',(-0.181742644394406,-0.983346129909773,8.68769869850415E-14)) ;
#55696=DIRECTION('ref_axis',(0.983346129909773,-0.181742644394406,-7.34270832319073E-31)) ;
#55697=DIRECTION('center_axis',(0.,0.,1.)) ;
#55698=DIRECTION('ref_axis',(-0.928035725269356,-0.372491198048733,0.)) ;
#55699=DIRECTION('center_axis',(-1.11393785942449E-9,-3.4715828111092E-9,
-1.)) ;
#55700=DIRECTION('ref_axis',(-0.952182502114923,0.305529839240235,-3.60849389683753E-24)) ;
#55701=DIRECTION('center_axis',(-0.163968420330871,-0.511006903307736,0.843792807450998)) ;
#55702=DIRECTION('ref_axis',(-0.404256218079276,-0.745438148835749,-0.529998940003254)) ;
#55703=DIRECTION('center_axis',(-0.879056178903768,0.476718191735019,-4.37732160119147E-11)) ;
#55704=DIRECTION('ref_axis',(-0.476718191735019,-0.879056178903768,9.78614700219985E-28)) ;
#55705=DIRECTION('center_axis',(0.,0.,1.)) ;
#55706=DIRECTION('ref_axis',(1.,0.,0.)) ;
#55707=DIRECTION('center_axis',(-9.62361496574279E-12,-2.01503285987642E-11,
-1.)) ;
#55708=DIRECTION('ref_axis',(0.902369376537538,-0.430963465142064,9.56718048253853E-27)) ;
#55709=DIRECTION('center_axis',(0.430963465142353,0.9023693765374,1.31562059760998E-13)) ;
#55710=DIRECTION('ref_axis',(0.765207700889898,-0.36545628752882,-0.529998940003137)) ;
#55711=DIRECTION('center_axis',(0.43301555835997,-0.317035052992614,0.843792807146502)) ;
#55712=DIRECTION('ref_axis',(0.590745892319364,0.806857664466167,1.44988079538749E-16)) ;
#55713=DIRECTION('center_axis',(0.,0.,1.)) ;
#55714=DIRECTION('ref_axis',(1.,0.,0.)) ;
#55715=DIRECTION('center_axis',(-2.0282863014037E-11,9.68691220559095E-12,
-1.)) ;
#55716=DIRECTION('ref_axis',(-0.430963465142136,-0.902369376537504,2.16449102858497E-26)) ;
#55717=DIRECTION('center_axis',(0.902369376537521,-0.4309634651421,-8.69409141277904E-14)) ;
#55718=DIRECTION('ref_axis',(-0.365456287528697,-0.765207700889925,-0.529998940003183)) ;
#55719=DIRECTION('center_axis',(-0.317035052992546,-0.433015558360071,0.843792807146476)) ;
#55720=DIRECTION('ref_axis',(0.806857664466293,-0.590745892319192,-1.37211078002745E-16)) ;
#55721=DIRECTION('center_axis',(0.,0.,-1.)) ;
#55722=DIRECTION('ref_axis',(-1.,0.,0.)) ;
#55723=DIRECTION('center_axis',(-9.94253565853781E-16,5.06597495053088E-16,
1.)) ;
#55724=DIRECTION('ref_axis',(-0.453990499739548,-0.891006524188367,-3.14592610423102E-31)) ;
#55725=DIRECTION('center_axis',(0.,0.,1.)) ;
#55726=DIRECTION('ref_axis',(1.,0.,0.)) ;
#55727=DIRECTION('center_axis',(3.47146985480851E-9,-1.11390161477595E-9,
-1.)) ;
#55728=DIRECTION('ref_axis',(-0.305529839240301,-0.952182502114902,-1.48325462235839E-24)) ;
#55729=DIRECTION('center_axis',(0.511006903307789,-0.1639684203306,0.843792807451018)) ;
#55730=DIRECTION('ref_axis',(0.745438148835797,-0.404256218079275,-0.529998940003187)) ;
#55731=DIRECTION('center_axis',(-0.476718191734966,-0.879056178903797,-4.38641204088889E-11)) ;
#55732=DIRECTION('ref_axis',(0.879056178903797,-0.476718191734966,-1.80827304522098E-27)) ;
#55733=DIRECTION('center_axis',(0.,0.,1.)) ;
#55734=DIRECTION('ref_axis',(1.,0.,0.)) ;
#55735=DIRECTION('center_axis',(8.22631445047335E-14,-2.24489440180613E-11,
-1.)) ;
#55736=DIRECTION('ref_axis',(-0.9999932859525,-0.00366443036785559,1.09795538423137E-28)) ;
#55737=DIRECTION('center_axis',(0.0019665864417164,-0.536665474168584,0.843792807135245)) ;
#55738=DIRECTION('ref_axis',(-0.154117454211859,-0.833875850413457,-0.529998940003176)) ;
#55739=DIRECTION('center_axis',(-0.98334612990977,0.181742644394422,-1.2520130905831E-13)) ;
#55740=DIRECTION('ref_axis',(-0.181742644394422,-0.98334612990977,3.55276238107094E-31)) ;
#55741=DIRECTION('center_axis',(0.,0.,1.)) ;
#55742=DIRECTION('ref_axis',(1.,0.,0.)) ;
#55743=DIRECTION('center_axis',(-1.53521617614545E-11,-1.61615709562502E-11,
-1.)) ;
#55744=DIRECTION('ref_axis',(0.725029240977556,-0.688718084362179,4.97396118593888E-26)) ;
#55745=DIRECTION('center_axis',(0.688718084362295,0.725029240977446,1.16091691217673E-13)) ;
#55746=DIRECTION('ref_axis',(0.614823566703032,-0.584031767476833,-0.529998940003137)) ;
#55747=DIRECTION('center_axis',(0.313853049248137,-0.435327419404485,0.843792807146564)) ;
#55748=DIRECTION('ref_axis',(0.811165460726592,0.584816719429442,5.74276711858885E-15)) ;
#55749=DIRECTION('center_axis',(0.,0.,1.)) ;
#55750=DIRECTION('ref_axis',(1.,0.,0.)) ;
#55751=DIRECTION('center_axis',(-2.20203557186253E-11,2.91026462188401E-12,
-1.)) ;
#55752=DIRECTION('ref_axis',(-0.13102313925492,-0.991379310344828,-4.30145676726048E-27)) ;
#55753=DIRECTION('center_axis',(0.991379310344833,-0.131023139254877,-7.01280755869045E-14)) ;
#55754=DIRECTION('ref_axis',(-0.111107399873598,-0.840687973798168,-0.529998940003147)) ;
#55755=DIRECTION('center_axis',(-0.167709086680666,-0.50979148762307,0.843792807146277)) ;
#55756=DIRECTION('ref_axis',(0.949917759597151,-0.312500000003087,-4.01412734958935E-16)) ;
#55757=DIRECTION('center_axis',(0.,0.,-1.)) ;
#55758=DIRECTION('ref_axis',(-1.,0.,0.)) ;
#55759=DIRECTION('center_axis',(-2.57165665851294E-15,4.0731040056544E-16,
1.)) ;
#55760=DIRECTION('ref_axis',(-0.156434465040232,-0.987688340595138,-1.98479792514679E-30)) ;
#55761=DIRECTION('center_axis',(0.,0.,1.)) ;
#55762=DIRECTION('ref_axis',(1.,0.,0.)) ;
#55763=DIRECTION('center_axis',(2.95735407977765E-9,-2.13212987346573E-9,
-1.)) ;
#55764=DIRECTION('ref_axis',(-0.584816719432093,-0.811165460724681,2.97218307444548E-24)) ;
#55765=DIRECTION('center_axis',(0.435327416839734,-0.313853051987051,0.84379280745101)) ;
#55766=DIRECTION('ref_axis',(0.584031767477118,-0.614823566702701,-0.529998940003206)) ;
#55767=DIRECTION('center_axis',(-0.725029240977556,-0.688718084362179,-4.39928696743698E-11)) ;
#55768=DIRECTION('ref_axis',(0.688718084362179,-0.725029240977556,-1.08729406708994E-27)) ;
#55769=DIRECTION('center_axis',(0.,0.,1.)) ;
#55770=DIRECTION('ref_axis',(1.,0.,0.)) ;
#55771=DIRECTION('center_axis',(7.01181148690086E-12,-2.13140616267525E-11,
-1.)) ;
#55772=DIRECTION('ref_axis',(-0.949917759598147,-0.312500000000059,-1.64248236045399E-27)) ;
#55773=DIRECTION('center_axis',(0.167709086662834,-0.50979148764727,0.8437928071352)) ;
#55774=DIRECTION('ref_axis',(0.111107399873592,-0.840687973798123,-0.529998940003219)) ;
#55775=DIRECTION('center_axis',(-0.991379310344825,-0.131023139254943,-2.99498663741709E-13)) ;
#55776=DIRECTION('ref_axis',(0.131023139254943,-0.991379310344825,-1.19589846978882E-30)) ;
#55777=DIRECTION('center_axis',(0.,0.,1.)) ;
#55778=DIRECTION('ref_axis',(1.,0.,0.)) ;
#55779=DIRECTION('center_axis',(-1.9257300425779E-11,-1.04433660293747E-11,
-1.)) ;
#55780=DIRECTION('ref_axis',(0.476718191735025,-0.879056178903765,1.65334232004212E-26)) ;
#55781=DIRECTION('center_axis',(0.879056178903672,0.476718191735196,-1.47927408302731E-13)) ;
#55782=DIRECTION('ref_axis',(0.404256218079741,-0.745438148835528,-0.52999894000321)) ;
#55783=DIRECTION('center_axis',(0.163968416933482,-0.511006904901325,0.8437928071461)) ;
#55784=DIRECTION('ref_axis',(0.952182502115837,0.305529839237387,7.9536453947219E-16)) ;
#55785=DIRECTION('center_axis',(0.,0.,1.)) ;
#55786=DIRECTION('ref_axis',(1.,0.,0.)) ;
#55787=DIRECTION('center_axis',(-2.17530453907752E-11,-4.02041140215211E-12,
-1.)) ;
#55788=DIRECTION('ref_axis',(0.181742644394422,-0.98334612990977,1.13897981748785E-26)) ;
#55789=DIRECTION('center_axis',(0.983346129909754,0.181742644394508,-1.0017383267518E-13)) ;
#55790=DIRECTION('ref_axis',(0.15411745421188,-0.833875850413392,-0.529998940003271)) ;
#55791=DIRECTION('center_axis',(-0.00196658646623659,-0.536665474151653,
0.843792807145956)) ;
#55792=DIRECTION('ref_axis',(0.999993285952489,-0.00366443037087552,-6.21826829040495E-18)) ;
#55793=DIRECTION('center_axis',(0.,0.,-1.)) ;
#55794=DIRECTION('ref_axis',(-1.,0.,0.)) ;
#55795=DIRECTION('center_axis',(5.51069283967058E-16,8.72808001211679E-17,
1.)) ;
#55796=DIRECTION('ref_axis',(0.156434465040235,-0.987688340595137,9.09125219431195E-32)) ;
#55797=DIRECTION('center_axis',(0.,0.,1.)) ;
#55798=DIRECTION('ref_axis',(1.,0.,0.)) ;
#55799=DIRECTION('center_axis',(1.29546955665479E-11,-1.76938943540163E-11,
-1.)) ;
#55800=DIRECTION('ref_axis',(-0.806857664468129,-0.590745892316684,3.0891578375814E-26)) ;
#55801=DIRECTION('center_axis',(0.317035052983624,-0.433015558388607,0.843792807135184)) ;
#55802=DIRECTION('ref_axis',(0.365456287528694,-0.765207700889918,-0.529998940003195)) ;
#55803=DIRECTION('center_axis',(-0.902369376537504,-0.430963465142136,-4.698644991465E-13)) ;
#55804=DIRECTION('ref_axis',(0.430963465142136,-0.902369376537503,1.34307188058981E-30)) ;
#55805=DIRECTION('center_axis',(0.,0.,-1.)) ;
#55806=DIRECTION('ref_axis',(-1.,0.,0.)) ;
#55807=DIRECTION('center_axis',(-3.31417855284593E-16,-1.68865831684365E-16,
1.)) ;
#55808=DIRECTION('ref_axis',(0.453990499739554,-0.891006524188364,2.22675583611484E-31)) ;
#55809=DIRECTION('center_axis',(0.,0.,-1.)) ;
#55810=DIRECTION('ref_axis',(-0.24413400265269,-0.969741506149333,0.)) ;
#55811=DIRECTION('',(0.,0.,-1.)) ;
#55812=DIRECTION('center_axis',(0.,0.,1.)) ;
#55813=DIRECTION('ref_axis',(0.767508312901273,-0.641038992283185,0.)) ;
#55814=DIRECTION('',(0.,0.,1.)) ;
#55815=DIRECTION('center_axis',(0.,0.,1.)) ;
#55816=DIRECTION('ref_axis',(0.928035724967976,-0.3724911987996,0.)) ;
#55817=DIRECTION('',(0.,0.,1.)) ;
#55818=DIRECTION('center_axis',(0.,0.,1.)) ;
#55819=DIRECTION('ref_axis',(1.,0.,0.)) ;
#55820=DIRECTION('center_axis',(0.,0.,1.)) ;
#55821=DIRECTION('ref_axis',(0.309016994374953,-0.951056516295152,0.)) ;
#55822=DIRECTION('center_axis',(0.,0.,-1.)) ;
#55823=DIRECTION('ref_axis',(-0.531851839622895,-0.846837422820781,0.)) ;
#55824=DIRECTION('',(0.,0.,-1.)) ;
#55825=DIRECTION('center_axis',(0.,0.,-1.)) ;
#55826=DIRECTION('ref_axis',(-1.,0.,0.)) ;
#55827=DIRECTION('center_axis',(1.44658084518887E-15,1.44658084518888E-15,
1.)) ;
#55828=DIRECTION('ref_axis',(0.707106781186548,-0.707106781186547,5.66547588605294E-30)) ;
#55829=DIRECTION('center_axis',(0.,0.,-1.)) ;
#55830=DIRECTION('ref_axis',(0.0674813714788309,-0.99772053426966,0.)) ;
#55831=DIRECTION('',(0.,0.,-1.)) ;
#55832=DIRECTION('center_axis',(0.,0.,1.)) ;
#55833=DIRECTION('ref_axis',(1.,0.,0.)) ;
#55834=DIRECTION('center_axis',(0.,0.,1.)) ;
#55835=DIRECTION('ref_axis',(0.587785252292479,-0.809016994374943,0.)) ;
#55836=DIRECTION('center_axis',(0.,0.,1.)) ;
#55837=DIRECTION('ref_axis',(0.531851839622895,-0.846837422820781,0.)) ;
#55838=DIRECTION('',(0.,0.,1.)) ;
#55839=DIRECTION('center_axis',(0.,0.,1.)) ;
#55840=DIRECTION('ref_axis',(1.,0.,0.)) ;
#55841=DIRECTION('center_axis',(0.,0.,1.)) ;
#55842=DIRECTION('ref_axis',(0.,-1.,0.)) ;
#55843=DIRECTION('center_axis',(0.,0.,1.)) ;
#55844=DIRECTION('ref_axis',(0.99772053426966,-0.0674813714788309,0.)) ;
#55845=DIRECTION('',(0.,0.,1.)) ;
#55846=DIRECTION('center_axis',(0.,0.,-1.)) ;
#55847=DIRECTION('ref_axis',(-0.767508312901297,-0.641038992283156,0.)) ;
#55848=DIRECTION('',(0.,0.,-1.)) ;
#55849=DIRECTION('center_axis',(0.,0.,-1.)) ;
#55850=DIRECTION('ref_axis',(-1.,0.,0.)) ;
#55851=DIRECTION('center_axis',(5.06597495053079E-16,9.94253565853788E-16,
1.)) ;
#55852=DIRECTION('ref_axis',(0.891006524188372,-0.453990499739539,-6.76446233908251E-32)) ;
#55853=DIRECTION('center_axis',(0.,0.,-1.)) ;
#55854=DIRECTION('ref_axis',(0.37249119879969,-0.92803572496794,0.)) ;
#55855=DIRECTION('',(0.,0.,-1.)) ;
#55856=DIRECTION('center_axis',(0.,0.,1.)) ;
#55857=DIRECTION('ref_axis',(1.,0.,0.)) ;
#55858=DIRECTION('center_axis',(0.,0.,1.)) ;
#55859=DIRECTION('ref_axis',(0.809016994374954,-0.587785252292464,0.)) ;
#55860=DIRECTION('center_axis',(0.,0.,1.)) ;
#55861=DIRECTION('ref_axis',(0.24413400265269,-0.969741506149333,0.)) ;
#55862=DIRECTION('',(0.,0.,1.)) ;
#55863=DIRECTION('center_axis',(0.,0.,1.)) ;
#55864=DIRECTION('ref_axis',(1.,0.,0.)) ;
#55865=DIRECTION('center_axis',(0.,0.,1.)) ;
#55866=DIRECTION('ref_axis',(-0.309016994374946,-0.951056516295154,0.)) ;
#55867=DIRECTION('center_axis',(0.,0.,1.)) ;
#55868=DIRECTION('ref_axis',(0.969741506149316,0.244134002652757,0.)) ;
#55869=DIRECTION('',(0.,0.,1.)) ;
#55870=DIRECTION('center_axis',(0.,0.,-1.)) ;
#55871=DIRECTION('ref_axis',(-0.928035724967896,-0.372491198799799,0.)) ;
#55872=DIRECTION('',(0.,0.,-1.)) ;
#55873=DIRECTION('center_axis',(0.,0.,-1.)) ;
#55874=DIRECTION('ref_axis',(-1.,0.,0.)) ;
#55875=DIRECTION('center_axis',(1.25502561241578E-16,-3.96473122685091E-16,
1.)) ;
#55876=DIRECTION('ref_axis',(0.987688340595138,-0.156434465040227,-1.85979477303204E-16)) ;
#55877=DIRECTION('center_axis',(0.,0.,-1.)) ;
#55878=DIRECTION('ref_axis',(0.641038992283168,-0.767508312901288,0.)) ;
#55879=DIRECTION('',(0.,0.,-1.)) ;
#55880=DIRECTION('center_axis',(0.,0.,1.)) ;
#55881=DIRECTION('ref_axis',(1.,0.,0.)) ;
#55882=DIRECTION('center_axis',(0.,0.,1.)) ;
#55883=DIRECTION('ref_axis',(0.951056516295156,-0.309016994374941,0.)) ;
#55884=DIRECTION('center_axis',(0.,0.,1.)) ;
#55885=DIRECTION('ref_axis',(-0.0674813714788309,-0.99772053426966,0.)) ;
#55886=DIRECTION('',(0.,0.,1.)) ;
#55887=DIRECTION('center_axis',(0.,0.,1.)) ;
#55888=DIRECTION('ref_axis',(1.,0.,0.)) ;
#55889=DIRECTION('center_axis',(0.,0.,1.)) ;
#55890=DIRECTION('ref_axis',(-0.587785252292474,-0.809016994374947,0.)) ;
#55891=DIRECTION('center_axis',(0.,0.,1.)) ;
#55892=DIRECTION('ref_axis',(0.846837422820716,0.531851839622999,0.)) ;
#55893=DIRECTION('',(0.,0.,1.)) ;
#55894=DIRECTION('center_axis',(0.,0.,-1.)) ;
#55895=DIRECTION('ref_axis',(-0.997720534269675,-0.0674813714786051,0.)) ;
#55896=DIRECTION('',(0.,0.,-1.)) ;
#55897=DIRECTION('center_axis',(0.,0.,-1.)) ;
#55898=DIRECTION('ref_axis',(-1.,0.,0.)) ;
#55899=DIRECTION('center_axis',(-4.07310400565444E-16,2.57165665851294E-15,
1.)) ;
#55900=DIRECTION('ref_axis',(0.987688340595137,0.156434465040233,-1.02208220263746E-30)) ;
#55901=DIRECTION('center_axis',(0.,0.,-1.)) ;
#55902=DIRECTION('ref_axis',(0.846837422820716,-0.531851839622999,0.)) ;
#55903=DIRECTION('',(0.,0.,-1.)) ;
#55904=DIRECTION('center_axis',(0.,0.,1.)) ;
#55905=DIRECTION('ref_axis',(1.,0.,0.)) ;
#55906=DIRECTION('center_axis',(0.,0.,1.)) ;
#55907=DIRECTION('ref_axis',(1.,0.,0.)) ;
#55908=DIRECTION('center_axis',(0.,0.,1.)) ;
#55909=DIRECTION('ref_axis',(-0.37249119879969,-0.92803572496794,0.)) ;
#55910=DIRECTION('',(0.,0.,1.)) ;
#55911=DIRECTION('center_axis',(0.,0.,1.)) ;
#55912=DIRECTION('ref_axis',(1.,0.,0.)) ;
#55913=DIRECTION('center_axis',(0.,0.,1.)) ;
#55914=DIRECTION('ref_axis',(-0.809016994374946,-0.587785252292475,0.)) ;
#55915=DIRECTION('center_axis',(0.,0.,1.)) ;
#55916=DIRECTION('ref_axis',(0.641038992283213,0.76750831290125,0.)) ;
#55917=DIRECTION('',(0.,0.,1.)) ;
#55918=DIRECTION('center_axis',(0.,0.,-1.)) ;
#55919=DIRECTION('ref_axis',(-0.969741506149309,0.244134002652785,0.)) ;
#55920=DIRECTION('',(0.,0.,-1.)) ;
#55921=DIRECTION('center_axis',(0.,0.,-1.)) ;
#55922=DIRECTION('ref_axis',(-1.,0.,0.)) ;
#55923=DIRECTION('center_axis',(-5.06597495053093E-16,9.94253565853781E-16,
1.)) ;
#55924=DIRECTION('ref_axis',(0.891006524188366,0.453990499739551,6.90961123949975E-31)) ;
#55925=DIRECTION('center_axis',(0.,0.,-1.)) ;
#55926=DIRECTION('ref_axis',(0.969741506149316,-0.244134002652757,0.)) ;
#55927=DIRECTION('',(0.,0.,-1.)) ;
#55928=DIRECTION('center_axis',(0.,0.,1.)) ;
#55929=DIRECTION('ref_axis',(1.,0.,0.)) ;
#55930=DIRECTION('center_axis',(0.,0.,1.)) ;
#55931=DIRECTION('ref_axis',(0.951056516295154,0.309016994374947,0.)) ;
#55932=DIRECTION('center_axis',(0.,0.,1.)) ;
#55933=DIRECTION('ref_axis',(-0.641038992283066,-0.767508312901373,0.)) ;
#55934=DIRECTION('',(0.,0.,1.)) ;
#55935=DIRECTION('center_axis',(0.,0.,1.)) ;
#55936=DIRECTION('ref_axis',(1.,0.,0.)) ;
#55937=DIRECTION('center_axis',(0.,0.,1.)) ;
#55938=DIRECTION('ref_axis',(-0.951056516295152,-0.309016994374953,0.)) ;
#55939=DIRECTION('center_axis',(0.,0.,1.)) ;
#55940=DIRECTION('ref_axis',(0.37249119879961,0.928035724967972,0.)) ;
#55941=DIRECTION('',(0.,0.,1.)) ;
#55942=DIRECTION('center_axis',(0.,0.,-1.)) ;
#55943=DIRECTION('ref_axis',(-0.846837422820716,0.531851839622999,0.)) ;
#55944=DIRECTION('',(0.,0.,-1.)) ;
#55945=DIRECTION('center_axis',(0.,0.,-1.)) ;
#55946=DIRECTION('ref_axis',(-1.,0.,0.)) ;
#55947=DIRECTION('center_axis',(0.,0.,1.)) ;
#55948=DIRECTION('ref_axis',(0.707106781186546,0.707106781186549,0.)) ;
#55949=DIRECTION('center_axis',(0.,0.,-1.)) ;
#55950=DIRECTION('ref_axis',(0.99772053426966,0.0674813714788348,0.)) ;
#55951=DIRECTION('',(0.,0.,-1.)) ;
#55952=DIRECTION('center_axis',(0.,0.,1.)) ;
#55953=DIRECTION('ref_axis',(1.,0.,0.)) ;
#55954=DIRECTION('center_axis',(0.,0.,1.)) ;
#55955=DIRECTION('ref_axis',(0.809016994374945,0.587785252292477,0.)) ;
#55956=DIRECTION('center_axis',(0.,0.,1.)) ;
#55957=DIRECTION('ref_axis',(-0.846837422820716,-0.531851839622999,0.)) ;
#55958=DIRECTION('',(0.,0.,1.)) ;
#55959=DIRECTION('center_axis',(0.,0.,1.)) ;
#55960=DIRECTION('ref_axis',(-1.,0.,0.)) ;
#55961=DIRECTION('center_axis',(0.,0.,1.)) ;
#55962=DIRECTION('ref_axis',(-1.,-5.9211894646675E-15,0.)) ;
#55963=DIRECTION('center_axis',(0.,0.,1.)) ;
#55964=DIRECTION('ref_axis',(0.0674813714788309,0.99772053426966,0.)) ;
#55965=DIRECTION('',(0.,0.,1.)) ;
#55966=DIRECTION('center_axis',(0.,0.,-1.)) ;
#55967=DIRECTION('ref_axis',(-0.641038992283134,0.767508312901316,0.)) ;
#55968=DIRECTION('',(0.,0.,-1.)) ;
#55969=DIRECTION('center_axis',(0.,0.,-1.)) ;
#55970=DIRECTION('ref_axis',(-1.,0.,0.)) ;
#55971=DIRECTION('center_axis',(9.94253565853781E-16,-5.06597495053088E-16,
1.)) ;
#55972=DIRECTION('ref_axis',(0.453990499739548,0.891006524188367,-3.14592610423102E-31)) ;
#55973=DIRECTION('center_axis',(0.,0.,-1.)) ;
#55974=DIRECTION('ref_axis',(0.928035724967976,0.3724911987996,0.)) ;
#55975=DIRECTION('',(0.,0.,-1.)) ;
#55976=DIRECTION('center_axis',(0.,0.,1.)) ;
#55977=DIRECTION('ref_axis',(1.,0.,0.)) ;
#55978=DIRECTION('center_axis',(0.,0.,1.)) ;
#55979=DIRECTION('ref_axis',(0.587785252292479,0.809016994374943,0.)) ;
#55980=DIRECTION('center_axis',(0.,0.,1.)) ;
#55981=DIRECTION('ref_axis',(-0.96974150614937,-0.24413400265254,0.)) ;
#55982=DIRECTION('',(0.,0.,1.)) ;
#55983=DIRECTION('center_axis',(0.,0.,1.)) ;
#55984=DIRECTION('ref_axis',(1.,0.,0.)) ;
#55985=DIRECTION('center_axis',(0.,0.,1.)) ;
#55986=DIRECTION('ref_axis',(-0.95105651629515,0.309016994374958,0.)) ;
#55987=DIRECTION('center_axis',(0.,0.,1.)) ;
#55988=DIRECTION('ref_axis',(-0.244134002652526,0.969741506149374,0.)) ;
#55989=DIRECTION('',(0.,0.,1.)) ;
#55990=DIRECTION('center_axis',(0.,0.,-1.)) ;
#55991=DIRECTION('ref_axis',(-0.37249119879956,0.928035724967992,0.)) ;
#55992=DIRECTION('',(0.,0.,-1.)) ;
#55993=DIRECTION('center_axis',(0.,0.,-1.)) ;
#55994=DIRECTION('ref_axis',(-1.,0.,0.)) ;
#55995=DIRECTION('center_axis',(2.57165665851294E-15,-4.0731040056544E-16,
1.)) ;
#55996=DIRECTION('ref_axis',(0.156434465040232,0.987688340595138,-1.98479792514679E-30)) ;
#55997=DIRECTION('center_axis',(0.,0.,-1.)) ;
#55998=DIRECTION('ref_axis',(0.767508312901183,0.641038992283292,0.)) ;
#55999=DIRECTION('',(0.,0.,-1.)) ;
#56000=DIRECTION('center_axis',(0.,0.,1.)) ;
#56001=DIRECTION('ref_axis',(1.,0.,0.)) ;
#56002=DIRECTION('center_axis',(0.,0.,1.)) ;
#56003=DIRECTION('ref_axis',(0.30901699437495,0.951056516295153,0.)) ;
#56004=DIRECTION('center_axis',(0.,0.,1.)) ;
#56005=DIRECTION('ref_axis',(-0.99772053426966,0.0674813714788309,0.)) ;
#56006=DIRECTION('',(0.,0.,1.)) ;
#56007=DIRECTION('center_axis',(0.,0.,1.)) ;
#56008=DIRECTION('ref_axis',(1.,0.,0.)) ;
#56009=DIRECTION('center_axis',(0.,0.,1.)) ;
#56010=DIRECTION('ref_axis',(-0.809016994374941,0.587785252292481,0.)) ;
#56011=DIRECTION('center_axis',(0.,0.,1.)) ;
#56012=DIRECTION('ref_axis',(-0.531851839622895,0.846837422820781,0.)) ;
#56013=DIRECTION('',(0.,0.,1.)) ;
#56014=DIRECTION('center_axis',(0.,0.,-1.)) ;
#56015=DIRECTION('ref_axis',(-0.0674813714788309,0.99772053426966,0.)) ;
#56016=DIRECTION('',(0.,0.,-1.)) ;
#56017=DIRECTION('center_axis',(0.,0.,-1.)) ;
#56018=DIRECTION('ref_axis',(-1.,0.,0.)) ;
#56019=DIRECTION('center_axis',(-1.83689761322353E-16,-2.90936000403874E-17,
1.)) ;
#56020=DIRECTION('ref_axis',(-0.156434465040225,0.987688340595139,-9.33979109190074E-33)) ;
#56021=DIRECTION('center_axis',(0.,0.,-1.)) ;
#56022=DIRECTION('ref_axis',(0.531851839622895,0.846837422820781,0.)) ;
#56023=DIRECTION('',(0.,0.,-1.)) ;
#56024=DIRECTION('center_axis',(0.,0.,1.)) ;
#56025=DIRECTION('ref_axis',(1.,0.,0.)) ;
#56026=DIRECTION('center_axis',(0.,0.,1.)) ;
#56027=DIRECTION('ref_axis',(4.44089209850062E-15,1.,0.)) ;
#56028=DIRECTION('center_axis',(0.,0.,1.)) ;
#56029=DIRECTION('ref_axis',(-0.928035724967976,0.3724911987996,0.)) ;
#56030=DIRECTION('',(0.,0.,1.)) ;
#56031=DIRECTION('center_axis',(0.,0.,1.)) ;
#56032=DIRECTION('ref_axis',(1.,0.,0.)) ;
#56033=DIRECTION('center_axis',(0.,0.,1.)) ;
#56034=DIRECTION('ref_axis',(-0.587785252292473,0.809016994374948,0.)) ;
#56035=DIRECTION('center_axis',(0.,0.,1.)) ;
#56036=DIRECTION('ref_axis',(-0.767508312901273,0.641038992283185,0.)) ;
#56037=DIRECTION('',(0.,0.,1.)) ;
#56038=DIRECTION('center_axis',(0.,0.,-1.)) ;
#56039=DIRECTION('ref_axis',(0.244134002652635,0.969741506149347,0.)) ;
#56040=DIRECTION('',(0.,0.,-1.)) ;
#56041=DIRECTION('center_axis',(0.,0.,1.)) ;
#56042=DIRECTION('ref_axis',(1.,0.,0.)) ;
#56043=DIRECTION('center_axis',(0.,0.,1.)) ;
#56044=DIRECTION('ref_axis',(-0.309016994374939,0.951056516295156,0.)) ;
#56045=DIRECTION('center_axis',(0.,0.,-1.)) ;
#56046=DIRECTION('ref_axis',(-0.809016994374947,-0.587785252292473,0.)) ;
#56047=DIRECTION('center_axis',(0.,0.,-1.)) ;
#56048=DIRECTION('ref_axis',(-0.809016994374947,-0.587785252292473,0.)) ;
#56049=DIRECTION('center_axis',(0.,0.,-1.)) ;
#56050=DIRECTION('ref_axis',(-0.587785252292473,-0.809016994374948,0.)) ;
#56051=DIRECTION('center_axis',(0.,0.,-1.)) ;
#56052=DIRECTION('ref_axis',(-0.587785252292473,-0.809016994374948,0.)) ;
#56053=DIRECTION('center_axis',(0.,0.,-1.)) ;
#56054=DIRECTION('ref_axis',(-0.309016994374947,-0.951056516295154,0.)) ;
#56055=DIRECTION('center_axis',(0.,0.,-1.)) ;
#56056=DIRECTION('ref_axis',(-0.309016994374947,-0.951056516295154,0.)) ;
#56057=DIRECTION('center_axis',(0.,0.,-1.)) ;
#56058=DIRECTION('ref_axis',(0.,-1.,0.)) ;
#56059=DIRECTION('center_axis',(0.,0.,-1.)) ;
#56060=DIRECTION('ref_axis',(0.,-1.,0.)) ;
#56061=DIRECTION('center_axis',(0.,0.,-1.)) ;
#56062=DIRECTION('ref_axis',(0.309016994374947,-0.951056516295154,0.)) ;
#56063=DIRECTION('center_axis',(0.,0.,-1.)) ;
#56064=DIRECTION('ref_axis',(0.309016994374947,-0.951056516295154,0.)) ;
#56065=DIRECTION('center_axis',(0.,0.,-1.)) ;
#56066=DIRECTION('ref_axis',(0.587785252292473,-0.809016994374947,0.)) ;
#56067=DIRECTION('center_axis',(0.,0.,-1.)) ;
#56068=DIRECTION('ref_axis',(0.587785252292473,-0.809016994374947,0.)) ;
#56069=DIRECTION('center_axis',(0.,0.,-1.)) ;
#56070=DIRECTION('ref_axis',(0.809016994374947,-0.587785252292473,0.)) ;
#56071=DIRECTION('center_axis',(0.,0.,-1.)) ;
#56072=DIRECTION('ref_axis',(0.809016994374947,-0.587785252292473,0.)) ;
#56073=DIRECTION('center_axis',(0.,0.,-1.)) ;
#56074=DIRECTION('ref_axis',(0.951056516295154,-0.309016994374947,0.)) ;
#56075=DIRECTION('center_axis',(0.,0.,-1.)) ;
#56076=DIRECTION('ref_axis',(0.951056516295154,-0.309016994374947,0.)) ;
#56077=DIRECTION('center_axis',(0.,0.,-1.)) ;
#56078=DIRECTION('ref_axis',(1.,0.,0.)) ;
#56079=DIRECTION('center_axis',(0.,0.,-1.)) ;
#56080=DIRECTION('ref_axis',(1.,0.,0.)) ;
#56081=DIRECTION('center_axis',(0.,0.,-1.)) ;
#56082=DIRECTION('ref_axis',(0.951056516295154,0.309016994374948,0.)) ;
#56083=DIRECTION('center_axis',(0.,0.,-1.)) ;
#56084=DIRECTION('ref_axis',(0.951056516295154,0.309016994374948,0.)) ;
#56085=DIRECTION('center_axis',(0.,0.,-1.)) ;
#56086=DIRECTION('ref_axis',(0.809016994374947,0.587785252292473,0.)) ;
#56087=DIRECTION('center_axis',(0.,0.,-1.)) ;
#56088=DIRECTION('ref_axis',(0.809016994374947,0.587785252292473,0.)) ;
#56089=DIRECTION('center_axis',(0.,0.,-1.)) ;
#56090=DIRECTION('ref_axis',(0.587785252292473,0.809016994374947,0.)) ;
#56091=DIRECTION('center_axis',(0.,0.,-1.)) ;
#56092=DIRECTION('ref_axis',(0.587785252292473,0.809016994374947,0.)) ;
#56093=DIRECTION('center_axis',(0.,0.,-1.)) ;
#56094=DIRECTION('ref_axis',(0.309016994374947,0.951056516295154,0.)) ;
#56095=DIRECTION('center_axis',(0.,0.,-1.)) ;
#56096=DIRECTION('ref_axis',(0.309016994374947,0.951056516295154,0.)) ;
#56097=DIRECTION('center_axis',(0.,0.,-1.)) ;
#56098=DIRECTION('ref_axis',(-1.73472347597682E-16,1.,0.)) ;
#56099=DIRECTION('center_axis',(0.,0.,-1.)) ;
#56100=DIRECTION('ref_axis',(-1.73472347597682E-16,1.,0.)) ;
#56101=DIRECTION('center_axis',(0.,0.,-1.)) ;
#56102=DIRECTION('ref_axis',(-0.309016994374948,0.951056516295154,0.)) ;
#56103=DIRECTION('center_axis',(0.,0.,-1.)) ;
#56104=DIRECTION('ref_axis',(-0.309016994374948,0.951056516295154,0.)) ;
#56105=DIRECTION('center_axis',(0.,0.,-1.)) ;
#56106=DIRECTION('ref_axis',(-0.587785252292473,0.809016994374947,0.)) ;
#56107=DIRECTION('center_axis',(0.,0.,-1.)) ;
#56108=DIRECTION('ref_axis',(-0.587785252292473,0.809016994374947,0.)) ;
#56109=DIRECTION('center_axis',(0.,0.,-1.)) ;
#56110=DIRECTION('ref_axis',(-0.809016994374948,0.587785252292473,0.)) ;
#56111=DIRECTION('center_axis',(0.,0.,-1.)) ;
#56112=DIRECTION('ref_axis',(-0.809016994374948,0.587785252292473,0.)) ;
#56113=DIRECTION('center_axis',(0.,0.,-1.)) ;
#56114=DIRECTION('ref_axis',(-0.951056516295154,0.309016994374947,0.)) ;
#56115=DIRECTION('center_axis',(0.,0.,-1.)) ;
#56116=DIRECTION('ref_axis',(-0.951056516295154,0.309016994374947,0.)) ;
#56117=DIRECTION('center_axis',(0.,0.,-1.)) ;
#56118=DIRECTION('ref_axis',(-1.,-5.78241158658939E-17,0.)) ;
#56119=DIRECTION('center_axis',(0.,0.,-1.)) ;
#56120=DIRECTION('ref_axis',(-1.,-5.78241158658939E-17,0.)) ;
#56121=DIRECTION('center_axis',(0.,0.,-1.)) ;
#56122=DIRECTION('ref_axis',(-0.951056516295154,-0.309016994374947,0.)) ;
#56123=DIRECTION('center_axis',(0.,0.,-1.)) ;
#56124=DIRECTION('ref_axis',(-0.951056516295154,-0.309016994374947,0.)) ;
#56125=DIRECTION('center_axis',(0.,0.,1.)) ;
#56126=DIRECTION('ref_axis',(1.,0.,0.)) ;
#56127=DIRECTION('',(0.52999894000318,6.49061505426385E-17,-0.847998304005088)) ;
#56128=DIRECTION('center_axis',(0.,-1.67304619266744E-15,-1.)) ;
#56129=DIRECTION('ref_axis',(1.,0.,0.)) ;
#56130=DIRECTION('center_axis',(0.,0.,-1.)) ;
#56131=DIRECTION('ref_axis',(-1.,0.,0.)) ;
#56132=DIRECTION('center_axis',(0.,-1.,0.)) ;
#56133=DIRECTION('ref_axis',(-1.,0.,0.)) ;
#56134=DIRECTION('center_axis',(0.,0.,1.)) ;
#56135=DIRECTION('ref_axis',(-0.707106781186564,-0.707106781186531,0.)) ;
#56136=DIRECTION('center_axis',(-1.,0.,0.)) ;
#56137=DIRECTION('ref_axis',(0.,0.,-1.)) ;
#56138=DIRECTION('center_axis',(0.,0.,-1.)) ;
#56139=DIRECTION('ref_axis',(1.,0.,0.)) ;
#56140=DIRECTION('center_axis',(0.,0.,1.)) ;
#56141=DIRECTION('ref_axis',(1.,0.,0.)) ;
#56142=DIRECTION('',(1.26882631385732E-15,-1.,0.)) ;
#56143=DIRECTION('center_axis',(0.,0.,-1.)) ;
#56144=DIRECTION('ref_axis',(0.707106781186548,0.707106781186548,0.)) ;
#56145=DIRECTION('',(1.,0.,0.)) ;
#56146=DIRECTION('center_axis',(0.,0.,-1.)) ;
#56147=DIRECTION('ref_axis',(-0.707106781186548,0.707106781186548,0.)) ;
#56148=DIRECTION('',(0.,1.,0.)) ;
#56149=DIRECTION('center_axis',(0.,0.,1.)) ;
#56150=DIRECTION('ref_axis',(0.707106781186564,-0.707106781186531,0.)) ;
#56151=DIRECTION('',(1.,0.,0.)) ;
#56152=DIRECTION('center_axis',(0.,0.,-1.)) ;
#56153=DIRECTION('ref_axis',(-0.707106781186548,0.707106781186548,0.)) ;
#56154=DIRECTION('',(7.40148683083432E-15,1.,0.)) ;
#56155=DIRECTION('center_axis',(0.,0.,-1.)) ;
#56156=DIRECTION('ref_axis',(-0.707106781186548,-0.707106781186548,0.)) ;
#56157=DIRECTION('',(-1.,0.,0.)) ;
#56158=DIRECTION('center_axis',(0.,0.,1.)) ;
#56159=DIRECTION('ref_axis',(0.707106781186531,0.707106781186564,0.)) ;
#56160=DIRECTION('',(0.,1.,0.)) ;
#56161=DIRECTION('center_axis',(0.,0.,-1.)) ;
#56162=DIRECTION('ref_axis',(-0.707106781186548,-0.707106781186548,0.)) ;
#56163=DIRECTION('',(-1.,-2.96059473233375E-14,0.)) ;
#56164=DIRECTION('center_axis',(0.,0.,-1.)) ;
#56165=DIRECTION('ref_axis',(0.70710678118661,-0.707106781186485,0.)) ;
#56166=DIRECTION('',(1.26882631385732E-15,-1.,0.)) ;
#56167=DIRECTION('center_axis',(0.,0.,1.)) ;
#56168=DIRECTION('ref_axis',(-0.707106781186539,0.707106781186556,0.)) ;
#56169=DIRECTION('',(-1.,0.,0.)) ;
#56170=DIRECTION('center_axis',(0.,0.,-1.)) ;
#56171=DIRECTION('ref_axis',(0.707106781186548,-0.707106781186548,0.)) ;
#56172=DIRECTION('',(0.,-1.,0.)) ;
#56173=DIRECTION('center_axis',(0.,0.,-1.)) ;
#56174=DIRECTION('ref_axis',(0.707106781186548,0.707106781186548,0.)) ;
#56175=DIRECTION('',(1.,0.,0.)) ;
#56176=DIRECTION('center_axis',(-1.26882631385732E-15,1.,0.)) ;
#56177=DIRECTION('ref_axis',(-0.70710678118654,-8.97195690676432E-16,-0.707106781186555)) ;
#56178=DIRECTION('',(-1.26882631385732E-15,1.,0.)) ;
#56179=DIRECTION('center_axis',(0.,-1.,0.)) ;
#56180=DIRECTION('ref_axis',(-1.,0.,0.)) ;
#56181=DIRECTION('center_axis',(1.,1.26882631385732E-15,0.)) ;
#56182=DIRECTION('ref_axis',(1.26882631385732E-15,-1.,0.)) ;
#56183=DIRECTION('',(0.,0.,1.)) ;
#56184=DIRECTION('center_axis',(0.,0.,-1.)) ;
#56185=DIRECTION('ref_axis',(-1.,0.,0.)) ;
#56186=DIRECTION('center_axis',(-1.,0.,0.)) ;
#56187=DIRECTION('ref_axis',(0.,1.,0.)) ;
#56188=DIRECTION('center_axis',(0.,1.,0.)) ;
#56189=DIRECTION('ref_axis',(-4.44089209850062E-14,0.,-1.)) ;
#56190=DIRECTION('center_axis',(1.,0.,0.)) ;
#56191=DIRECTION('ref_axis',(0.,0.707106781186602,-0.707106781186493)) ;
#56192=DIRECTION('center_axis',(-1.,0.,0.)) ;
#56193=DIRECTION('ref_axis',(0.,1.,0.)) ;
#56194=DIRECTION('center_axis',(0.,0.,-1.)) ;
#56195=DIRECTION('ref_axis',(-1.,0.,0.)) ;
#56196=DIRECTION('center_axis',(1.,0.,0.)) ;
#56197=DIRECTION('ref_axis',(0.,-1.,0.)) ;
#56198=DIRECTION('center_axis',(0.,-1.,0.)) ;
#56199=DIRECTION('ref_axis',(4.44089209850062E-14,0.,-1.)) ;
#56200=DIRECTION('center_axis',(0.,0.,-1.)) ;
#56201=DIRECTION('ref_axis',(0.707106781186564,-0.707106781186531,0.)) ;
#56202=DIRECTION('center_axis',(0.,0.,-1.)) ;
#56203=DIRECTION('ref_axis',(0.707106781186548,-0.707106781186548,0.)) ;
#56204=DIRECTION('',(0.,0.,-1.)) ;
#56205=DIRECTION('',(0.,0.,1.)) ;
#56206=DIRECTION('center_axis',(-1.,0.,0.)) ;
#56207=DIRECTION('ref_axis',(0.,-0.707106781186477,-0.707106781186618)) ;
#56208=DIRECTION('',(-1.,0.,0.)) ;
#56209=DIRECTION('center_axis',(1.,0.,0.)) ;
#56210=DIRECTION('ref_axis',(0.,-1.,0.)) ;
#56211=DIRECTION('center_axis',(0.,1.,0.)) ;
#56212=DIRECTION('ref_axis',(1.,0.,0.)) ;
#56213=DIRECTION('',(0.,0.,1.)) ;
#56214=DIRECTION('center_axis',(0.,0.,-1.)) ;
#56215=DIRECTION('ref_axis',(-1.,0.,0.)) ;
#56216=DIRECTION('center_axis',(0.,1.,0.)) ;
#56217=DIRECTION('ref_axis',(1.,0.,0.)) ;
#56218=DIRECTION('center_axis',(1.,0.,0.)) ;
#56219=DIRECTION('ref_axis',(0.,0.,-1.)) ;
#56220=DIRECTION('center_axis',(0.,0.,-1.)) ;
#56221=DIRECTION('ref_axis',(0.707106781186531,0.707106781186564,0.)) ;
#56222=DIRECTION('center_axis',(0.,0.,-1.)) ;
#56223=DIRECTION('ref_axis',(0.707106781186548,0.707106781186548,0.)) ;
#56224=DIRECTION('',(0.,0.,1.)) ;
#56225=DIRECTION('center_axis',(0.,-1.,0.)) ;
#56226=DIRECTION('ref_axis',(0.70710678118654,0.,-0.707106781186555)) ;
#56227=DIRECTION('center_axis',(0.,1.,0.)) ;
#56228=DIRECTION('ref_axis',(1.,0.,0.)) ;
#56229=DIRECTION('center_axis',(0.,0.,1.)) ;
#56230=DIRECTION('ref_axis',(1.,0.,0.)) ;
#56231=DIRECTION('center_axis',(0.,-1.,0.)) ;
#56232=DIRECTION('ref_axis',(-1.,0.,0.)) ;
#56233=DIRECTION('center_axis',(0.,0.,-1.)) ;
#56234=DIRECTION('ref_axis',(-1.,0.,0.)) ;
#56235=DIRECTION('center_axis',(0.,1.,0.)) ;
#56236=DIRECTION('ref_axis',(0.,0.,-1.)) ;
#56237=DIRECTION('center_axis',(0.,0.,-1.)) ;
#56238=DIRECTION('ref_axis',(-1.,0.,0.)) ;
#56239=DIRECTION('center_axis',(0.,-1.,0.)) ;
#56240=DIRECTION('ref_axis',(-1.,0.,0.)) ;
#56241=DIRECTION('center_axis',(-1.,0.,0.)) ;
#56242=DIRECTION('ref_axis',(0.,0.,-1.)) ;
#56243=DIRECTION('center_axis',(0.,1.,0.)) ;
#56244=DIRECTION('ref_axis',(-0.70710678118654,0.,-0.707106781186555)) ;
#56245=DIRECTION('center_axis',(0.,0.,1.)) ;
#56246=DIRECTION('ref_axis',(1.,0.,0.)) ;
#56247=DIRECTION('center_axis',(0.,1.,0.)) ;
#56248=DIRECTION('ref_axis',(0.,0.,-1.)) ;
#56249=DIRECTION('center_axis',(-1.,-4.44089209850072E-14,0.)) ;
#56250=DIRECTION('ref_axis',(-4.44089209850072E-14,1.,0.)) ;
#56251=DIRECTION('center_axis',(-1.26882631385732E-15,1.,0.)) ;
#56252=DIRECTION('ref_axis',(-0.70710678118654,-8.97195690676432E-16,-0.707106781186555)) ;
#56253=DIRECTION('center_axis',(-1.,0.,0.)) ;
#56254=DIRECTION('ref_axis',(0.,-0.707106781186477,-0.707106781186618)) ;
#56255=DIRECTION('center_axis',(0.,0.,-1.)) ;
#56256=DIRECTION('ref_axis',(-1.,0.,0.)) ;
#56257=DIRECTION('center_axis',(1.,4.44089209850072E-14,0.)) ;
#56258=DIRECTION('ref_axis',(0.,0.,-1.)) ;
#56259=DIRECTION('center_axis',(0.,0.,-1.)) ;
#56260=DIRECTION('ref_axis',(-1.,0.,0.)) ;
#56261=DIRECTION('center_axis',(0.,0.,1.)) ;
#56262=DIRECTION('ref_axis',(0.,1.,0.)) ;
#56263=DIRECTION('center_axis',(-1.,0.,0.)) ;
#56264=DIRECTION('ref_axis',(0.,0.,-1.)) ;
#56265=DIRECTION('center_axis',(0.,0.,-1.)) ;
#56266=DIRECTION('ref_axis',(0.70710678118661,0.707106781186485,0.)) ;
#56267=DIRECTION('',(0.,0.,-1.)) ;
#56268=DIRECTION('center_axis',(0.,0.,-1.)) ;
#56269=DIRECTION('ref_axis',(-1.,0.,0.)) ;
#56270=DIRECTION('center_axis',(1.,0.,0.)) ;
#56271=DIRECTION('ref_axis',(0.,-1.,0.)) ;
#56272=DIRECTION('center_axis',(0.,0.,1.)) ;
#56273=DIRECTION('ref_axis',(-1.,0.,0.)) ;
#56274=DIRECTION('center_axis',(0.,-1.,0.)) ;
#56275=DIRECTION('ref_axis',(0.,0.,-1.)) ;
#56276=DIRECTION('center_axis',(-1.,0.,0.)) ;
#56277=DIRECTION('ref_axis',(0.,-0.707106781186477,-0.707106781186618)) ;
#56278=DIRECTION('',(-1.,0.,0.)) ;
#56279=DIRECTION('center_axis',(0.,0.,-1.)) ;
#56280=DIRECTION('ref_axis',(-0.70710678118661,0.707106781186485,0.)) ;
#56281=DIRECTION('',(0.,0.,-1.)) ;
#56282=DIRECTION('',(0.,0.,1.)) ;
#56283=DIRECTION('center_axis',(0.,0.,-1.)) ;
#56284=DIRECTION('ref_axis',(-1.,0.,0.)) ;
#56285=DIRECTION('center_axis',(0.,1.,0.)) ;
#56286=DIRECTION('ref_axis',(1.,0.,0.)) ;
#56287=DIRECTION('center_axis',(0.,0.,1.)) ;
#56288=DIRECTION('ref_axis',(0.,-1.,0.)) ;
#56289=DIRECTION('center_axis',(1.,0.,0.)) ;
#56290=DIRECTION('ref_axis',(0.,0.,-1.)) ;
#56291=DIRECTION('center_axis',(0.,-1.,0.)) ;
#56292=DIRECTION('ref_axis',(0.70710678118654,0.,-0.707106781186555)) ;
#56293=DIRECTION('',(0.,-1.,0.)) ;
#56294=DIRECTION('center_axis',(0.,0.,-1.)) ;
#56295=DIRECTION('ref_axis',(-1.,0.,0.)) ;
#56296=DIRECTION('center_axis',(0.,0.,1.)) ;
#56297=DIRECTION('ref_axis',(-1.,0.,0.)) ;
#56298=DIRECTION('center_axis',(0.,-1.,0.)) ;
#56299=DIRECTION('ref_axis',(0.,0.,-1.)) ;
#56300=DIRECTION('center_axis',(0.,0.,-1.)) ;
#56301=DIRECTION('ref_axis',(-0.70710678118661,0.707106781186485,0.)) ;
#56302=DIRECTION('',(0.,0.,-1.)) ;
#56303=DIRECTION('center_axis',(-7.40148683083432E-15,-1.,0.)) ;
#56304=DIRECTION('ref_axis',(0.70710678118654,-5.23364152894582E-15,-0.707106781186555)) ;
#56305=DIRECTION('',(-7.40148683083432E-15,-1.,0.)) ;
#56306=DIRECTION('center_axis',(0.,0.,-1.)) ;
#56307=DIRECTION('ref_axis',(-0.707106781186485,-0.70710678118661,0.)) ;
#56308=DIRECTION('',(0.,0.,-1.)) ;
#56309=DIRECTION('',(0.,0.,1.)) ;
#56310=DIRECTION('center_axis',(1.,0.,0.)) ;
#56311=DIRECTION('ref_axis',(0.,0.707106781186602,-0.707106781186493)) ;
#56312=DIRECTION('',(1.,0.,0.)) ;
#56313=DIRECTION('center_axis',(1.,2.96059473233375E-14,0.)) ;
#56314=DIRECTION('ref_axis',(-2.09345661157853E-14,0.707106781186602,-0.707106781186493)) ;
#56315=DIRECTION('center_axis',(0.,0.,-1.)) ;
#56316=DIRECTION('ref_axis',(0.951056516295153,0.309016994374948,0.)) ;
#56317=DIRECTION('center_axis',(0.,0.,-1.)) ;
#56318=DIRECTION('ref_axis',(0.809016994374947,0.587785252292473,0.)) ;
#56319=DIRECTION('center_axis',(0.,0.,-1.)) ;
#56320=DIRECTION('ref_axis',(0.587785252292473,0.809016994374948,0.)) ;
#56321=DIRECTION('center_axis',(0.,0.,-1.)) ;
#56322=DIRECTION('ref_axis',(0.309016994374947,0.951056516295154,0.)) ;
#56323=DIRECTION('center_axis',(0.,0.,-1.)) ;
#56324=DIRECTION('ref_axis',(-2.22044604925031E-16,1.,0.)) ;
#56325=DIRECTION('center_axis',(0.,0.,-1.)) ;
#56326=DIRECTION('ref_axis',(-0.309016994374948,0.951056516295153,0.)) ;
#56327=DIRECTION('center_axis',(0.,0.,-1.)) ;
#56328=DIRECTION('ref_axis',(-0.587785252292473,0.809016994374947,0.)) ;
#56329=DIRECTION('center_axis',(0.,0.,-1.)) ;
#56330=DIRECTION('ref_axis',(-0.809016994374947,0.587785252292473,0.)) ;
#56331=DIRECTION('center_axis',(0.,0.,-1.)) ;
#56332=DIRECTION('ref_axis',(-0.951056516295154,0.309016994374947,0.)) ;
#56333=DIRECTION('center_axis',(0.,0.,-1.)) ;
#56334=DIRECTION('ref_axis',(-1.,-1.11022302462516E-16,0.)) ;
#56335=DIRECTION('center_axis',(0.,0.,-1.)) ;
#56336=DIRECTION('ref_axis',(-0.951056516295154,-0.309016994374948,0.)) ;
#56337=DIRECTION('center_axis',(0.,0.,-1.)) ;
#56338=DIRECTION('ref_axis',(-0.809016994374947,-0.587785252292473,0.)) ;
#56339=DIRECTION('center_axis',(0.,0.,-1.)) ;
#56340=DIRECTION('ref_axis',(-0.587785252292473,-0.809016994374947,0.)) ;
#56341=DIRECTION('center_axis',(0.,0.,-1.)) ;
#56342=DIRECTION('ref_axis',(-0.309016994374947,-0.951056516295154,0.)) ;
#56343=DIRECTION('center_axis',(0.,0.,-1.)) ;
#56344=DIRECTION('ref_axis',(5.55111512312578E-17,-1.,0.)) ;
#56345=DIRECTION('center_axis',(0.,0.,-1.)) ;
#56346=DIRECTION('ref_axis',(0.309016994374948,-0.951056516295154,0.)) ;
#56347=DIRECTION('center_axis',(0.,0.,-1.)) ;
#56348=DIRECTION('ref_axis',(0.587785252292473,-0.809016994374947,0.)) ;
#56349=DIRECTION('center_axis',(0.,0.,-1.)) ;
#56350=DIRECTION('ref_axis',(0.809016994374947,-0.587785252292473,0.)) ;
#56351=DIRECTION('center_axis',(0.,0.,-1.)) ;
#56352=DIRECTION('ref_axis',(0.951056516295154,-0.309016994374947,0.)) ;
#56353=DIRECTION('center_axis',(0.,0.,-1.)) ;
#56354=DIRECTION('ref_axis',(1.,0.,0.)) ;
#56355=DIRECTION('center_axis',(-1.,0.,0.)) ;
#56356=DIRECTION('ref_axis',(0.,1.,0.)) ;
#56357=DIRECTION('center_axis',(-1.,7.40148683083432E-15,0.)) ;
#56358=DIRECTION('ref_axis',(7.40148683083432E-15,1.,0.)) ;
#56359=DIRECTION('center_axis',(0.,-1.,0.)) ;
#56360=DIRECTION('ref_axis',(-1.,0.,0.)) ;
#56361=DIRECTION('center_axis',(0.,1.,0.)) ;
#56362=DIRECTION('ref_axis',(1.,0.,0.)) ;
#69886=CARTESIAN_POINT('',(0.,0.,0.)) ;
#69887=CARTESIAN_POINT('Origin',(74.5283628290597,239.4,18.3213203435596)) ;
#69888=CARTESIAN_POINT('',(68.7283628290597,239.4,18.5213203435596)) ;
#69889=CARTESIAN_POINT('Origin',(74.5283628290597,239.4,18.5213203435596)) ;
#69890=CARTESIAN_POINT('',(68.5283628290597,239.4,18.3213203435596)) ;
#69891=CARTESIAN_POINT('Origin',(68.7283628290597,239.4,18.3213203435596)) ;
#69892=CARTESIAN_POINT('Origin',(74.5283628290597,239.4,18.3213203435596)) ;
#69893=CARTESIAN_POINT('Origin',(74.5283628290597,239.4,16.0213203435596)) ;
#69894=CARTESIAN_POINT('',(68.5283628290597,239.4,16.2213203435596)) ;
#69895=CARTESIAN_POINT('',(68.5283628290597,239.4,16.0213203435596)) ;
#69896=CARTESIAN_POINT('',(68.5800869669907,238.61386116447,16.2213203435596)) ;
#69897=CARTESIAN_POINT('Origin',(74.5283628290597,239.4,16.2213203435596)) ;
#69898=CARTESIAN_POINT('',(68.5800869669907,238.61386116447,7.2786795888419)) ;
#69899=CARTESIAN_POINT('',(68.5800869669907,238.61386116447,16.0213203435596)) ;
#69900=CARTESIAN_POINT('',(68.6282860496011,238.309544133633,7.2786795888419)) ;
#69901=CARTESIAN_POINT('Origin',(74.5283628290597,239.4,7.2786795888419)) ;
#69902=CARTESIAN_POINT('',(68.6282860496011,238.309544133633,16.2213203435596)) ;
#69903=CARTESIAN_POINT('',(68.6282860496011,238.309544133633,16.0213203435596)) ;
#69904=CARTESIAN_POINT('',(69.1141465698346,236.814219209147,16.2213203435596)) ;
#69905=CARTESIAN_POINT('Origin',(74.5283628290597,239.4,16.2213203435596)) ;
#69906=CARTESIAN_POINT('',(69.1141465698346,236.814219209147,7.2786795888419)) ;
#69907=CARTESIAN_POINT('',(69.1141465698346,236.814219209147,16.0213203435596)) ;
#69908=CARTESIAN_POINT('',(69.254025755637,236.53969084959,7.2786795888419)) ;
#69909=CARTESIAN_POINT('Origin',(74.5283628290597,239.4,7.2786795888419)) ;
#69910=CARTESIAN_POINT('',(69.254025755637,236.53969084959,16.2213203435596)) ;
#69911=CARTESIAN_POINT('',(69.254025755637,236.53969084959,16.0213203435596)) ;
#69912=CARTESIAN_POINT('',(70.1781873831942,235.267691493827,16.2213203435596)) ;
#69913=CARTESIAN_POINT('Origin',(74.5283628290597,239.4,16.2213203435596)) ;
#69914=CARTESIAN_POINT('',(70.1781873831942,235.267691493827,7.2786795888419)) ;
#69915=CARTESIAN_POINT('',(70.1781873831942,235.267691493827,16.0213203435596)) ;
#69916=CARTESIAN_POINT('',(70.3960543228867,235.049824554134,7.2786795888419)) ;
#69917=CARTESIAN_POINT('Origin',(74.5283628290597,239.4,7.2786795888419)) ;
#69918=CARTESIAN_POINT('',(70.3960543228867,235.049824554134,16.2213203435596)) ;
#69919=CARTESIAN_POINT('',(70.3960543228867,235.049824554134,16.0213203435596)) ;
#69920=CARTESIAN_POINT('',(71.6680536786498,234.125662926577,16.2213203435596)) ;
#69921=CARTESIAN_POINT('Origin',(74.5283628290597,239.4,16.2213203435596)) ;
#69922=CARTESIAN_POINT('',(71.6680536786497,234.125662926577,7.2786795888419)) ;
#69923=CARTESIAN_POINT('',(71.6680536786497,234.125662926577,16.0213203435596)) ;
#69924=CARTESIAN_POINT('',(71.942582038207,233.985783740775,7.2786795888419)) ;
#69925=CARTESIAN_POINT('Origin',(74.5283628290597,239.4,7.2786795888419)) ;
#69926=CARTESIAN_POINT('',(71.942582038207,233.985783740775,16.2213203435596)) ;
#69927=CARTESIAN_POINT('',(71.942582038207,233.985783740775,16.0213203435596)) ;
#69928=CARTESIAN_POINT('',(73.4379069626931,233.499923220541,16.2213203435596)) ;
#69929=CARTESIAN_POINT('Origin',(74.5283628290597,239.4,16.2213203435596)) ;
#69930=CARTESIAN_POINT('',(73.4379069626931,233.499923220541,7.2786795888419)) ;
#69931=CARTESIAN_POINT('',(73.4379069626931,233.499923220541,16.0213203435596)) ;
#69932=CARTESIAN_POINT('',(73.7422239935301,233.451724137931,7.2786795888419)) ;
#69933=CARTESIAN_POINT('Origin',(74.5283628290597,239.4,7.2786795888419)) ;
#69934=CARTESIAN_POINT('',(73.7422239935301,233.451724137931,16.2213203435596)) ;
#69935=CARTESIAN_POINT('',(73.7422239935301,233.451724137931,16.0213203435596)) ;
#69936=CARTESIAN_POINT('',(75.3145016645892,233.451724137931,16.2213203435596)) ;
#69937=CARTESIAN_POINT('Origin',(74.5283628290597,239.4,16.2213203435596)) ;
#69938=CARTESIAN_POINT('',(75.3145016645892,233.451724137931,7.2786795888419)) ;
#69939=CARTESIAN_POINT('',(75.3145016645892,233.451724137931,16.0213203435596)) ;
#69940=CARTESIAN_POINT('',(75.6188186954263,233.499923220541,7.2786795888419)) ;
#69941=CARTESIAN_POINT('Origin',(74.5283628290597,239.4,7.2786795888419)) ;
#69942=CARTESIAN_POINT('',(75.6188186954263,233.499923220541,16.2213203435596)) ;
#69943=CARTESIAN_POINT('',(75.6188186954263,233.499923220541,16.0213203435596)) ;
#69944=CARTESIAN_POINT('',(77.1141436199124,233.985783740775,16.2213203435596)) ;
#69945=CARTESIAN_POINT('Origin',(74.5283628290597,239.4,16.2213203435596)) ;
#69946=CARTESIAN_POINT('',(77.1141436199123,233.985783740775,7.2786795888419)) ;
#69947=CARTESIAN_POINT('',(77.1141436199123,233.985783740775,16.0213203435596)) ;
#69948=CARTESIAN_POINT('',(77.3886719794696,234.125662926577,7.2786795888419)) ;
#69949=CARTESIAN_POINT('Origin',(74.5283628290597,239.4,7.2786795888419)) ;
#69950=CARTESIAN_POINT('',(77.3886719794696,234.125662926577,16.2213203435596)) ;
#69951=CARTESIAN_POINT('',(77.3886719794696,234.125662926577,16.0213203435596)) ;
#69952=CARTESIAN_POINT('',(78.6606713352326,235.049824554134,16.2213203435596)) ;
#69953=CARTESIAN_POINT('Origin',(74.5283628290597,239.4,16.2213203435596)) ;
#69954=CARTESIAN_POINT('',(78.6606713352326,235.049824554134,7.2786795888419)) ;
#69955=CARTESIAN_POINT('',(78.6606713352326,235.049824554134,16.0213203435596)) ;
#69956=CARTESIAN_POINT('',(78.8785382749251,235.267691493827,7.2786795888419)) ;
#69957=CARTESIAN_POINT('Origin',(74.5283628290597,239.4,7.2786795888419)) ;
#69958=CARTESIAN_POINT('',(78.8785382749251,235.267691493827,16.2213203435596)) ;
#69959=CARTESIAN_POINT('',(78.8785382749251,235.267691493827,16.0213203435596)) ;
#69960=CARTESIAN_POINT('',(79.8026999024824,236.53969084959,16.2213203435596)) ;
#69961=CARTESIAN_POINT('Origin',(74.5283628290597,239.4,16.2213203435596)) ;
#69962=CARTESIAN_POINT('',(79.8026999024824,236.53969084959,7.2786795888419)) ;
#69963=CARTESIAN_POINT('',(79.8026999024824,236.53969084959,16.0213203435596)) ;
#69964=CARTESIAN_POINT('',(79.9425790882848,236.814219209147,7.2786795888419)) ;
#69965=CARTESIAN_POINT('Origin',(74.5283628290597,239.4,7.2786795888419)) ;
#69966=CARTESIAN_POINT('',(79.9425790882848,236.814219209147,16.2213203435596)) ;
#69967=CARTESIAN_POINT('',(79.9425790882848,236.814219209147,16.0213203435596)) ;
#69968=CARTESIAN_POINT('',(80.4284396085183,238.309544133633,16.2213203435596)) ;
#69969=CARTESIAN_POINT('Origin',(74.5283628290597,239.4,16.2213203435596)) ;
#69970=CARTESIAN_POINT('',(80.4284396085183,238.309544133633,7.2786795888419)) ;
#69971=CARTESIAN_POINT('',(80.4284396085183,238.309544133633,16.0213203435596)) ;
#69972=CARTESIAN_POINT('',(80.4766386911286,238.61386116447,7.2786795888419)) ;
#69973=CARTESIAN_POINT('Origin',(74.5283628290597,239.4,7.2786795888419)) ;
#69974=CARTESIAN_POINT('',(80.4766386911286,238.61386116447,16.2213203435596)) ;
#69975=CARTESIAN_POINT('',(80.4766386911286,238.61386116447,16.0213203435596)) ;
#69976=CARTESIAN_POINT('',(80.4766386911286,240.186138835529,16.2213203435596)) ;
#69977=CARTESIAN_POINT('Origin',(74.5283628290597,239.4,16.2213203435596)) ;
#69978=CARTESIAN_POINT('',(80.4766386911286,240.186138835529,7.2786795888419)) ;
#69979=CARTESIAN_POINT('',(80.4766386911286,240.186138835529,16.0213203435596)) ;
#69980=CARTESIAN_POINT('',(80.4284396085183,240.490455866367,7.2786795888419)) ;
#69981=CARTESIAN_POINT('Origin',(74.5283628290597,239.4,7.2786795888419)) ;
#69982=CARTESIAN_POINT('',(80.4284396085183,240.490455866367,16.2213203435596)) ;
#69983=CARTESIAN_POINT('',(80.4284396085183,240.490455866367,16.0213203435596)) ;
#69984=CARTESIAN_POINT('',(79.9425790882847,241.985780790853,16.2213203435596)) ;
#69985=CARTESIAN_POINT('Origin',(74.5283628290597,239.4,16.2213203435596)) ;
#69986=CARTESIAN_POINT('',(79.9425790882848,241.985780790853,7.2786795888419)) ;
#69987=CARTESIAN_POINT('',(79.9425790882848,241.985780790853,16.0213203435596)) ;
#69988=CARTESIAN_POINT('',(79.8026999024823,242.26030915041,7.2786795888419)) ;
#69989=CARTESIAN_POINT('Origin',(74.5283628290597,239.4,7.2786795888419)) ;
#69990=CARTESIAN_POINT('',(79.8026999024823,242.26030915041,16.2213203435596)) ;
#69991=CARTESIAN_POINT('',(79.8026999024823,242.26030915041,16.0213203435596)) ;
#69992=CARTESIAN_POINT('',(78.8785382749251,243.532308506173,16.2213203435596)) ;
#69993=CARTESIAN_POINT('Origin',(74.5283628290597,239.4,16.2213203435596)) ;
#69994=CARTESIAN_POINT('',(78.8785382749251,243.532308506173,7.2786795888419)) ;
#69995=CARTESIAN_POINT('',(78.8785382749251,243.532308506173,16.0213203435596)) ;
#69996=CARTESIAN_POINT('',(78.6606713352326,243.750175445865,7.2786795888419)) ;
#69997=CARTESIAN_POINT('Origin',(74.5283628290597,239.4,7.2786795888419)) ;
#69998=CARTESIAN_POINT('',(78.6606713352326,243.750175445865,16.2213203435596)) ;
#69999=CARTESIAN_POINT('',(78.6606713352326,243.750175445865,16.0213203435596)) ;
#70000=CARTESIAN_POINT('',(77.3886719794696,244.674337073423,16.2213203435596)) ;
#70001=CARTESIAN_POINT('Origin',(74.5283628290597,239.4,16.2213203435596)) ;
#70002=CARTESIAN_POINT('',(77.3886719794696,244.674337073423,7.2786795888419)) ;
#70003=CARTESIAN_POINT('',(77.3886719794696,244.674337073423,16.0213203435596)) ;
#70004=CARTESIAN_POINT('',(77.1141436199123,244.814216259225,7.2786795888419)) ;
#70005=CARTESIAN_POINT('Origin',(74.5283628290597,239.4,7.2786795888419)) ;
#70006=CARTESIAN_POINT('',(77.1141436199123,244.814216259225,16.2213203435596)) ;
#70007=CARTESIAN_POINT('',(77.1141436199123,244.814216259225,16.0213203435596)) ;
#70008=CARTESIAN_POINT('',(75.6188186954263,245.300076779458,16.2213203435596)) ;
#70009=CARTESIAN_POINT('Origin',(74.5283628290597,239.4,16.2213203435596)) ;
#70010=CARTESIAN_POINT('',(75.6188186954263,245.300076779458,7.2786795888419)) ;
#70011=CARTESIAN_POINT('',(75.6188186954263,245.300076779458,16.0213203435596)) ;
#70012=CARTESIAN_POINT('',(75.3145016645892,245.348275862069,7.2786795888419)) ;
#70013=CARTESIAN_POINT('Origin',(74.5283628290597,239.4,7.2786795888419)) ;
#70014=CARTESIAN_POINT('',(75.3145016645892,245.348275862069,16.2213203435596)) ;
#70015=CARTESIAN_POINT('',(75.3145016645892,245.348275862069,16.0213203435596)) ;
#70016=CARTESIAN_POINT('',(73.7422239935302,245.348275862069,16.2213203435596)) ;
#70017=CARTESIAN_POINT('Origin',(74.5283628290597,239.4,16.2213203435596)) ;
#70018=CARTESIAN_POINT('',(73.7422239935302,245.348275862069,7.2786795888419)) ;
#70019=CARTESIAN_POINT('',(73.7422239935302,245.348275862069,16.0213203435596)) ;
#70020=CARTESIAN_POINT('',(73.4379069626931,245.300076779459,7.2786795888419)) ;
#70021=CARTESIAN_POINT('Origin',(74.5283628290597,239.4,7.2786795888419)) ;
#70022=CARTESIAN_POINT('',(73.4379069626931,245.300076779459,16.2213203435596)) ;
#70023=CARTESIAN_POINT('',(73.4379069626931,245.300076779459,16.0213203435596)) ;
#70024=CARTESIAN_POINT('',(71.9425820382071,244.814216259225,16.2213203435596)) ;
#70025=CARTESIAN_POINT('Origin',(74.5283628290597,239.4,16.2213203435596)) ;
#70026=CARTESIAN_POINT('',(71.9425820382071,244.814216259225,7.2786795888419)) ;
#70027=CARTESIAN_POINT('',(71.9425820382071,244.814216259225,16.0213203435596)) ;
#70028=CARTESIAN_POINT('',(71.6680536786498,244.674337073423,7.2786795888419)) ;
#70029=CARTESIAN_POINT('Origin',(74.5283628290597,239.4,7.2786795888419)) ;
#70030=CARTESIAN_POINT('',(71.6680536786498,244.674337073423,16.2213203435596)) ;
#70031=CARTESIAN_POINT('',(71.6680536786498,244.674337073423,16.0213203435596)) ;
#70032=CARTESIAN_POINT('',(70.3960543228867,243.750175445865,16.2213203435596)) ;
#70033=CARTESIAN_POINT('Origin',(74.5283628290597,239.4,16.2213203435596)) ;
#70034=CARTESIAN_POINT('',(70.3960543228867,243.750175445865,7.2786795888419)) ;
#70035=CARTESIAN_POINT('',(70.3960543228867,243.750175445865,16.0213203435596)) ;
#70036=CARTESIAN_POINT('',(70.1781873831942,243.532308506173,7.2786795888419)) ;
#70037=CARTESIAN_POINT('Origin',(74.5283628290597,239.4,7.2786795888419)) ;
#70038=CARTESIAN_POINT('',(70.1781873831942,243.532308506173,16.2213203435596)) ;
#70039=CARTESIAN_POINT('',(70.1781873831942,243.532308506173,16.0213203435596)) ;
#70040=CARTESIAN_POINT('',(69.254025755637,242.26030915041,16.2213203435596)) ;
#70041=CARTESIAN_POINT('Origin',(74.5283628290597,239.4,16.2213203435596)) ;
#70042=CARTESIAN_POINT('',(69.254025755637,242.26030915041,7.2786795888419)) ;
#70043=CARTESIAN_POINT('',(69.254025755637,242.26030915041,16.0213203435596)) ;
#70044=CARTESIAN_POINT('',(69.1141465698346,241.985780790853,7.2786795888419)) ;
#70045=CARTESIAN_POINT('Origin',(74.5283628290597,239.4,7.2786795888419)) ;
#70046=CARTESIAN_POINT('',(69.1141465698346,241.985780790853,16.2213203435596)) ;
#70047=CARTESIAN_POINT('',(69.1141465698346,241.985780790853,16.0213203435596)) ;
#70048=CARTESIAN_POINT('',(68.6282860496011,240.490455866366,16.2213203435596)) ;
#70049=CARTESIAN_POINT('Origin',(74.5283628290597,239.4,16.2213203435596)) ;
#70050=CARTESIAN_POINT('',(68.6282860496011,240.490455866367,7.2786795888419)) ;
#70051=CARTESIAN_POINT('',(68.6282860496011,240.490455866367,16.0213203435596)) ;
#70052=CARTESIAN_POINT('',(68.5800869669907,240.186138835529,7.2786795888419)) ;
#70053=CARTESIAN_POINT('Origin',(74.5283628290597,239.4,7.2786795888419)) ;
#70054=CARTESIAN_POINT('',(68.5800869669907,240.186138835529,16.2213203435596)) ;
#70055=CARTESIAN_POINT('',(68.5800869669907,240.186138835529,16.0213203435596)) ;
#70056=CARTESIAN_POINT('Origin',(74.5283628290597,239.4,16.2213203435596)) ;
#70057=CARTESIAN_POINT('Origin',(74.5283628290597,239.4,18.5213203435596)) ;
#70058=CARTESIAN_POINT('Origin',(77.8283628290598,239.7,10.8213203435596)) ;
#70059=CARTESIAN_POINT('',(78.0283628290598,239.,10.8213203435596)) ;
#70060=CARTESIAN_POINT('',(77.8283628290598,239.,11.0213203435596)) ;
#70061=CARTESIAN_POINT('Origin',(77.8283628290598,239.,10.8213203435596)) ;
#70062=CARTESIAN_POINT('',(77.8283628290598,239.8,11.0213203435596)) ;
#70063=CARTESIAN_POINT('',(77.8283628290598,239.7,11.0213203435596)) ;
#70064=CARTESIAN_POINT('',(78.0283628290598,239.8,10.8213203435596)) ;
#70065=CARTESIAN_POINT('Origin',(77.8283628290598,239.8,10.8213203435596)) ;
#70066=CARTESIAN_POINT('',(78.0283628290598,239.7,10.8213203435596)) ;
#70067=CARTESIAN_POINT('Origin',(74.9283628290597,239.1,10.8213203435596)) ;
#70068=CARTESIAN_POINT('',(75.1283628290597,236.1,10.8213203435596)) ;
#70069=CARTESIAN_POINT('',(74.9283628290597,236.1,11.0213203435596)) ;
#70070=CARTESIAN_POINT('Origin',(74.9283628290597,236.1,10.8213203435596)) ;
#70071=CARTESIAN_POINT('',(74.9283628290597,237.85,11.0213203435596)) ;
#70072=CARTESIAN_POINT('',(74.9283628290597,239.1,11.0213203435596)) ;
#70073=CARTESIAN_POINT('',(75.1283628290597,237.85,10.8213203435596)) ;
#70074=CARTESIAN_POINT('Origin',(74.9283628290597,237.85,10.8213203435596)) ;
#70075=CARTESIAN_POINT('',(75.1283628290597,239.1,10.8213203435596)) ;
#70076=CARTESIAN_POINT('Origin',(76.0783628290597,237.85,10.8213203435596)) ;
#70077=CARTESIAN_POINT('',(76.0783628290597,239.,11.0213203435596)) ;
#70078=CARTESIAN_POINT('',(76.0783628290597,238.8,10.8213203435596)) ;
#70079=CARTESIAN_POINT('Origin',(76.0783628290597,239.,10.8213203435596)) ;
#70080=CARTESIAN_POINT('Origin',(76.0783628290597,237.85,10.8213203435596)) ;
#70081=CARTESIAN_POINT('Origin',(76.0783628290597,237.85,11.0213203435596)) ;
#70082=CARTESIAN_POINT('Origin',(76.2783628290598,239.,10.8213203435596)) ;
#70083=CARTESIAN_POINT('',(77.8283628290598,238.8,10.8213203435596)) ;
#70084=CARTESIAN_POINT('Origin',(77.8283628290598,239.,10.8213203435596)) ;
#70085=CARTESIAN_POINT('',(76.2783628290598,238.8,10.8213203435596)) ;
#70086=CARTESIAN_POINT('',(76.2783628290598,239.,11.0213203435596)) ;
#70087=CARTESIAN_POINT('Origin',(74.8283628290597,236.1,10.8213203435596)) ;
#70088=CARTESIAN_POINT('',(74.1283628290597,235.9,10.8213203435596)) ;
#70089=CARTESIAN_POINT('',(74.1283628290597,236.1,11.0213203435596)) ;
#70090=CARTESIAN_POINT('Origin',(74.1283628290597,236.1,10.8213203435596)) ;
#70091=CARTESIAN_POINT('',(74.8283628290597,236.1,11.0213203435596)) ;
#70092=CARTESIAN_POINT('',(74.9283628290597,235.9,10.8213203435596)) ;
#70093=CARTESIAN_POINT('Origin',(74.9283628290597,236.1,10.8213203435596)) ;
#70094=CARTESIAN_POINT('',(74.8283628290598,235.9,10.8213203435596)) ;
#70095=CARTESIAN_POINT('Origin',(74.2283628290597,239.,10.8213203435596)) ;
#70096=CARTESIAN_POINT('',(71.2283628290597,238.8,10.8213203435596)) ;
#70097=CARTESIAN_POINT('',(71.2283628290597,239.,11.0213203435596)) ;
#70098=CARTESIAN_POINT('Origin',(71.2283628290597,239.,10.8213203435596)) ;
#70099=CARTESIAN_POINT('',(72.9783628290596,239.,11.0213203435596)) ;
#70100=CARTESIAN_POINT('',(74.2283628290597,239.,11.0213203435596)) ;
#70101=CARTESIAN_POINT('',(72.9783628290596,238.8,10.8213203435596)) ;
#70102=CARTESIAN_POINT('Origin',(72.9783628290596,239.,10.8213203435596)) ;
#70103=CARTESIAN_POINT('',(74.2283628290597,238.8,10.8213203435596)) ;
#70104=CARTESIAN_POINT('Origin',(72.9783628290596,237.85,10.8213203435596)) ;
#70105=CARTESIAN_POINT('',(74.1283628290597,237.85,11.0213203435596)) ;
#70106=CARTESIAN_POINT('',(73.9283628290597,237.85,10.8213203435596)) ;
#70107=CARTESIAN_POINT('Origin',(74.1283628290597,237.85,10.8213203435596)) ;
#70108=CARTESIAN_POINT('Origin',(72.9783628290596,237.85,10.8213203435596)) ;
#70109=CARTESIAN_POINT('Origin',(72.9783628290596,237.85,11.0213203435596)) ;
#70110=CARTESIAN_POINT('Origin',(74.1283628290597,237.65,10.8213203435596)) ;
#70111=CARTESIAN_POINT('',(73.9283628290597,236.1,10.8213203435596)) ;
#70112=CARTESIAN_POINT('Origin',(74.1283628290597,236.1,10.8213203435596)) ;
#70113=CARTESIAN_POINT('',(73.9283628290597,237.65,10.8213203435596)) ;
#70114=CARTESIAN_POINT('',(74.1283628290597,237.65,11.0213203435596)) ;
#70115=CARTESIAN_POINT('Origin',(71.2283628290597,239.1,10.8213203435596)) ;
#70116=CARTESIAN_POINT('',(71.0283628290598,239.8,10.8213203435596)) ;
#70117=CARTESIAN_POINT('',(71.2283628290598,239.8,11.0213203435596)) ;
#70118=CARTESIAN_POINT('Origin',(71.2283628290598,239.8,10.8213203435596)) ;
#70119=CARTESIAN_POINT('',(71.2283628290597,239.1,11.0213203435596)) ;
#70120=CARTESIAN_POINT('',(71.0283628290597,239.,10.8213203435596)) ;
#70121=CARTESIAN_POINT('Origin',(71.2283628290597,239.,10.8213203435596)) ;
#70122=CARTESIAN_POINT('',(71.0283628290597,239.1,10.8213203435596)) ;
#70123=CARTESIAN_POINT('Origin',(74.1283628290597,239.7,10.8213203435596)) ;
#70124=CARTESIAN_POINT('',(73.9283628290597,242.7,10.8213203435596)) ;
#70125=CARTESIAN_POINT('',(74.1283628290597,242.7,11.0213203435596)) ;
#70126=CARTESIAN_POINT('Origin',(74.1283628290597,242.7,10.8213203435596)) ;
#70127=CARTESIAN_POINT('',(74.1283628290597,240.95,11.0213203435596)) ;
#70128=CARTESIAN_POINT('',(74.1283628290597,239.7,11.0213203435596)) ;
#70129=CARTESIAN_POINT('',(73.9283628290597,240.95,10.8213203435596)) ;
#70130=CARTESIAN_POINT('Origin',(74.1283628290597,240.95,10.8213203435596)) ;
#70131=CARTESIAN_POINT('',(73.9283628290597,239.7,10.8213203435596)) ;
#70132=CARTESIAN_POINT('Origin',(72.9783628290596,240.95,10.8213203435596)) ;
#70133=CARTESIAN_POINT('',(72.9783628290596,239.8,11.0213203435596)) ;
#70134=CARTESIAN_POINT('',(72.9783628290596,240.,10.8213203435596)) ;
#70135=CARTESIAN_POINT('Origin',(72.9783628290596,239.8,10.8213203435596)) ;
#70136=CARTESIAN_POINT('Origin',(72.9783628290596,240.95,10.8213203435596)) ;
#70137=CARTESIAN_POINT('Origin',(72.9783628290596,240.95,11.0213203435596)) ;
#70138=CARTESIAN_POINT('Origin',(72.7783628290598,239.8,10.8213203435596)) ;
#70139=CARTESIAN_POINT('',(71.2283628290598,240.,10.8213203435596)) ;
#70140=CARTESIAN_POINT('Origin',(71.2283628290598,239.8,10.8213203435596)) ;
#70141=CARTESIAN_POINT('',(72.7783628290598,240.,10.8213203435596)) ;
#70142=CARTESIAN_POINT('',(72.7783628290598,239.8,11.0213203435596)) ;
#70143=CARTESIAN_POINT('Origin',(74.2283628290597,242.7,10.8213203435596)) ;
#70144=CARTESIAN_POINT('',(74.9283628290597,242.9,10.8213203435596)) ;
#70145=CARTESIAN_POINT('',(74.9283628290597,242.7,11.0213203435596)) ;
#70146=CARTESIAN_POINT('Origin',(74.9283628290597,242.7,10.8213203435596)) ;
#70147=CARTESIAN_POINT('',(74.2283628290597,242.7,11.0213203435596)) ;
#70148=CARTESIAN_POINT('',(74.1283628290597,242.9,10.8213203435596)) ;
#70149=CARTESIAN_POINT('Origin',(74.1283628290597,242.7,10.8213203435596)) ;
#70150=CARTESIAN_POINT('',(74.2283628290597,242.9,10.8213203435596)) ;
#70151=CARTESIAN_POINT('Origin',(76.0783628290596,240.95,10.8213203435596)) ;
#70152=CARTESIAN_POINT('',(76.0783628290596,240.,10.8213203435596)) ;
#70153=CARTESIAN_POINT('',(76.0783628290596,239.8,11.0213203435596)) ;
#70154=CARTESIAN_POINT('Origin',(76.0783628290596,239.8,10.8213203435596)) ;
#70155=CARTESIAN_POINT('',(74.9283628290596,240.95,11.0213203435596)) ;
#70156=CARTESIAN_POINT('Origin',(76.0783628290596,240.95,11.0213203435596)) ;
#70157=CARTESIAN_POINT('',(75.1283628290596,240.95,10.8213203435596)) ;
#70158=CARTESIAN_POINT('Origin',(74.9283628290596,240.95,10.8213203435596)) ;
#70159=CARTESIAN_POINT('Origin',(76.0783628290596,240.95,10.8213203435596)) ;
#70160=CARTESIAN_POINT('Origin',(74.9283628290597,241.15,10.8213203435596)) ;
#70161=CARTESIAN_POINT('',(75.1283628290596,242.7,10.8213203435596)) ;
#70162=CARTESIAN_POINT('Origin',(74.9283628290597,242.7,10.8213203435596)) ;
#70163=CARTESIAN_POINT('',(75.1283628290596,241.15,10.8213203435596)) ;
#70164=CARTESIAN_POINT('',(74.9283628290597,241.15,11.0213203435596)) ;
#70165=CARTESIAN_POINT('Origin',(74.8283628290597,239.8,10.8213203435596)) ;
#70166=CARTESIAN_POINT('',(77.8283628290598,240.,10.8213203435596)) ;
#70167=CARTESIAN_POINT('Origin',(77.8283628290598,239.8,10.8213203435596)) ;
#70168=CARTESIAN_POINT('',(74.8283628290597,239.8,11.0213203435596)) ;
#70169=CARTESIAN_POINT('',(74.8283628290597,240.,10.8213203435596)) ;
#70170=CARTESIAN_POINT('Origin',(74.9283628290597,242.7,10.8213203435596)) ;
#70171=CARTESIAN_POINT('Origin',(74.9283628290597,242.7,10.8213203435596)) ;
#70172=CARTESIAN_POINT('Origin',(74.1283628290597,242.7,10.8213203435596)) ;
#70173=CARTESIAN_POINT('Origin',(74.1283628290597,242.7,10.8213203435596)) ;
#70174=CARTESIAN_POINT('Origin',(71.2283628290598,239.8,10.8213203435596)) ;
#70175=CARTESIAN_POINT('Origin',(71.2283628290598,239.8,10.8213203435596)) ;
#70176=CARTESIAN_POINT('Origin',(71.2283628290597,239.,10.8213203435596)) ;
#70177=CARTESIAN_POINT('Origin',(71.2283628290597,239.,10.8213203435596)) ;
#70178=CARTESIAN_POINT('Origin',(74.1283628290597,236.1,10.8213203435596)) ;
#70179=CARTESIAN_POINT('Origin',(74.1283628290597,236.1,10.8213203435596)) ;
#70180=CARTESIAN_POINT('Origin',(74.9283628290597,236.1,10.8213203435596)) ;
#70181=CARTESIAN_POINT('Origin',(74.9283628290597,236.1,10.8213203435596)) ;
#70182=CARTESIAN_POINT('Origin',(77.8283628290598,239.,10.8213203435596)) ;
#70183=CARTESIAN_POINT('Origin',(77.8283628290598,239.,10.8213203435596)) ;
#70184=CARTESIAN_POINT('Origin',(77.8283628290598,239.8,10.8213203435596)) ;
#70185=CARTESIAN_POINT('Origin',(77.8283628290598,239.8,10.8213203435596)) ;
#70186=CARTESIAN_POINT('Origin',(73.9283628290597,235.9,11.0213203435596)) ;
#70187=CARTESIAN_POINT('',(73.9283628290597,236.1,6.22132034355964)) ;
#70188=CARTESIAN_POINT('',(73.9283628290597,236.1,11.0213203435596)) ;
#70189=CARTESIAN_POINT('',(73.9283628290597,237.85,6.22132034355964)) ;
#70190=CARTESIAN_POINT('',(73.9283628290597,237.65,6.22132034355964)) ;
#70191=CARTESIAN_POINT('',(73.9283628290597,237.85,11.0213203435596)) ;
#70192=CARTESIAN_POINT('Origin',(74.1283628290597,236.1,11.0213203435596)) ;
#70193=CARTESIAN_POINT('',(74.1283628290597,235.9,6.22132034355964)) ;
#70194=CARTESIAN_POINT('',(74.1283628290597,235.9,11.0213203435596)) ;
#70195=CARTESIAN_POINT('Origin',(74.1283628290597,236.1,6.22132034355964)) ;
#70196=CARTESIAN_POINT('Origin',(75.1283628290597,235.9,11.0213203435596)) ;
#70197=CARTESIAN_POINT('',(74.9283628290597,235.9,6.22132034355964)) ;
#70198=CARTESIAN_POINT('',(74.9283628290597,235.9,11.0213203435596)) ;
#70199=CARTESIAN_POINT('',(74.8283628290597,235.9,6.22132034355964)) ;
#70200=CARTESIAN_POINT('Origin',(74.9283628290597,236.1,11.0213203435596)) ;
#70201=CARTESIAN_POINT('',(75.1283628290597,236.1,6.22132034355964)) ;
#70202=CARTESIAN_POINT('',(75.1283628290597,236.1,11.0213203435596)) ;
#70203=CARTESIAN_POINT('Origin',(74.9283628290597,236.1,6.22132034355964)) ;
#70204=CARTESIAN_POINT('Origin',(75.1283628290597,238.8,11.0213203435596)) ;
#70205=CARTESIAN_POINT('',(75.1283628290597,237.85,6.22132034355964)) ;
#70206=CARTESIAN_POINT('',(75.1283628290597,237.85,11.0213203435596)) ;
#70207=CARTESIAN_POINT('',(75.1283628290597,239.1,6.22132034355964)) ;
#70208=CARTESIAN_POINT('Origin',(76.0783628290597,237.85,11.0213203435596)) ;
#70209=CARTESIAN_POINT('',(76.0783628290597,238.8,6.22132034355964)) ;
#70210=CARTESIAN_POINT('',(76.0783628290597,238.8,11.0213203435596)) ;
#70211=CARTESIAN_POINT('Origin',(76.0783628290597,237.85,6.22132034355964)) ;
#70212=CARTESIAN_POINT('Origin',(78.0283628290598,238.8,11.0213203435596)) ;
#70213=CARTESIAN_POINT('',(77.8283628290598,238.8,6.22132034355964)) ;
#70214=CARTESIAN_POINT('',(77.8283628290598,238.8,11.0213203435596)) ;
#70215=CARTESIAN_POINT('',(76.2783628290597,238.8,6.22132034355964)) ;
#70216=CARTESIAN_POINT('Origin',(77.8283628290598,239.,11.0213203435596)) ;
#70217=CARTESIAN_POINT('',(78.0283628290598,239.,6.22132034355964)) ;
#70218=CARTESIAN_POINT('',(78.0283628290598,239.,11.0213203435596)) ;
#70219=CARTESIAN_POINT('Origin',(77.8283628290598,239.,6.22132034355964)) ;
#70220=CARTESIAN_POINT('Origin',(78.0283628290598,240.,11.0213203435596)) ;
#70221=CARTESIAN_POINT('',(78.0283628290598,239.8,6.22132034355964)) ;
#70222=CARTESIAN_POINT('',(78.0283628290598,239.8,11.0213203435596)) ;
#70223=CARTESIAN_POINT('',(78.0283628290598,239.7,6.22132034355964)) ;
#70224=CARTESIAN_POINT('Origin',(77.8283628290598,239.8,11.0213203435596)) ;
#70225=CARTESIAN_POINT('',(77.8283628290598,240.,6.22132034355964)) ;
#70226=CARTESIAN_POINT('',(77.8283628290598,240.,11.0213203435596)) ;
#70227=CARTESIAN_POINT('Origin',(77.8283628290598,239.8,6.22132034355964)) ;
#70228=CARTESIAN_POINT('Origin',(75.1283628290596,240.,11.0213203435596)) ;
#70229=CARTESIAN_POINT('',(76.0783628290596,240.,6.22132034355964)) ;
#70230=CARTESIAN_POINT('',(76.0783628290596,240.,11.0213203435596)) ;
#70231=CARTESIAN_POINT('',(74.8283628290597,240.,6.22132034355964)) ;
#70232=CARTESIAN_POINT('Origin',(76.0783628290596,240.95,11.0213203435596)) ;
#70233=CARTESIAN_POINT('',(75.1283628290596,240.95,6.22132034355964)) ;
#70234=CARTESIAN_POINT('',(75.1283628290596,240.95,11.0213203435596)) ;
#70235=CARTESIAN_POINT('Origin',(76.0783628290596,240.95,6.22132034355964)) ;
#70236=CARTESIAN_POINT('Origin',(74.5283628290598,239.4,11.0213203435596)) ;
#70237=CARTESIAN_POINT('Origin',(72.0287747312354,244.633742383918,7.27867958884205)) ;
#70238=CARTESIAN_POINT('',(72.1901462641302,244.751891562379,7.27867958883792)) ;
#70239=CARTESIAN_POINT('Origin',(72.0287747312355,244.633742383918,7.27867958883752)) ;
#70240=CARTESIAN_POINT('',(71.9556834737297,244.786783924095,7.17267980084126)) ;
#70241=CARTESIAN_POINT('Origin',(72.0287747312354,244.633742383918,7.27867958884205)) ;
#70242=CARTESIAN_POINT('Origin',(72.0287747312355,244.633742383918,7.2786795888419)) ;
#70243=CARTESIAN_POINT('Origin',(73.474255491572,245.103407553477,7.2786795888419)) ;
#70244=CARTESIAN_POINT('',(73.2742568343815,245.10414043955,7.27867958883757)) ;
#70245=CARTESIAN_POINT('Origin',(73.474255491572,245.103407553477,7.2786795888419)) ;
#70246=CARTESIAN_POINT('',(73.4434320007296,245.270182723559,7.17267980084145)) ;
#70247=CARTESIAN_POINT('Origin',(73.474255491572,245.103407553477,7.2786795888419)) ;
#70248=CARTESIAN_POINT('Origin',(73.474255491572,245.103407553474,7.27867958883797)) ;
#70249=CARTESIAN_POINT('Origin',(71.7633973169968,244.498525837642,7.2786795888419)) ;
#70250=CARTESIAN_POINT('',(71.5729608165738,244.437419869794,7.27867958883749)) ;
#70251=CARTESIAN_POINT('Origin',(71.7633973169968,244.498525837642,7.2786795888419)) ;
#70252=CARTESIAN_POINT('',(71.6825460733808,244.647613467409,7.17267980084143)) ;
#70253=CARTESIAN_POINT('Origin',(71.7633973169968,244.498525837642,7.2786795888419)) ;
#70254=CARTESIAN_POINT('Origin',(71.7633973169975,244.498525837639,7.2786795888379)) ;
#70255=CARTESIAN_POINT('Origin',(74.5283628290597,239.4,7.2786795888419)) ;
#70256=CARTESIAN_POINT('Origin',(74.5283628290597,239.4,7.17267980084126)) ;
#70257=CARTESIAN_POINT('Origin',(73.7684286213811,245.15,7.27867958884205)) ;
#70258=CARTESIAN_POINT('',(73.9584121733014,245.212499999998,7.27867958883793)) ;
#70259=CARTESIAN_POINT('Origin',(73.7684286213812,245.15,7.2786795888375)) ;
#70260=CARTESIAN_POINT('',(73.7462071414064,245.31813759476,7.17267980084126)) ;
#70261=CARTESIAN_POINT('Origin',(73.7684286213811,245.15,7.27867958884205)) ;
#70262=CARTESIAN_POINT('Origin',(73.7684286213811,245.15,7.2786795888419)) ;
#70263=CARTESIAN_POINT('Origin',(70.5337979397465,243.605169597679,7.27867958886637)) ;
#70264=CARTESIAN_POINT('',(70.6507612838972,243.767402689633,7.27867958819172)) ;
#70265=CARTESIAN_POINT('Origin',(70.5337979397592,243.60516959767,7.2786795881253)) ;
#70266=CARTESIAN_POINT('',(70.4169915862605,243.728134311007,7.17267980084127)) ;
#70267=CARTESIAN_POINT('Origin',(70.5337979397465,243.605169597679,7.27867958886637)) ;
#70268=CARTESIAN_POINT('Origin',(70.5337979397592,243.60516959767,7.2786795888419)) ;
#70269=CARTESIAN_POINT('Ctrl Pts',(70.6501568829842,243.767838986024,7.28037086445601)) ;
#70270=CARTESIAN_POINT('Ctrl Pts',(70.695018761352,243.735411937294,7.16429143740118)) ;
#70271=CARTESIAN_POINT('Ctrl Pts',(70.7949584384066,243.681786355863,6.93457499380776)) ;
#70272=CARTESIAN_POINT('Ctrl Pts',(70.9495221917943,243.649443421145,6.66101676411208)) ;
#70273=CARTESIAN_POINT('Ctrl Pts',(71.0970424533863,243.657858652391,6.46925478973694)) ;
#70274=CARTESIAN_POINT('Ctrl Pts',(71.2015317828535,243.685094051328,6.37321776533927)) ;
#70275=CARTESIAN_POINT('Ctrl Pts',(71.2899862061965,243.726262429777,6.32731112524896)) ;
#70276=CARTESIAN_POINT('Ctrl Pts',(71.3551880178236,243.767424556722,6.31493581996192)) ;
#70277=CARTESIAN_POINT('Ctrl Pts',(71.414511662802,243.816727035925,6.32729394384689)) ;
#70278=CARTESIAN_POINT('Ctrl Pts',(71.4809943478713,243.888111400172,6.37316824150563)) ;
#70279=CARTESIAN_POINT('Ctrl Pts',(71.5392090359803,243.979129806174,6.469294125934)) ;
#70280=CARTESIAN_POINT('Ctrl Pts',(71.5928225191086,244.116852003807,6.66106251922067)) ;
#70281=CARTESIAN_POINT('Ctrl Pts',(71.609820551523,244.273797881523,6.93454059478913)) ;
#70282=CARTESIAN_POINT('Ctrl Pts',(71.5897065079004,244.385452427618,7.16431248483623)) ;
#70283=CARTESIAN_POINT('Ctrl Pts',(71.572732687827,244.438129374609,7.28037056287155)) ;
#70284=CARTESIAN_POINT('Ctrl Pts',(70.6133143716979,243.794496370374,7.25145480381165)) ;
#70285=CARTESIAN_POINT('Ctrl Pts',(70.6579201115597,243.756943743429,7.13666531376885)) ;
#70286=CARTESIAN_POINT('Ctrl Pts',(70.759669756855,243.693403731017,6.90913510331608)) ;
#70287=CARTESIAN_POINT('Ctrl Pts',(70.9218627556374,243.650786986153,6.63763508188674)) ;
#70288=CARTESIAN_POINT('Ctrl Pts',(71.079042730125,243.654281538889,6.44713797226046)) ;
#70289=CARTESIAN_POINT('Ctrl Pts',(71.190989976115,243.680725469535,6.35168754197124)) ;
#70290=CARTESIAN_POINT('Ctrl Pts',(71.2857727915241,243.723478511816,6.30605227260946)) ;
#70291=CARTESIAN_POINT('Ctrl Pts',(71.3554410054417,243.767068640434,6.2937492054939)) ;
#70292=CARTESIAN_POINT('Ctrl Pts',(71.4184657724347,243.819875939003,6.30603519484955)) ;
#70293=CARTESIAN_POINT('Ctrl Pts',(71.4884050005537,243.896782573748,6.35163826841188)) ;
#70294=CARTESIAN_POINT('Ctrl Pts',(71.5481929415663,243.99516005771,6.44717720448016)) ;
#70295=CARTESIAN_POINT('Ctrl Pts',(71.6000835672938,244.143570042457,6.63768049386459)) ;
#70296=CARTESIAN_POINT('Ctrl Pts',(71.6096864560401,244.310955271312,6.90910115397914)) ;
#70297=CARTESIAN_POINT('Ctrl Pts',(71.5806917188778,244.427389248978,7.13668612730514)) ;
#70298=CARTESIAN_POINT('Ctrl Pts',(71.5587649839846,244.481406266543,7.25145450557636)) ;
#70299=CARTESIAN_POINT('Ctrl Pts',(70.5257088411162,243.808149962819,7.20122603502762)) ;
#70300=CARTESIAN_POINT('Ctrl Pts',(70.575768050217,243.76371921269,7.08852834828282)) ;
#70301=CARTESIAN_POINT('Ctrl Pts',(70.6900507860591,243.688214812907,6.86460074648092)) ;
#70302=CARTESIAN_POINT('Ctrl Pts',(70.8726290515606,243.636494804644,6.59656897970077)) ;
#70303=CARTESIAN_POINT('Ctrl Pts',(71.0492486924007,243.637943299584,6.40823334015557)) ;
#70304=CARTESIAN_POINT('Ctrl Pts',(71.1748856832364,243.666416799429,6.31379313877718)) ;
#70305=CARTESIAN_POINT('Ctrl Pts',(71.2810357577914,243.713684729473,6.26862706307453)) ;
#70306=CARTESIAN_POINT('Ctrl Pts',(71.3589348514346,243.762249702892,6.25644899326161)) ;
#70307=CARTESIAN_POINT('Ctrl Pts',(71.4292274030523,243.821341305003,6.26861012760492)) ;
#70308=CARTESIAN_POINT('Ctrl Pts',(71.5069799006174,243.907665972781,6.3137443011777)) ;
#70309=CARTESIAN_POINT('Ctrl Pts',(71.5729076291523,244.018427912558,6.40827217011468)) ;
#70310=CARTESIAN_POINT('Ctrl Pts',(71.6288977778067,244.185986520421,6.59661403907028)) ;
#70311=CARTESIAN_POINT('Ctrl Pts',(71.6361239251143,244.375552037511,6.86456746639935)) ;
#70312=CARTESIAN_POINT('Ctrl Pts',(71.5996334283149,244.507615608175,7.0885487827586)) ;
#70313=CARTESIAN_POINT('Ctrl Pts',(71.5728512558348,244.568943250038,7.20122574222209)) ;
#70314=CARTESIAN_POINT('Ctrl Pts',(70.4438236562226,243.75797324979,7.17772391322105)) ;
#70315=CARTESIAN_POINT('Ctrl Pts',(70.5015563262582,243.71393505825,7.06321986768199)) ;
#70316=CARTESIAN_POINT('Ctrl Pts',(70.631018084871,243.640737186515,6.83627960612169)) ;
#70317=CARTESIAN_POINT('Ctrl Pts',(70.8333007271835,243.595570389089,6.56550158124689)) ;
#70318=CARTESIAN_POINT('Ctrl Pts',(71.0274438557767,243.6052704527,6.37551287208947)) ;
#70319=CARTESIAN_POINT('Ctrl Pts',(71.1653543352155,243.640682678267,6.28031724281592)) ;
#70320=CARTESIAN_POINT('Ctrl Pts',(71.2822399569048,243.694858370743,6.23480374698507)) ;
#70321=CARTESIAN_POINT('Ctrl Pts',(71.3684114405816,243.749198508394,6.22253350040122)) ;
#70322=CARTESIAN_POINT('Ctrl Pts',(71.4467557829302,243.814374864135,6.23478671054199)) ;
#70323=CARTESIAN_POINT('Ctrl Pts',(71.5343942575121,243.908773769962,6.28026810039496)) ;
#70324=CARTESIAN_POINT('Ctrl Pts',(71.6107180544398,244.029068327693,6.37555197849753)) ;
#70325=CARTESIAN_POINT('Ctrl Pts',(71.6799733584262,244.210745485926,6.56554689303006)) ;
#70326=CARTESIAN_POINT('Ctrl Pts',(71.6995177608991,244.417020600932,6.83624573656735)) ;
#70327=CARTESIAN_POINT('Ctrl Pts',(71.6699141621299,244.562812309387,7.06324062946311)) ;
#70328=CARTESIAN_POINT('Ctrl Pts',(71.6458760522509,244.631315212985,7.17772361572752)) ;
#70329=CARTESIAN_POINT('Ctrl Pts',(70.4161308161459,243.728748828007,7.17434119724341)) ;
#70330=CARTESIAN_POINT('Ctrl Pts',(70.4762342283297,243.685779217861,7.05826310306117)) ;
#70331=CARTESIAN_POINT('Ctrl Pts',(70.6105145005683,243.615236269817,6.82854891848138)) ;
#70332=CARTESIAN_POINT('Ctrl Pts',(70.8194164063599,243.574668856811,6.554992815528)) ;
#70333=CARTESIAN_POINT('Ctrl Pts',(71.0198900905357,243.589126800135,6.36323214814111)) ;
#70334=CARTESIAN_POINT('Ctrl Pts',(71.162493478287,243.628114813195,6.26719572987436)) ;
#70335=CARTESIAN_POINT('Ctrl Pts',(71.2837091433123,243.685533784822,6.22128937019327)) ;
#70336=CARTESIAN_POINT('Ctrl Pts',(71.3733381280523,243.742414020762,6.20891413955045)) ;
#70337=CARTESIAN_POINT('Ctrl Pts',(71.4551693674424,243.810095751249,6.22127218889828)) ;
#70338=CARTESIAN_POINT('Ctrl Pts',(71.5472287971451,243.907609473381,6.26714620629932)) ;
#70339=CARTESIAN_POINT('Ctrl Pts',(71.6284090431722,244.031265917727,6.36327148423066)) ;
#70340=CARTESIAN_POINT('Ctrl Pts',(71.7041419702003,244.217490856572,6.55503857028213)) ;
#70341=CARTESIAN_POINT('Ctrl Pts',(71.7301069186013,244.428640448521,6.82851451992736)) ;
#70342=CARTESIAN_POINT('Ctrl Pts',(71.704517229436,244.578194768653,7.05828415025454)) ;
#70343=CARTESIAN_POINT('Ctrl Pts',(71.6822276827102,244.648621821033,7.17434089566242)) ;
#70344=CARTESIAN_POINT('Ctrl Pts',(71.6825460733808,244.647613467409,7.17267980084144)) ;
#70345=CARTESIAN_POINT('Ctrl Pts',(71.6935886426337,244.612559352449,7.11495383284403)) ;
#70346=CARTESIAN_POINT('Ctrl Pts',(71.7022927623503,244.576361719043,7.05741591593104)) ;
#70347=CARTESIAN_POINT('Ctrl Pts',(71.7083791693549,244.538999323656,7.00033196889614)) ;
#70348=CARTESIAN_POINT('Ctrl Pts',(71.7126272417874,244.512921842846,6.96048962158692)) ;
#70349=CARTESIAN_POINT('Ctrl Pts',(71.715600317724,244.486277068799,6.92086843822223)) ;
#70350=CARTESIAN_POINT('Ctrl Pts',(71.7172074984982,244.459059598684,6.88155816675306)) ;
#70351=CARTESIAN_POINT('Ctrl Pts',(71.7179029988757,244.447281358772,6.86454682049581)) ;
#70352=CARTESIAN_POINT('Ctrl Pts',(71.7183428322704,244.435395593456,6.84759321077135)) ;
#70353=CARTESIAN_POINT('Ctrl Pts',(71.7185197039289,244.423398003082,6.83069915794562)) ;
#70354=CARTESIAN_POINT('Ctrl Pts',(71.7195612719805,244.352746170378,6.73121286472363)) ;
#70355=CARTESIAN_POINT('Ctrl Pts',(71.711478526729,244.278245478875,6.633836781897)) ;
#70356=CARTESIAN_POINT('Ctrl Pts',(71.6894930170596,244.199202524374,6.54295091299619)) ;
#70357=CARTESIAN_POINT('Ctrl Pts',(71.6867556442851,244.189361040827,6.53163489135909)) ;
#70358=CARTESIAN_POINT('Ctrl Pts',(71.6838028080864,244.179449163839,6.52041945932379)) ;
#70359=CARTESIAN_POINT('Ctrl Pts',(71.6806253447614,244.169465574853,6.5093130441619)) ;
#70360=CARTESIAN_POINT('Ctrl Pts',(71.6727462032902,244.144709314288,6.4817725165935)) ;
#70361=CARTESIAN_POINT('Ctrl Pts',(71.6634872275843,244.119517200743,6.45490825271367)) ;
#70362=CARTESIAN_POINT('Ctrl Pts',(71.6524916152515,244.093896418644,6.42914051265344)) ;
#70363=CARTESIAN_POINT('Ctrl Pts',(71.6434485774699,244.072825313779,6.40794854627107)) ;
#70364=CARTESIAN_POINT('Ctrl Pts',(71.6332306941195,244.051463461098,6.38749730975455)) ;
#70365=CARTESIAN_POINT('Ctrl Pts',(71.6216396098452,244.029812746213,6.36801731440074)) ;
#70366=CARTESIAN_POINT('Ctrl Pts',(71.6143706676241,244.016235259257,6.35580111811206)) ;
#70367=CARTESIAN_POINT('Ctrl Pts',(71.6065616958071,244.002544178426,6.34396688159399)) ;
#70368=CARTESIAN_POINT('Ctrl Pts',(71.5981620367324,243.988783067631,6.33264057742806)) ;
#70369=CARTESIAN_POINT('Ctrl Pts',(71.5925581358654,243.979602230643,6.32508414148572)) ;
#70370=CARTESIAN_POINT('Ctrl Pts',(71.5866877247482,243.970384272286,6.31774884713379)) ;
#70371=CARTESIAN_POINT('Ctrl Pts',(71.5805340060758,243.961141063887,6.31067237243103)) ;
#70372=CARTESIAN_POINT('Ctrl Pts',(71.5633212059787,243.935286534796,6.29087849641324)) ;
#70373=CARTESIAN_POINT('Ctrl Pts',(71.5438942831396,243.909242925014,6.27311943149809)) ;
#70374=CARTESIAN_POINT('Ctrl Pts',(71.5219543369792,243.883348662293,6.25826321902762)) ;
#70375=CARTESIAN_POINT('Ctrl Pts',(71.5108882767763,243.870288125677,6.25077004924574)) ;
#70376=CARTESIAN_POINT('Ctrl Pts',(71.4991835316302,243.857265683635,6.24401485835062)) ;
#70377=CARTESIAN_POINT('Ctrl Pts',(71.4868681437631,243.844407671654,6.23816299485402)) ;
#70378=CARTESIAN_POINT('Ctrl Pts',(71.4777070320372,243.834842915302,6.23380993867133)) ;
#70379=CARTESIAN_POINT('Ctrl Pts',(71.4682072078246,243.825367887728,6.22995574083448)) ;
#70380=CARTESIAN_POINT('Ctrl Pts',(71.45836978832,243.816024472857,6.2266646345835)) ;
#70381=CARTESIAN_POINT('Ctrl Pts',(71.4566034155626,243.81434680185,6.22607369501641)) ;
#70382=CARTESIAN_POINT('Ctrl Pts',(71.4548262223221,243.812673441663,6.22550094157797)) ;
#70383=CARTESIAN_POINT('Ctrl Pts',(71.4530382562569,243.811004678101,6.2249467661821)) ;
#70384=CARTESIAN_POINT('Ctrl Pts',(71.4323658483102,243.791710485783,6.21853940751896)) ;
#70385=CARTESIAN_POINT('Ctrl Pts',(71.4102573909446,243.77303338664,6.21461505937639)) ;
#70386=CARTESIAN_POINT('Ctrl Pts',(71.3871541199649,243.755454107357,6.21342329168862)) ;
#70387=CARTESIAN_POINT('Ctrl Pts',(71.3821602173354,243.751654246761,6.21316568436562)) ;
#70388=CARTESIAN_POINT('Ctrl Pts',(71.3771200764926,243.747905917213,6.21303584367958)) ;
#70389=CARTESIAN_POINT('Ctrl Pts',(71.3720385038273,243.744214269853,6.21303635288226)) ;
#70390=CARTESIAN_POINT('Ctrl Pts',(71.3556121478995,243.7322808946,6.21303799889719)) ;
#70391=CARTESIAN_POINT('Ctrl Pts',(71.338757067714,243.720943084757,6.21440203650676)) ;
#70392=CARTESIAN_POINT('Ctrl Pts',(71.3216869500583,243.710299988263,6.21704113221422)) ;
#70393=CARTESIAN_POINT('Ctrl Pts',(71.3090499734372,243.702420923555,6.21899484989965)) ;
#70394=CARTESIAN_POINT('Ctrl Pts',(71.2962921174743,243.694920539031,6.22164757766141)) ;
#70395=CARTESIAN_POINT('Ctrl Pts',(71.2834953493073,243.687836452692,6.22496512671297)) ;
#70396=CARTESIAN_POINT('Ctrl Pts',(71.2706004162921,243.680698023862,6.22830812490099)) ;
#70397=CARTESIAN_POINT('Ctrl Pts',(71.25766693237,243.673982902621,6.23232603291034)) ;
#70398=CARTESIAN_POINT('Ctrl Pts',(71.2447600103528,243.667682392571,6.23693149431686)) ;
#70399=CARTESIAN_POINT('Ctrl Pts',(71.2352301656824,243.6630304018,6.24033194345426)) ;
#70400=CARTESIAN_POINT('Ctrl Pts',(71.2257122185925,243.658603091933,6.24405349551631)) ;
#70401=CARTESIAN_POINT('Ctrl Pts',(71.216226504895,243.654394834633,6.24806417943962)) ;
#70402=CARTESIAN_POINT('Ctrl Pts',(71.2085878920803,243.651006028143,6.25129388493034)) ;
#70403=CARTESIAN_POINT('Ctrl Pts',(71.2009715347077,243.647759930132,6.25471059910582)) ;
#70404=CARTESIAN_POINT('Ctrl Pts',(71.1933918074453,243.644655269533,6.25829603786513)) ;
#70405=CARTESIAN_POINT('Ctrl Pts',(71.1611612922872,243.631453632189,6.27354204003386)) ;
#70406=CARTESIAN_POINT('Ctrl Pts',(71.1295941708611,243.620812694726,6.29184252320046)) ;
#70407=CARTESIAN_POINT('Ctrl Pts',(71.0989314377017,243.612317013262,6.3122744441402)) ;
#70408=CARTESIAN_POINT('Ctrl Pts',(71.0820668876359,243.607644375482,6.32351203186064)) ;
#70409=CARTESIAN_POINT('Ctrl Pts',(71.0654757041949,243.603619907437,6.33539347318128)) ;
#70410=CARTESIAN_POINT('Ctrl Pts',(71.0491959191737,243.600170118652,6.34776114160793)) ;
#70411=CARTESIAN_POINT('Ctrl Pts',(71.0404977678413,243.598326925705,6.35436908215903)) ;
#70412=CARTESIAN_POINT('Ctrl Pts',(71.0318814733597,243.596646250274,6.36112111245423)) ;
#70413=CARTESIAN_POINT('Ctrl Pts',(71.0233515826097,243.595117214015,6.36799498925902)) ;
#70414=CARTESIAN_POINT('Ctrl Pts',(70.96981984014,243.585521314418,6.41113394773635)) ;
#70415=CARTESIAN_POINT('Ctrl Pts',(70.9196911860922,243.581899679019,6.45907508759202)) ;
#70416=CARTESIAN_POINT('Ctrl Pts',(70.8723567390609,243.582213043482,6.50928897930807)) ;
#70417=CARTESIAN_POINT('Ctrl Pts',(70.8498554030447,243.582362007281,6.53315911450659)) ;
#70418=CARTESIAN_POINT('Ctrl Pts',(70.8279854810731,243.583399804612,6.5575421964682)) ;
#70419=CARTESIAN_POINT('Ctrl Pts',(70.8067113969608,243.585247990717,6.58235409106085)) ;
#70420=CARTESIAN_POINT('Ctrl Pts',(70.7633271573144,243.589016996635,6.63295298760588)) ;
#70421=CARTESIAN_POINT('Ctrl Pts',(70.7224350251622,243.596073422295,6.68522047956527)) ;
#70422=CARTESIAN_POINT('Ctrl Pts',(70.6836563803347,243.605727456895,6.73849780320215)) ;
#70423=CARTESIAN_POINT('Ctrl Pts',(70.6614902200515,243.611245774496,6.76895151555969)) ;
#70424=CARTESIAN_POINT('Ctrl Pts',(70.6400153868192,243.617613628525,6.79973533853582)) ;
#70425=CARTESIAN_POINT('Ctrl Pts',(70.6191665025799,243.624707302679,6.83072647984526)) ;
#70426=CARTESIAN_POINT('Ctrl Pts',(70.5810380909751,243.637680204481,6.88740303761148)) ;
#70427=CARTESIAN_POINT('Ctrl Pts',(70.5450012307065,243.653079304507,6.94477373817397)) ;
#70428=CARTESIAN_POINT('Ctrl Pts',(70.5109406822167,243.670718836386,7.00266316541486)) ;
#70429=CARTESIAN_POINT('Ctrl Pts',(70.4778053242332,243.687879223679,7.05898013563804)) ;
#70430=CARTESIAN_POINT('Ctrl Pts',(70.446515553258,243.707086570428,7.11572953304929)) ;
#70431=CARTESIAN_POINT('Ctrl Pts',(70.4169915862637,243.728134311011,7.17267980084145)) ;
#70432=CARTESIAN_POINT('Ctrl Pts',(70.6507612838973,243.767402689634,7.27867958819153)) ;
#70433=CARTESIAN_POINT('Ctrl Pts',(70.6684362520318,243.754659769268,7.23300052669799)) ;
#70434=CARTESIAN_POINT('Ctrl Pts',(70.6869194298059,243.742792494175,7.18746933677425)) ;
#70435=CARTESIAN_POINT('Ctrl Pts',(70.7062562007618,243.73185516032,7.14219315636161)) ;
#70436=CARTESIAN_POINT('Ctrl Pts',(70.7248835542395,243.721319089727,7.09857804510088)) ;
#70437=CARTESIAN_POINT('Ctrl Pts',(70.7443039240259,243.711645777375,7.05519957527199)) ;
#70438=CARTESIAN_POINT('Ctrl Pts',(70.7645634985461,243.702931060682,7.01215352027502)) ;
#70439=CARTESIAN_POINT('Ctrl Pts',(70.7764572906237,243.697814910377,6.98688246498295)) ;
#70440=CARTESIAN_POINT('Ctrl Pts',(70.7886403641635,243.693030055314,6.96172597692718)) ;
#70441=CARTESIAN_POINT('Ctrl Pts',(70.8011210393687,243.688604301858,6.93670343437627)) ;
#70442=CARTESIAN_POINT('Ctrl Pts',(70.8183500983234,243.682494731184,6.9021608432327)) ;
#70443=CARTESIAN_POINT('Ctrl Pts',(70.836126802622,243.677073327903,6.86787350758113)) ;
#70444=CARTESIAN_POINT('Ctrl Pts',(70.854531822304,243.672418328196,6.83402414428508)) ;
#70445=CARTESIAN_POINT('Ctrl Pts',(70.8724247945859,243.667892835578,6.80111650660351)) ;
#70446=CARTESIAN_POINT('Ctrl Pts',(70.8909123497292,243.664091596054,6.76862281055142)) ;
#70447=CARTESIAN_POINT('Ctrl Pts',(70.9100593736244,243.661134078233,6.73671094319522)) ;
#70448=CARTESIAN_POINT('Ctrl Pts',(70.9283638588753,243.658306701946,6.70620331399155)) ;
#70449=CARTESIAN_POINT('Ctrl Pts',(70.947271724205,243.65625053939,6.67622743493549)) ;
#70450=CARTESIAN_POINT('Ctrl Pts',(70.9668210539553,243.655113775303,6.64692999111437)) ;
#70451=CARTESIAN_POINT('Ctrl Pts',(70.9739232856404,243.654700791225,6.63628628943998)) ;
#70452=CARTESIAN_POINT('Ctrl Pts',(70.9811099480349,243.65440957849,6.62573213131839)) ;
#70453=CARTESIAN_POINT('Ctrl Pts',(70.9883819374054,243.654248714521,6.61527455030405)) ;
#70454=CARTESIAN_POINT('Ctrl Pts',(71.0058228527503,243.653862903331,6.59019341006963)) ;
#70455=CARTESIAN_POINT('Ctrl Pts',(71.0237569280687,243.654222647332,6.56566779824074)) ;
#70456=CARTESIAN_POINT('Ctrl Pts',(71.0422577508755,243.655477612093,6.54201530058587)) ;
#70457=CARTESIAN_POINT('Ctrl Pts',(71.0591803639201,243.656625522283,6.52038047550117)) ;
#70458=CARTESIAN_POINT('Ctrl Pts',(71.0765776157427,243.658522933216,6.49947615643607)) ;
#70459=CARTESIAN_POINT('Ctrl Pts',(71.0944794582127,243.661326346066,6.47954539033945)) ;
#70460=CARTESIAN_POINT('Ctrl Pts',(71.0961489913088,243.661587793487,6.47768663900227)) ;
#70461=CARTESIAN_POINT('Ctrl Pts',(71.0978228895911,243.661857150439,6.47583635514527)) ;
#70462=CARTESIAN_POINT('Ctrl Pts',(71.0995011620659,243.662134562174,6.47399473591177)) ;
#70463=CARTESIAN_POINT('Ctrl Pts',(71.1177037387764,243.665143375378,6.45402049700077)) ;
#70464=CARTESIAN_POINT('Ctrl Pts',(71.1364174559616,243.669096373618,6.43506553102507)) ;
#70465=CARTESIAN_POINT('Ctrl Pts',(71.1555892310845,243.674185491156,6.41767878130173)) ;
#70466=CARTESIAN_POINT('Ctrl Pts',(71.1738953556318,243.679044823111,6.40107708407407)) ;
#70467=CARTESIAN_POINT('Ctrl Pts',(71.1926195333131,243.684940452386,6.38590518299697)) ;
#70468=CARTESIAN_POINT('Ctrl Pts',(71.211672149302,243.69205993109,6.37264097007206)) ;
#70469=CARTESIAN_POINT('Ctrl Pts',(71.2157986470463,243.693601898493,6.36976814962858)) ;
#70470=CARTESIAN_POINT('Ctrl Pts',(71.2199403691951,243.695201339153,6.36698481647962)) ;
#70471=CARTESIAN_POINT('Ctrl Pts',(71.2240960892816,243.696860256998,6.36429582586576)) ;
#70472=CARTESIAN_POINT('Ctrl Pts',(71.2401983004994,243.703288082976,6.35387676637042)) ;
#70473=CARTESIAN_POINT('Ctrl Pts',(71.2565168735863,243.710615594979,6.34487410716004)) ;
#70474=CARTESIAN_POINT('Ctrl Pts',(71.2728169071997,243.71887377027,6.3377356388658)) ;
#70475=CARTESIAN_POINT('Ctrl Pts',(71.2785027662801,243.721754428192,6.33524556272643)) ;
#70476=CARTESIAN_POINT('Ctrl Pts',(71.2841863608018,243.724747868746,6.33298231923947)) ;
#70477=CARTESIAN_POINT('Ctrl Pts',(71.2898577861283,243.727853897203,6.33096491471358)) ;
#70478=CARTESIAN_POINT('Ctrl Pts',(71.3034194112714,243.735281094282,6.32614085685032)) ;
#70479=CARTESIAN_POINT('Ctrl Pts',(71.316912179818,243.743356911529,6.32272248960801)) ;
#70480=CARTESIAN_POINT('Ctrl Pts',(71.3301413890697,243.75201206251,6.32081539597999)) ;
#70481=CARTESIAN_POINT('Ctrl Pts',(71.3383047211844,243.757352886033,6.31963858802697)) ;
#70482=CARTESIAN_POINT('Ctrl Pts',(71.3463680534785,243.76291335346,6.31903723360498)) ;
#70483=CARTESIAN_POINT('Ctrl Pts',(71.3542903145311,243.768668411348,6.31903614088288)) ;
#70484=CARTESIAN_POINT('Ctrl Pts',(71.3670532685345,243.777939948681,6.31903438048116)) ;
#70485=CARTESIAN_POINT('Ctrl Pts',(71.3794502709664,243.787720035148,6.32059053861267)) ;
#70486=CARTESIAN_POINT('Ctrl Pts',(71.391331743839,243.797868294085,6.32360061213219)) ;
#70487=CARTESIAN_POINT('Ctrl Pts',(71.3987772128469,243.804227652744,6.32548686052423)) ;
#70488=CARTESIAN_POINT('Ctrl Pts',(71.4060208997469,243.810730744532,6.32794403869006)) ;
#70489=CARTESIAN_POINT('Ctrl Pts',(71.4130334230589,243.817335711349,6.33094655418276)) ;
#70490=CARTESIAN_POINT('Ctrl Pts',(71.4266399543435,243.830151453079,6.3367723916404)) ;
#70491=CARTESIAN_POINT('Ctrl Pts',(71.4393767723351,243.843353445295,6.34465133540946)) ;
#70492=CARTESIAN_POINT('Ctrl Pts',(71.4511861305303,243.856712421974,6.35412854620593)) ;
#70493=CARTESIAN_POINT('Ctrl Pts',(71.4551755784542,243.861225363396,6.35733014601447)) ;
#70494=CARTESIAN_POINT('Ctrl Pts',(71.4590596019843,243.865756070438,6.36071414477957)) ;
#70495=CARTESIAN_POINT('Ctrl Pts',(71.462837250583,243.870295331209,6.36426300702838)) ;
#70496=CARTESIAN_POINT('Ctrl Pts',(71.4760836447931,243.886212332493,6.37670715769954)) ;
#70497=CARTESIAN_POINT('Ctrl Pts',(71.4880287658818,243.902237362419,6.39117841554036)) ;
#70498=CARTESIAN_POINT('Ctrl Pts',(71.4988220697557,243.918213233306,6.40719115654323)) ;
#70499=CARTESIAN_POINT('Ctrl Pts',(71.5101121008671,243.934924342476,6.42394083265832)) ;
#70500=CARTESIAN_POINT('Ctrl Pts',(71.5201425169332,243.951581936066,6.44237714045534)) ;
#70501=CARTESIAN_POINT('Ctrl Pts',(71.5290803896567,243.968062508258,6.46194427505928)) ;
#70502=CARTESIAN_POINT('Ctrl Pts',(71.5308979488639,243.971413911512,6.46592334555604)) ;
#70503=CARTESIAN_POINT('Ctrl Pts',(71.5326702971534,243.974758164482,6.46994917932546)) ;
#70504=CARTESIAN_POINT('Ctrl Pts',(71.53439878569,243.978094479398,6.47401710240149)) ;
#70505=CARTESIAN_POINT('Ctrl Pts',(71.5427855239735,243.994282495369,6.49375492852842)) ;
#70506=CARTESIAN_POINT('Ctrl Pts',(71.5501387651293,244.010273697668,6.51448364351368)) ;
#70507=CARTESIAN_POINT('Ctrl Pts',(71.5566194596361,244.026044169239,6.53596191343711)) ;
#70508=CARTESIAN_POINT('Ctrl Pts',(71.5633848267489,244.042507378485,6.55838364321145)) ;
#70509=CARTESIAN_POINT('Ctrl Pts',(71.5691996947475,244.058730639276,6.58162222447675)) ;
#70510=CARTESIAN_POINT('Ctrl Pts',(71.5742121078923,244.074730455715,6.60540310320344)) ;
#70511=CARTESIAN_POINT('Ctrl Pts',(71.5749062081047,244.076946050413,6.60869619028523)) ;
#70512=CARTESIAN_POINT('Ctrl Pts',(71.5755848629926,244.079157417819,6.61199967628627)) ;
#70513=CARTESIAN_POINT('Ctrl Pts',(71.5762484098432,244.081364654275,6.6153128321625)) ;
#70514=CARTESIAN_POINT('Ctrl Pts',(71.5820478706719,244.100656104999,6.64427012087318)) ;
#70515=CARTESIAN_POINT('Ctrl Pts',(71.5866962665371,244.119629043175,6.67396608377127)) ;
#70516=CARTESIAN_POINT('Ctrl Pts',(71.5903623616101,244.13826024683,6.70425263042087)) ;
#70517=CARTESIAN_POINT('Ctrl Pts',(71.5941409686902,244.157463239835,6.73546866746413)) ;
#70518=CARTESIAN_POINT('Ctrl Pts',(71.5968763478246,244.176303979186,6.76731209439664)) ;
#70519=CARTESIAN_POINT('Ctrl Pts',(71.5987132229992,244.194797005408,6.79962076342479)) ;
#70520=CARTESIAN_POINT('Ctrl Pts',(71.6006246850276,244.21404094637,6.83324133541157)) ;
#70521=CARTESIAN_POINT('Ctrl Pts',(71.6015634590013,244.23290912843,6.86736569916324)) ;
#70522=CARTESIAN_POINT('Ctrl Pts',(71.6016454480536,244.251448540695,6.90181114181182)) ;
#70523=CARTESIAN_POINT('Ctrl Pts',(71.6016730476434,244.257689376029,6.91340634949709)) ;
#70524=CARTESIAN_POINT('Ctrl Pts',(71.6016031603688,244.263893152714,6.9250379407503)) ;
#70525=CARTESIAN_POINT('Ctrl Pts',(71.6014390043077,244.27006217053,6.93669894594631)) ;
#70526=CARTESIAN_POINT('Ctrl Pts',(71.6008393973384,244.292595521116,6.97929268228135)) ;
#70527=CARTESIAN_POINT('Ctrl Pts',(71.598986155638,244.314631427322,7.02227885814213)) ;
#70528=CARTESIAN_POINT('Ctrl Pts',(71.5960122668263,244.336169373341,7.06555758389289)) ;
#70529=CARTESIAN_POINT('Ctrl Pts',(71.5929199249018,244.358565198356,7.11056014671543)) ;
#70530=CARTESIAN_POINT('Ctrl Pts',(71.5886160783604,244.380423612925,7.15587902870036)) ;
#70531=CARTESIAN_POINT('Ctrl Pts',(71.5831973640719,244.401764396013,7.20140192234408)) ;
#70532=CARTESIAN_POINT('Ctrl Pts',(71.5801381119917,244.413812795611,7.22710285427377)) ;
#70533=CARTESIAN_POINT('Ctrl Pts',(71.5767225386487,244.425696478238,7.25286881309734)) ;
#70534=CARTESIAN_POINT('Ctrl Pts',(71.5729608165744,244.437419869792,7.27867958883833)) ;
#70535=CARTESIAN_POINT('Origin',(75.2882970367382,245.15,7.2786795888419)) ;
#70536=CARTESIAN_POINT('',(75.0983134848186,245.2125,7.27867958883755)) ;
#70537=CARTESIAN_POINT('Origin',(75.2882970367382,245.15,7.2786795888419)) ;
#70538=CARTESIAN_POINT('',(75.3105185167129,245.31813759476,7.17267980084143)) ;
#70539=CARTESIAN_POINT('Origin',(75.2882970367382,245.15,7.2786795888419)) ;
#70540=CARTESIAN_POINT('Origin',(75.2882970367374,245.149999999998,7.27867958883798)) ;
#70541=CARTESIAN_POINT('Origin',(70.3231932313898,243.3945648893,7.2786795888419)) ;
#70542=CARTESIAN_POINT('',(70.1609601392448,243.277601545414,7.27867958883745)) ;
#70543=CARTESIAN_POINT('Origin',(70.3231932313898,243.3945648893,7.2786795888419)) ;
#70544=CARTESIAN_POINT('',(70.2002285180491,243.511371242796,7.17267980084141)) ;
#70545=CARTESIAN_POINT('Origin',(70.3231932313898,243.3945648893,7.2786795888419)) ;
#70546=CARTESIAN_POINT('Origin',(70.3231932313913,243.394564889298,7.27867958883786)) ;
#70547=CARTESIAN_POINT('Origin',(74.5283628290597,239.4,7.2786795888419)) ;
#70548=CARTESIAN_POINT('Origin',(74.5283628290597,239.4,7.17267980084127)) ;
#70549=CARTESIAN_POINT('Origin',(75.5824701665474,245.103407553477,7.27867958884206)) ;
#70550=CARTESIAN_POINT('',(75.7824688237379,245.104140439548,7.27867958883791)) ;
#70551=CARTESIAN_POINT('Origin',(75.5824701665474,245.103407553477,7.27867958883751)) ;
#70552=CARTESIAN_POINT('',(75.6132936573898,245.270182723559,7.17267980084128)) ;
#70553=CARTESIAN_POINT('Origin',(75.5824701665474,245.103407553477,7.27867958884206)) ;
#70554=CARTESIAN_POINT('Origin',(75.5824701665474,245.103407553477,7.2786795888419)) ;
#70555=CARTESIAN_POINT('Origin',(69.4298369914029,242.164965512068,7.27867958886636)) ;
#70556=CARTESIAN_POINT('',(69.4909429595611,242.355402012391,7.27867958819176)) ;
#70557=CARTESIAN_POINT('Origin',(69.4298369914177,242.164965512063,7.27867958812535)) ;
#70558=CARTESIAN_POINT('',(69.2807493616484,242.245816755675,7.17267980084126)) ;
#70559=CARTESIAN_POINT('Origin',(69.4298369914029,242.164965512068,7.27867958886636)) ;
#70560=CARTESIAN_POINT('Origin',(69.4298369914177,242.164965512063,7.2786795888419)) ;
#70561=CARTESIAN_POINT('Ctrl Pts',(69.4909429592547,242.355402012489,7.27867958886636)) ;
#70562=CARTESIAN_POINT('Ctrl Pts',(69.5434105984377,242.338566553604,7.16316434207535)) ;
#70563=CARTESIAN_POINT('Ctrl Pts',(69.6548363472646,242.318447141452,6.93376983755156)) ;
#70564=CARTESIAN_POINT('Ctrl Pts',(69.8115179376631,242.335283243238,6.66059049824912)) ;
#70565=CARTESIAN_POINT('Ctrl Pts',(69.9320961586154,242.382043605764,6.4924392790701)) ;
#70566=CARTESIAN_POINT('Ctrl Pts',(70.0038423289643,242.42384128837,6.4112217229231)) ;
#70567=CARTESIAN_POINT('Ctrl Pts',(70.0853128564862,242.483004335118,6.33512166788152)) ;
#70568=CARTESIAN_POINT('Ctrl Pts',(70.1739356804575,242.581754164171,6.30139292105391)) ;
#70569=CARTESIAN_POINT('Ctrl Pts',(70.2630551704512,242.761871347334,6.38459950069724)) ;
#70570=CARTESIAN_POINT('Ctrl Pts',(70.2766922354173,242.880428587697,6.52710936966954)) ;
#70571=CARTESIAN_POINT('Ctrl Pts',(70.2731493424206,242.966128315359,6.65331963180678)) ;
#70572=CARTESIAN_POINT('Ctrl Pts',(70.2672749757801,243.03292209962,6.75725826388023)) ;
#70573=CARTESIAN_POINT('Ctrl Pts',(70.2400533595442,243.145774108243,6.96268987067883)) ;
#70574=CARTESIAN_POINT('Ctrl Pts',(70.1931792067253,243.232912339636,7.16318512433994)) ;
#70575=CARTESIAN_POINT('Ctrl Pts',(70.1609601392448,243.277601545414,7.27867958884205)) ;
#70576=CARTESIAN_POINT('Ctrl Pts',(69.4476956000447,242.369278930705,7.24979207610077)) ;
#70577=CARTESIAN_POINT('Ctrl Pts',(69.50150865405,242.347521264376,7.13555826270376)) ;
#70578=CARTESIAN_POINT('Ctrl Pts',(69.6176942987279,242.318512021194,6.9083440833659)) ;
#70579=CARTESIAN_POINT('Ctrl Pts',(69.7848017901261,242.327968834837,6.6372185129258)) ;
#70580=CARTESIAN_POINT('Ctrl Pts',(69.9147387087311,242.37320396469,6.47017552473)) ;
#70581=CARTESIAN_POINT('Ctrl Pts',(69.9922050270014,242.415732076274,6.38946597909784)) ;
#70582=CARTESIAN_POINT('Ctrl Pts',(70.0801887888135,242.477057954304,6.3138257023692)) ;
#70583=CARTESIAN_POINT('Ctrl Pts',(70.1754581944923,242.581877167593,6.28029131424589)) ;
#70584=CARTESIAN_POINT('Ctrl Pts',(70.2684663048936,242.774904229625,6.36301246673742)) ;
#70585=CARTESIAN_POINT('Ctrl Pts',(70.2790542356121,242.90185505708,6.50464021891)) ;
#70586=CARTESIAN_POINT('Ctrl Pts',(70.2715880028707,242.992611796454,6.62996444336295)) ;
#70587=CARTESIAN_POINT('Ctrl Pts',(70.2622816507088,243.06319032064,6.73315738197291)) ;
#70588=CARTESIAN_POINT('Ctrl Pts',(70.227188364081,243.181213854183,6.93698950249586)) ;
#70589=CARTESIAN_POINT('Ctrl Pts',(70.1717134407734,243.269996255639,7.13557881442655)) ;
#70590=CARTESIAN_POINT('Ctrl Pts',(70.1343982367933,243.314444024645,7.24979207607672)) ;
#70591=CARTESIAN_POINT('Ctrl Pts',(69.3602854366959,242.355114488823,7.19960833957127)) ;
#70592=CARTESIAN_POINT('Ctrl Pts',(69.4213790495086,242.328536560427,7.08745246144888)) ;
#70593=CARTESIAN_POINT('Ctrl Pts',(69.5531897217821,242.292089762554,6.86383160650544)) ;
#70594=CARTESIAN_POINT('Ctrl Pts',(69.7424264478363,242.29914527047,6.59616795491574)) ;
#70595=CARTESIAN_POINT('Ctrl Pts',(69.8891297803734,242.347952204288,6.43101832592783)) ;
#70596=CARTESIAN_POINT('Ctrl Pts',(69.9764181098155,242.394722276976,6.35118125015187)) ;
#70597=CARTESIAN_POINT('Ctrl Pts',(70.0753852288502,242.462564006987,6.27633386832372)) ;
#70598=CARTESIAN_POINT('Ctrl Pts',(70.1820851481564,242.579361897691,6.24313659439274)) ;
#70599=CARTESIAN_POINT('Ctrl Pts',(70.2851436276679,242.795516871846,6.32501770065842)) ;
#70600=CARTESIAN_POINT('Ctrl Pts',(70.2953060969612,242.938129691503,6.46512808573764)) ;
#70601=CARTESIAN_POINT('Ctrl Pts',(70.2852400421153,243.040198107596,6.5889491341787)) ;
#70602=CARTESIAN_POINT('Ctrl Pts',(70.2733858425031,243.119595484145,6.69087987237211)) ;
#70603=CARTESIAN_POINT('Ctrl Pts',(70.2309948427504,243.252450612718,6.89202719270369)) ;
#70604=CARTESIAN_POINT('Ctrl Pts',(70.1650063280899,243.352071612089,7.0874726393318)) ;
#70605=CARTESIAN_POINT('Ctrl Pts',(70.1208581955899,243.401953083345,7.19960833954767)) ;
#70606=CARTESIAN_POINT('Ctrl Pts',(69.2980284313546,242.282143340439,7.17608503413729)) ;
#70607=CARTESIAN_POINT('Ctrl Pts',(69.3662601562767,242.258303056981,7.06213458186476)) ;
#70608=CARTESIAN_POINT('Ctrl Pts',(69.5117541198825,242.228719169598,6.83550818080611)) ;
#70609=CARTESIAN_POINT('Ctrl Pts',(69.7176650261854,242.248060838742,6.56510244268801)) ;
#70610=CARTESIAN_POINT('Ctrl Pts',(69.8767158105699,242.30846111626,6.39850449270415)) ;
#70611=CARTESIAN_POINT('Ctrl Pts',(69.9714892930823,242.363136499339,6.31801004275899)) ;
#70612=CARTESIAN_POINT('Ctrl Pts',(70.0791779627476,242.440864892285,6.24257136321944)) ;
#70613=CARTESIAN_POINT('Ctrl Pts',(70.1963946085699,242.571276507691,6.20912630982003)) ;
#70614=CARTESIAN_POINT('Ctrl Pts',(70.3137925639844,242.809340189588,6.29162715593499)) ;
#70615=CARTESIAN_POINT('Ctrl Pts',(70.3308790897817,242.965626066389,6.43287720578516)) ;
#70616=CARTESIAN_POINT('Ctrl Pts',(70.3251826391914,243.07816667912,6.55786814745459)) ;
#70617=CARTESIAN_POINT('Ctrl Pts',(70.3165658070084,243.16580527229,6.66078695502675)) ;
#70618=CARTESIAN_POINT('Ctrl Pts',(70.2787474042028,243.313338909124,6.8640798425796)) ;
#70619=CARTESIAN_POINT('Ctrl Pts',(70.2147697560625,243.426197514365,7.06215508260825)) ;
#70620=CARTESIAN_POINT('Ctrl Pts',(70.1710194090925,243.483712338908,7.1760850341133)) ;
#70621=CARTESIAN_POINT('Ctrl Pts',(69.2807493616358,242.245816755683,7.17267980086572)) ;
#70622=CARTESIAN_POINT('Ctrl Pts',(69.3508960370599,242.223719506269,7.05716455407472)) ;
#70623=CARTESIAN_POINT('Ctrl Pts',(69.5001356158098,242.198132189401,6.82777004955092)) ;
#70624=CARTESIAN_POINT('Ctrl Pts',(69.710911608549,242.223881724253,6.55459071024847)) ;
#70625=CARTESIAN_POINT('Ctrl Pts',(69.8739373345158,242.28994594427,6.38643949106947)) ;
#70626=CARTESIAN_POINT('Ctrl Pts',(69.9712979550201,242.348344696013,6.30522193492245)) ;
#70627=CARTESIAN_POINT('Ctrl Pts',(70.082153166785,242.43062586115,6.22912187988088)) ;
#70628=CARTESIAN_POINT('Ctrl Pts',(70.2036250939698,242.567006326368,6.19539313305328)) ;
#70629=CARTESIAN_POINT('Ctrl Pts',(70.3276776120394,242.813968315643,6.2785997126966)) ;
#70630=CARTESIAN_POINT('Ctrl Pts',(70.348633230693,242.975275641354,6.42110958166891)) ;
#70631=CARTESIAN_POINT('Ctrl Pts',(70.3456213203833,243.09149482855,6.54731984380613)) ;
#70632=CARTESIAN_POINT('Ctrl Pts',(70.3390649159907,243.181991491806,6.65125847587959)) ;
#70633=CARTESIAN_POINT('Ctrl Pts',(70.3045673928554,243.334423102977,6.85669008267818)) ;
#70634=CARTESIAN_POINT('Ctrl Pts',(70.2429130851605,243.451496989519,7.05718533633929)) ;
#70635=CARTESIAN_POINT('Ctrl Pts',(70.2002285180491,243.511371242796,7.17267980084141)) ;
#70636=CARTESIAN_POINT('Ctrl Pts',(70.2002285180491,243.511371242796,7.17267980084141)) ;
#70637=CARTESIAN_POINT('Ctrl Pts',(70.2313933057879,243.467655948939,7.08835516749437)) ;
#70638=CARTESIAN_POINT('Ctrl Pts',(70.2585789380893,243.42009714279,7.00442256017519)) ;
#70639=CARTESIAN_POINT('Ctrl Pts',(70.2809775421819,243.368344041036,6.92172413787986)) ;
#70640=CARTESIAN_POINT('Ctrl Pts',(70.2858591151139,243.357064921158,6.90370076561406)) ;
#70641=CARTESIAN_POINT('Ctrl Pts',(70.2905133120903,243.345586461082,6.88573585920702)) ;
#70642=CARTESIAN_POINT('Ctrl Pts',(70.2949317635032,243.33390483265,6.86783787320399)) ;
#70643=CARTESIAN_POINT('Ctrl Pts',(70.2979780832332,243.325850885272,6.85549803220697)) ;
#70644=CARTESIAN_POINT('Ctrl Pts',(70.3009109484532,243.317698916943,6.84319006572952)) ;
#70645=CARTESIAN_POINT('Ctrl Pts',(70.3037274475218,243.309447539126,6.83091681197913)) ;
#70646=CARTESIAN_POINT('Ctrl Pts',(70.3204319542847,243.260509054436,6.75812479420123)) ;
#70647=CARTESIAN_POINT('Ctrl Pts',(70.3330403214039,243.208071641295,6.6865553202387)) ;
#70648=CARTESIAN_POINT('Ctrl Pts',(70.3401180984443,243.151348445742,6.61757279026188)) ;
#70649=CARTESIAN_POINT('Ctrl Pts',(70.3411905548211,243.142753493904,6.60712024933831)) ;
#70650=CARTESIAN_POINT('Ctrl Pts',(70.3421361030927,243.134060194437,6.59672706305293)) ;
#70651=CARTESIAN_POINT('Ctrl Pts',(70.3429498371333,243.125265870193,6.58639792831063)) ;
#70652=CARTESIAN_POINT('Ctrl Pts',(70.3439815081954,243.114116220087,6.57330240953252)) ;
#70653=CARTESIAN_POINT('Ctrl Pts',(70.344801294108,243.102804186611,6.56030986280214)) ;
#70654=CARTESIAN_POINT('Ctrl Pts',(70.3453617679955,243.091339667682,6.5475056875169)) ;
#70655=CARTESIAN_POINT('Ctrl Pts',(70.3459224809741,243.079870258134,6.53469605013184)) ;
#70656=CARTESIAN_POINT('Ctrl Pts',(70.346223677288,243.068248220193,6.52207490449511)) ;
#70657=CARTESIAN_POINT('Ctrl Pts',(70.3462973843869,243.056426804173,6.50953957109844)) ;
#70658=CARTESIAN_POINT('Ctrl Pts',(70.346312595762,243.053987147801,6.50695257932533)) ;
#70659=CARTESIAN_POINT('Ctrl Pts',(70.3463181179843,243.051539000306,6.50436924332236)) ;
#70660=CARTESIAN_POINT('Ctrl Pts',(70.3463136044882,243.049082390573,6.50179014031024)) ;
#70661=CARTESIAN_POINT('Ctrl Pts',(70.3462749444578,243.028040474061,6.47969901630214)) ;
#70662=CARTESIAN_POINT('Ctrl Pts',(70.3454302657341,243.006412398833,6.45803982307202)) ;
#70663=CARTESIAN_POINT('Ctrl Pts',(70.3436337525118,242.984193617895,6.43706415935564)) ;
#70664=CARTESIAN_POINT('Ctrl Pts',(70.3419956946639,242.963934569402,6.41793858313386)) ;
#70665=CARTESIAN_POINT('Ctrl Pts',(70.339566698251,242.943184067893,6.39938013482495)) ;
#70666=CARTESIAN_POINT('Ctrl Pts',(70.336207088231,242.921910636217,6.38158470105561)) ;
#70667=CARTESIAN_POINT('Ctrl Pts',(70.332847478211,242.900637204541,6.36378926728627)) ;
#70668=CARTESIAN_POINT('Ctrl Pts',(70.3285580513409,242.878841054704,6.34675571504515)) ;
#70669=CARTESIAN_POINT('Ctrl Pts',(70.3231594750068,242.856461675999,6.3307017817941)) ;
#70670=CARTESIAN_POINT('Ctrl Pts',(70.3179443203035,242.834842657411,6.31519329579368)) ;
#70671=CARTESIAN_POINT('Ctrl Pts',(70.3117103388422,242.812760858963,6.30066206320242)) ;
#70672=CARTESIAN_POINT('Ctrl Pts',(70.3042672680503,242.790239415608,6.28741860766138)) ;
#70673=CARTESIAN_POINT('Ctrl Pts',(70.2982890477912,242.772150356308,6.27678156061052)) ;
#70674=CARTESIAN_POINT('Ctrl Pts',(70.2915312746284,242.753778155301,6.26697531069235)) ;
#70675=CARTESIAN_POINT('Ctrl Pts',(70.2839131880942,242.735149852357,6.2581530367002)) ;
#70676=CARTESIAN_POINT('Ctrl Pts',(70.2762425980247,242.716393163924,6.249269959963)) ;
#70677=CARTESIAN_POINT('Ctrl Pts',(70.2676997909606,242.69737744558,6.24138521936161)) ;
#70678=CARTESIAN_POINT('Ctrl Pts',(70.2582982006726,242.678406955222,6.23482036252682)) ;
#70679=CARTESIAN_POINT('Ctrl Pts',(70.2505801554145,242.662833515126,6.22943107618143)) ;
#70680=CARTESIAN_POINT('Ctrl Pts',(70.2422224563955,242.647221418542,6.22494162734417)) ;
#70681=CARTESIAN_POINT('Ctrl Pts',(70.2332777382532,242.631713974233,6.22144947621304)) ;
#70682=CARTESIAN_POINT('Ctrl Pts',(70.2282164607882,242.62293924515,6.21947347813873)) ;
#70683=CARTESIAN_POINT('Ctrl Pts',(70.2229666179565,242.614197342908,6.21781685667503)) ;
#70684=CARTESIAN_POINT('Ctrl Pts',(70.2175328092121,242.605508743235,6.21649820450614)) ;
#70685=CARTESIAN_POINT('Ctrl Pts',(70.2163743948262,242.603656451532,6.21621708573398)) ;
#70686=CARTESIAN_POINT('Ctrl Pts',(70.2152080325008,242.601806717165,6.21595091938064)) ;
#70687=CARTESIAN_POINT('Ctrl Pts',(70.2140335854535,242.599959879669,6.21570025794295)) ;
#70688=CARTESIAN_POINT('Ctrl Pts',(70.2055139162308,242.586562558252,6.21388191071223)) ;
#70689=CARTESIAN_POINT('Ctrl Pts',(70.1965658083798,242.573314830591,6.21288076424351)) ;
#70690=CARTESIAN_POINT('Ctrl Pts',(70.1872375019662,242.560327455973,6.21273140721762)) ;
#70691=CARTESIAN_POINT('Ctrl Pts',(70.1850974079421,242.557347900888,6.21269714182534)) ;
#70692=CARTESIAN_POINT('Ctrl Pts',(70.1829374521883,242.55438219318,6.21270764357374)) ;
#70693=CARTESIAN_POINT('Ctrl Pts',(70.1807584781267,242.551431924514,6.21276321324356)) ;
#70694=CARTESIAN_POINT('Ctrl Pts',(70.1687049623989,242.535111808368,6.21307061015158)) ;
#70695=CARTESIAN_POINT('Ctrl Pts',(70.1560696732988,242.519265969027,6.2147585524089)) ;
#70696=CARTESIAN_POINT('Ctrl Pts',(70.1430567186737,242.504001518625,6.21764257922973)) ;
#70697=CARTESIAN_POINT('Ctrl Pts',(70.1289995289569,242.487512160027,6.2207580371205)) ;
#70698=CARTESIAN_POINT('Ctrl Pts',(70.1144902283092,242.471701143486,6.22528409350145)) ;
#70699=CARTESIAN_POINT('Ctrl Pts',(70.0996916826711,242.456735839965,6.23114390838201)) ;
#70700=CARTESIAN_POINT('Ctrl Pts',(70.0939033603583,242.450882291758,6.23343592396595)) ;
#70701=CARTESIAN_POINT('Ctrl Pts',(70.0880709269218,242.445158604079,6.23593225992976)) ;
#70702=CARTESIAN_POINT('Ctrl Pts',(70.0822047726577,242.43957665699,6.23862924141461)) ;
#70703=CARTESIAN_POINT('Ctrl Pts',(70.0699166428066,242.427883870275,6.24427874485421)) ;
#70704=CARTESIAN_POINT('Ctrl Pts',(70.0574947471439,242.416711633889,6.25069645438963)) ;
#70705=CARTESIAN_POINT('Ctrl Pts',(70.0450391756289,242.406159149867,6.25783532677176)) ;
#70706=CARTESIAN_POINT('Ctrl Pts',(70.0267404124392,242.390656255764,6.2683232064331)) ;
#70707=CARTESIAN_POINT('Ctrl Pts',(70.0083678172079,242.37649017468,6.28036889709359)) ;
#70708=CARTESIAN_POINT('Ctrl Pts',(69.9900275617557,242.363426272423,6.29352850225734)) ;
#70709=CARTESIAN_POINT('Ctrl Pts',(69.9838292441962,242.359011164086,6.29797595458291)) ;
#70710=CARTESIAN_POINT('Ctrl Pts',(69.9776349202651,242.354722200375,6.30255041575482)) ;
#70711=CARTESIAN_POINT('Ctrl Pts',(69.9714495377026,242.350551114819,6.30723414323133)) ;
#70712=CARTESIAN_POINT('Ctrl Pts',(69.9546992737991,242.339255647946,6.31991786497235)) ;
#70713=CARTESIAN_POINT('Ctrl Pts',(69.9380132958858,242.328823185994,6.33340373088781)) ;
#70714=CARTESIAN_POINT('Ctrl Pts',(69.9214895956895,242.319297806037,6.34757136463829)) ;
#70715=CARTESIAN_POINT('Ctrl Pts',(69.9138517594529,242.314894839913,6.35412014397709)) ;
#70716=CARTESIAN_POINT('Ctrl Pts',(69.9062427572804,242.310664931116,6.36080436695981)) ;
#70717=CARTESIAN_POINT('Ctrl Pts',(69.8986686267112,242.306604278837,6.3676101865645)) ;
#70718=CARTESIAN_POINT('Ctrl Pts',(69.8659264492777,242.289050502043,6.39703103573528)) ;
#70719=CARTESIAN_POINT('Ctrl Pts',(69.8338335372565,242.274655893542,6.42872449053609)) ;
#70720=CARTESIAN_POINT('Ctrl Pts',(69.8024037650707,242.262721225499,6.46185807151192)) ;
#70721=CARTESIAN_POINT('Ctrl Pts',(69.7878029806823,242.257176943669,6.47725036481219)) ;
#70722=CARTESIAN_POINT('Ctrl Pts',(69.7733457297794,242.252164212083,6.49295339842054)) ;
#70723=CARTESIAN_POINT('Ctrl Pts',(69.7590354098376,242.247615994147,6.50888317841182)) ;
#70724=CARTESIAN_POINT('Ctrl Pts',(69.7375091503596,242.240774349805,6.53284550622236)) ;
#70725=CARTESIAN_POINT('Ctrl Pts',(69.7163151111706,242.234983455156,6.55732102883111)) ;
#70726=CARTESIAN_POINT('Ctrl Pts',(69.6954473136586,242.230180873332,6.58223895379559)) ;
#70727=CARTESIAN_POINT('Ctrl Pts',(69.6546794117156,242.220798417672,6.6309192958869)) ;
#70728=CARTESIAN_POINT('Ctrl Pts',(69.615164454165,242.214993311974,6.6811176994941)) ;
#70729=CARTESIAN_POINT('Ctrl Pts',(69.5767655747089,242.212087601469,6.73226793926176)) ;
#70730=CARTESIAN_POINT('Ctrl Pts',(69.5524260639884,242.210245788037,6.76469002622929)) ;
#70731=CARTESIAN_POINT('Ctrl Pts',(69.5285355441474,242.209570019988,6.79749468373767)) ;
#70732=CARTESIAN_POINT('Ctrl Pts',(69.5050643349143,242.20989684534,6.83053755702586)) ;
#70733=CARTESIAN_POINT('Ctrl Pts',(69.4647641483364,242.210458006145,6.88727233985513)) ;
#70734=CARTESIAN_POINT('Ctrl Pts',(69.4256984745267,242.213972936061,6.94471044687498)) ;
#70735=CARTESIAN_POINT('Ctrl Pts',(69.3878301535716,242.220237135349,7.00265575379959)) ;
#70736=CARTESIAN_POINT('Ctrl Pts',(69.3510225444185,242.226325871085,7.05897798187159)) ;
#70737=CARTESIAN_POINT('Ctrl Pts',(69.3153324323798,242.234922572387,7.11572953305061)) ;
#70738=CARTESIAN_POINT('Ctrl Pts',(69.2807493616506,242.245816755679,7.17267980084179)) ;
#70739=CARTESIAN_POINT('Ctrl Pts',(69.4909429592547,242.355402012489,7.27867958886636)) ;
#70740=CARTESIAN_POINT('Ctrl Pts',(69.5434105984377,242.338566553604,7.16316434207535)) ;
#70741=CARTESIAN_POINT('Ctrl Pts',(69.6548363472646,242.318447141452,6.93376983755156)) ;
#70742=CARTESIAN_POINT('Ctrl Pts',(69.8115179376631,242.335283243238,6.66059049824912)) ;
#70743=CARTESIAN_POINT('Ctrl Pts',(69.9320961586154,242.382043605764,6.4924392790701)) ;
#70744=CARTESIAN_POINT('Ctrl Pts',(70.0038423289643,242.42384128837,6.4112217229231)) ;
#70745=CARTESIAN_POINT('Ctrl Pts',(70.0853128564862,242.483004335118,6.33512166788152)) ;
#70746=CARTESIAN_POINT('Ctrl Pts',(70.1739356804575,242.581754164171,6.30139292105391)) ;
#70747=CARTESIAN_POINT('Ctrl Pts',(70.2630551704512,242.761871347334,6.38459950069724)) ;
#70748=CARTESIAN_POINT('Ctrl Pts',(70.2766922354173,242.880428587697,6.52710936966954)) ;
#70749=CARTESIAN_POINT('Ctrl Pts',(70.2731493424206,242.966128315359,6.65331963180678)) ;
#70750=CARTESIAN_POINT('Ctrl Pts',(70.2672749757801,243.03292209962,6.75725826388023)) ;
#70751=CARTESIAN_POINT('Ctrl Pts',(70.2400533595442,243.145774108243,6.96268987067883)) ;
#70752=CARTESIAN_POINT('Ctrl Pts',(70.1931792067253,243.232912339636,7.16318512433994)) ;
#70753=CARTESIAN_POINT('Ctrl Pts',(70.1609601392448,243.277601545414,7.27867958884205)) ;
#70754=CARTESIAN_POINT('Origin',(77.0279509268838,244.633742383918,7.2786795888419)) ;
#70755=CARTESIAN_POINT('',(76.8665793939902,244.751891562381,7.27867958883744)) ;
#70756=CARTESIAN_POINT('Origin',(77.0279509268838,244.633742383918,7.2786795888419)) ;
#70757=CARTESIAN_POINT('',(77.1010421843896,244.786783924096,7.1726798008414)) ;
#70758=CARTESIAN_POINT('Origin',(77.0279509268838,244.633742383918,7.2786795888419)) ;
#70759=CARTESIAN_POINT('Origin',(77.0279509268823,244.633742383915,7.27867958883784)) ;
#70760=CARTESIAN_POINT('Origin',(69.2946204451421,241.899588097824,7.2786795888419)) ;
#70761=CARTESIAN_POINT('',(69.1764712666787,241.738216564931,7.27867958883751)) ;
#70762=CARTESIAN_POINT('Origin',(69.2946204451421,241.899588097824,7.2786795888419)) ;
#70763=CARTESIAN_POINT('',(69.141578904964,241.97267935533,7.17267980084143)) ;
#70764=CARTESIAN_POINT('Origin',(69.2946204451421,241.899588097824,7.2786795888419)) ;
#70765=CARTESIAN_POINT('Origin',(69.2946204451441,241.899588097823,7.27867958883792)) ;
#70766=CARTESIAN_POINT('Origin',(74.5283628290597,239.4,7.2786795888419)) ;
#70767=CARTESIAN_POINT('Origin',(74.5283628290597,239.4,7.17267980084126)) ;
#70768=CARTESIAN_POINT('Origin',(77.2933283411274,244.498525837657,7.27867958886636)) ;
#70769=CARTESIAN_POINT('',(77.4837648414508,244.437419869498,7.27867958819177)) ;
#70770=CARTESIAN_POINT('Origin',(77.2933283411226,244.498525837642,7.27867958812533)) ;
#70771=CARTESIAN_POINT('',(77.3741795847345,244.647613467411,7.17267980084127)) ;
#70772=CARTESIAN_POINT('Origin',(77.2933283411274,244.498525837657,7.27867958886636)) ;
#70773=CARTESIAN_POINT('Origin',(77.2933283411226,244.498525837642,7.2786795888419)) ;
#70774=CARTESIAN_POINT('Origin',(68.8249552755829,240.454107337488,7.27867958884205)) ;
#70775=CARTESIAN_POINT('',(68.8242223895113,240.654105994678,7.27867958883789)) ;
#70776=CARTESIAN_POINT('Origin',(68.824955275583,240.454107337488,7.27867958883748)) ;
#70777=CARTESIAN_POINT('',(68.6581801055003,240.48493082833,7.17267980084126)) ;
#70778=CARTESIAN_POINT('Origin',(68.8249552755829,240.454107337488,7.27867958884205)) ;
#70779=CARTESIAN_POINT('Origin',(68.824955275583,240.454107337488,7.2786795888419)) ;
#70780=CARTESIAN_POINT('Ctrl Pts',(68.823478978367,240.65410371336,7.28036633815045)) ;
#70781=CARTESIAN_POINT('Ctrl Pts',(68.8788199964157,240.654238914554,7.16431454328368)) ;
#70782=CARTESIAN_POINT('Ctrl Pts',(68.9912316969021,240.669605262881,6.93452062458097)) ;
#70783=CARTESIAN_POINT('Ctrl Pts',(69.1352415531504,240.73427548165,6.66105171324341)) ;
#70784=CARTESIAN_POINT('Ctrl Pts',(69.2496672165496,240.827807397918,6.46924271771741)) ;
#70785=CARTESIAN_POINT('Ctrl Pts',(69.3181848499291,240.911256512681,6.37322074285091)) ;
#70786=CARTESIAN_POINT('Ctrl Pts',(69.3655488171773,240.996556047987,6.32731305663253)) ;
#70787=CARTESIAN_POINT('Ctrl Pts',(69.3941022131729,241.068181512082,6.31494113130069)) ;
#70788=CARTESIAN_POINT('Ctrl Pts',(69.413116155554,241.142937408252,6.32730060289559)) ;
#70789=CARTESIAN_POINT('Ctrl Pts',(69.4249419942325,241.239765149908,6.37317673297408)) ;
#70790=CARTESIAN_POINT('Ctrl Pts',(69.4185389338756,241.347617143788,6.46930275432656)) ;
#70791=CARTESIAN_POINT('Ctrl Pts',(69.3809619428502,241.490548424926,6.66107020782191)) ;
#70792=CARTESIAN_POINT('Ctrl Pts',(69.3024638526453,241.627509960403,6.93454546811374)) ;
#70793=CARTESIAN_POINT('Ctrl Pts',(69.2205648017604,241.706016476848,7.16431125123397)) ;
#70794=CARTESIAN_POINT('Ctrl Pts',(69.1758711574328,241.738655389459,7.28036638463671)) ;
#70795=CARTESIAN_POINT('Ctrl Pts',(68.7780040901399,240.654014301732,7.25145035187167)) ;
#70796=CARTESIAN_POINT('Ctrl Pts',(68.8361499763342,240.649853313117,7.13668818254113)) ;
#70797=CARTESIAN_POINT('Ctrl Pts',(68.9558559523436,240.658260475784,6.90908120499668)) ;
#70798=CARTESIAN_POINT('Ctrl Pts',(69.112073402727,240.719105343023,6.63766971564194)) ;
#70799=CARTESIAN_POINT('Ctrl Pts',(69.2372083217771,240.814333745853,6.44712593764351)) ;
#70800=CARTESIAN_POINT('Ctrl Pts',(69.3122241176583,240.90152651754,6.35169043930914)) ;
#70801=CARTESIAN_POINT('Ctrl Pts',(69.3637764481677,240.991827836744,6.30605413587496)) ;
#70802=CARTESIAN_POINT('Ctrl Pts',(69.3945159315641,241.068042932172,6.29375442711715)) ;
#70803=CARTESIAN_POINT('Ctrl Pts',(69.414463970372,241.14780971815,6.30604175826672)) ;
#70804=CARTESIAN_POINT('Ctrl Pts',(69.4258401804862,241.251136693392,6.35164665503157)) ;
#70805=CARTESIAN_POINT('Ctrl Pts',(69.4163843073265,241.36586689815,6.44718573025484)) ;
#70806=CARTESIAN_POINT('Ctrl Pts',(69.371131407933,241.516431939832,6.63768809472266)) ;
#70807=CARTESIAN_POINT('Ctrl Pts',(69.2805145667129,241.657492172259,6.90910596666903)) ;
#70808=CARTESIAN_POINT('Ctrl Pts',(69.1886219438466,241.734645309753,7.13668492609714)) ;
#70809=CARTESIAN_POINT('Ctrl Pts',(69.1391337530583,241.765457193289,7.25145039784871)) ;
#70810=CARTESIAN_POINT('Ctrl Pts',(68.6991046675913,240.613567029917,7.20122166120201)) ;
#70811=CARTESIAN_POINT('Ctrl Pts',(68.7657033479242,240.607047577728,7.08855078925677)) ;
#70812=CARTESIAN_POINT('Ctrl Pts',(68.9025872549629,240.61314163398,6.86454768292916)) ;
#70813=CARTESIAN_POINT('Ctrl Pts',(69.0806405675914,240.67860356143,6.59660315772466)) ;
#70814=CARTESIAN_POINT('Ctrl Pts',(69.2227090288745,240.783604097628,6.40822147676959)) ;
#70815=CARTESIAN_POINT('Ctrl Pts',(69.3076059616354,240.880485387066,6.31379600947305)) ;
#70816=CARTESIAN_POINT('Ctrl Pts',(69.365700953512,240.981120970982,6.26862892350856)) ;
#70817=CARTESIAN_POINT('Ctrl Pts',(69.4001749811632,241.066198804175,6.25645417405324)) ;
#70818=CARTESIAN_POINT('Ctrl Pts',(69.4223088609324,241.155321559545,6.26861663959037)) ;
#70819=CARTESIAN_POINT('Ctrl Pts',(69.4344701867662,241.270860282556,6.31375261664818)) ;
#70820=CARTESIAN_POINT('Ctrl Pts',(69.4227020381915,241.399218428313,6.40828062353936)) ;
#70821=CARTESIAN_POINT('Ctrl Pts',(69.3695104139579,241.567684448781,6.59662156925732)) ;
#70822=CARTESIAN_POINT('Ctrl Pts',(69.2639336121494,241.725291673058,6.86457223317537)) ;
#70823=CARTESIAN_POINT('Ctrl Pts',(69.1567902570243,241.810683344395,7.08854759093498)) ;
#70824=CARTESIAN_POINT('Ctrl Pts',(69.099077085805,241.844555641315,7.20122170635049)) ;
#70825=CARTESIAN_POINT('Ctrl Pts',(68.6623516026379,240.524842467592,7.1777195209085)) ;
#70826=CARTESIAN_POINT('Ctrl Pts',(68.7349260692677,240.52314980779,7.06324272629545)) ;
#70827=CARTESIAN_POINT('Ctrl Pts',(68.8827380168196,240.540035758777,6.83622590255729)) ;
#70828=CARTESIAN_POINT('Ctrl Pts',(69.0728764366945,240.622376363191,6.56553617725173)) ;
#70829=CARTESIAN_POINT('Ctrl Pts',(69.2242737408035,240.744355820845,6.37550092461942)) ;
#70830=CARTESIAN_POINT('Ctrl Pts',(69.315021033008,240.854064083064,6.2803201868701)) ;
#70831=CARTESIAN_POINT('Ctrl Pts',(69.3777411120263,240.966598605412,6.23480565964425)) ;
#70832=CARTESIAN_POINT('Ctrl Pts',(69.415512997241,241.061210952531,6.2225387622577)) ;
#70833=CARTESIAN_POINT('Ctrl Pts',(69.4405843624923,241.159989075466,6.23479331069613)) ;
#70834=CARTESIAN_POINT('Ctrl Pts',(69.4559976225698,241.28787069269,6.28027651889111)) ;
#70835=CARTESIAN_POINT('Ctrl Pts',(69.4470369050469,241.430051431758,6.37556053614025)) ;
#70836=CARTESIAN_POINT('Ctrl Pts',(69.3962783214387,241.617736510688,6.56555452752839)) ;
#70837=CARTESIAN_POINT('Ctrl Pts',(69.2908455632846,241.796102429654,6.83625059124941)) ;
#70838=CARTESIAN_POINT('Ctrl Pts',(69.1812048429608,241.896648294788,7.06323947800677)) ;
#70839=CARTESIAN_POINT('Ctrl Pts',(69.1214942201225,241.93793823252,7.17771956677077)) ;
#70840=CARTESIAN_POINT('Ctrl Pts',(68.6571253579994,240.484922057358,7.17433674456111)) ;
#70841=CARTESIAN_POINT('Ctrl Pts',(68.7309893897257,240.48548685222,7.05828627896513)) ;
#70842=CARTESIAN_POINT('Ctrl Pts',(68.8811399119051,240.507354683134,6.82849461444546)) ;
#70843=CARTESIAN_POINT('Ctrl Pts',(69.0739290706077,240.597304732332,6.55502782380495)) ;
#70844=CARTESIAN_POINT('Ctrl Pts',(69.2276518090002,240.726855840636,6.36322013241374)) ;
#70845=CARTESIAN_POINT('Ctrl Pts',(69.320093824317,240.842215057189,6.26719876206499)) ;
#70846=CARTESIAN_POINT('Ctrl Pts',(69.3844106748995,240.959918688398,6.22129135557805)) ;
#70847=CARTESIAN_POINT('Ctrl Pts',(69.4234866951096,241.058618246624,6.20891950468442)) ;
#70848=CARTESIAN_POINT('Ctrl Pts',(69.4499063975124,241.16147279248,6.22127890191958)) ;
#70849=CARTESIAN_POINT('Ctrl Pts',(69.4670654246099,241.294472860653,6.26715475242069)) ;
#70850=CARTESIAN_POINT('Ctrl Pts',(69.460057572545,241.442227922388,6.36328016877133)) ;
#70851=CARTESIAN_POINT('Ctrl Pts',(69.4118663483261,241.63739962514,6.55504631826445)) ;
#70852=CARTESIAN_POINT('Ctrl Pts',(69.308762748304,241.823482930368,6.82851945789384)) ;
#70853=CARTESIAN_POINT('Ctrl Pts',(69.2001577213478,241.929432109674,7.05828298695213)) ;
#70854=CARTESIAN_POINT('Ctrl Pts',(69.1407307279281,241.973306433417,7.17433679104683)) ;
#70855=CARTESIAN_POINT('Ctrl Pts',(69.141578904964,241.97267935533,7.17267980084139)) ;
#70856=CARTESIAN_POINT('Ctrl Pts',(69.20067570445,241.928926404034,7.05718689586838)) ;
#70857=CARTESIAN_POINT('Ctrl Pts',(69.3089595963666,241.823127655304,6.8279973358951)) ;
#70858=CARTESIAN_POINT('Ctrl Pts',(69.4118663483261,241.63739962514,6.55504631826448)) ;
#70859=CARTESIAN_POINT('Ctrl Pts',(69.4600575725451,241.442227922388,6.36328016877132)) ;
#70860=CARTESIAN_POINT('Ctrl Pts',(69.4670654246099,241.294472860653,6.2671547524207)) ;
#70861=CARTESIAN_POINT('Ctrl Pts',(69.4499063975123,241.16147279248,6.22127890191957)) ;
#70862=CARTESIAN_POINT('Ctrl Pts',(69.4234866951097,241.058618246625,6.20891950468443)) ;
#70863=CARTESIAN_POINT('Ctrl Pts',(69.3844106748994,240.959918688398,6.22129135557804)) ;
#70864=CARTESIAN_POINT('Ctrl Pts',(69.320093824317,240.84221505719,6.26719876206501)) ;
#70865=CARTESIAN_POINT('Ctrl Pts',(69.2276518090002,240.726855840635,6.36322013241375)) ;
#70866=CARTESIAN_POINT('Ctrl Pts',(69.0739290706076,240.597304732333,6.55502782380495)) ;
#70867=CARTESIAN_POINT('Ctrl Pts',(68.8815079899584,240.507526418096,6.82797250456833)) ;
#70868=CARTESIAN_POINT('Ctrl Pts',(68.7317057496143,240.485591464222,7.05719005384199)) ;
#70869=CARTESIAN_POINT('Ctrl Pts',(68.6581801055003,240.48493082833,7.17267980084126)) ;
#70870=CARTESIAN_POINT('Ctrl Pts',(68.8242223895114,240.654105994679,7.27867958883793)) ;
#70871=CARTESIAN_POINT('Ctrl Pts',(68.846136652679,240.654186298509,7.23273887151479)) ;
#70872=CARTESIAN_POINT('Ctrl Pts',(68.8681968853879,240.655463750951,7.18693755682195)) ;
#70873=CARTESIAN_POINT('Ctrl Pts',(68.8904046060548,240.658011322165,7.14139111650319)) ;
#70874=CARTESIAN_POINT('Ctrl Pts',(68.9117833995295,240.660463802528,7.09754474632908)) ;
#70875=CARTESIAN_POINT('Ctrl Pts',(68.9332997260423,240.664093734056,7.05393457870595)) ;
#70876=CARTESIAN_POINT('Ctrl Pts',(68.9549311097582,240.669007419404,7.01066363168771)) ;
#70877=CARTESIAN_POINT('Ctrl Pts',(68.9673169131455,240.671820921372,6.98588734140569)) ;
#70878=CARTESIAN_POINT('Ctrl Pts',(68.9797399341188,240.675056046509,6.96122226577)) ;
#70879=CARTESIAN_POINT('Ctrl Pts',(68.9921905637294,240.678738386296,6.93668774373476)) ;
#70880=CARTESIAN_POINT('Ctrl Pts',(69.0096876499474,240.683913242409,6.90220895344093)) ;
#70881=CARTESIAN_POINT('Ctrl Pts',(69.0272213641983,240.68996292711,6.86798799566502)) ;
#70882=CARTESIAN_POINT('Ctrl Pts',(69.0448122049251,240.696997581045,6.83420433559753)) ;
#70883=CARTESIAN_POINT('Ctrl Pts',(69.0619154995078,240.70383726315,6.80135702038434)) ;
#70884=CARTESIAN_POINT('Ctrl Pts',(69.0790734570707,240.711608425905,6.76892309859212)) ;
#70885=CARTESIAN_POINT('Ctrl Pts',(69.0962696297009,240.720445534448,6.73706752304788)) ;
#70886=CARTESIAN_POINT('Ctrl Pts',(69.1127093625799,240.728893908803,6.70661323743941)) ;
#70887=CARTESIAN_POINT('Ctrl Pts',(69.1291845017098,240.73831699583,6.67668753562406)) ;
#70888=CARTESIAN_POINT('Ctrl Pts',(69.1456400045051,240.748856968541,6.64743454569603)) ;
#70889=CARTESIAN_POINT('Ctrl Pts',(69.1517207684508,240.752751780317,6.63662475588462)) ;
#70890=CARTESIAN_POINT('Ctrl Pts',(69.1577984019575,240.756799317963,6.62590682536183)) ;
#70891=CARTESIAN_POINT('Ctrl Pts',(69.1638684211109,240.76100744383,6.61528802672607)) ;
#70892=CARTESIAN_POINT('Ctrl Pts',(69.1782061081319,240.770947246342,6.59020589641802)) ;
#70893=CARTESIAN_POINT('Ctrl Pts',(69.1925055813629,240.781780951008,6.56567685055204)) ;
#70894=CARTESIAN_POINT('Ctrl Pts',(69.2067372272363,240.793672247361,6.54202080782637)) ;
#70895=CARTESIAN_POINT('Ctrl Pts',(69.219775148156,240.804566123085,6.52034899157445)) ;
#70896=CARTESIAN_POINT('Ctrl Pts',(69.2327562318609,240.816348281174,6.49940986864529)) ;
#70897=CARTESIAN_POINT('Ctrl Pts',(69.245611680359,240.829162853668,6.47944941873786)) ;
#70898=CARTESIAN_POINT('Ctrl Pts',(69.2467886985169,240.830336129303,6.47762188141132)) ;
#70899=CARTESIAN_POINT('Ctrl Pts',(69.2479646283666,240.83151806915,6.47580254815704)) ;
#70900=CARTESIAN_POINT('Ctrl Pts',(69.2491393952322,240.83270878926,6.47399160776851)) ;
#70901=CARTESIAN_POINT('Ctrl Pts',(69.2620888106481,240.845834056741,6.45402967313127)) ;
#70902=CARTESIAN_POINT('Ctrl Pts',(69.2748961857949,240.860021506773,6.43508752022125)) ;
#70903=CARTESIAN_POINT('Ctrl Pts',(69.2874067034248,240.875395365772,6.41771166031512)) ;
#70904=CARTESIAN_POINT('Ctrl Pts',(69.299351774167,240.890074361378,6.40112114968035)) ;
#70905=CARTESIAN_POINT('Ctrl Pts',(69.3110262930533,240.905835564842,6.38595854597711)) ;
#70906=CARTESIAN_POINT('Ctrl Pts',(69.3222483340953,240.922778337834,6.37269955612442)) ;
#70907=CARTESIAN_POINT('Ctrl Pts',(69.3246968500832,240.926475049545,6.36980660211394)) ;
#70908=CARTESIAN_POINT('Ctrl Pts',(69.3271236375482,240.930227955764,6.36700427164681)) ;
#70909=CARTESIAN_POINT('Ctrl Pts',(69.3295264854414,240.934037981198,6.36429750592655)) ;
#70910=CARTESIAN_POINT('Ctrl Pts',(69.3387699425403,240.948694675342,6.35388491473295)) ;
#70911=CARTESIAN_POINT('Ctrl Pts',(69.347660159287,240.96420569066,6.34488653389899)) ;
#70912=CARTESIAN_POINT('Ctrl Pts',(69.3559890267521,240.980457921475,6.33775012566548)) ;
#70913=CARTESIAN_POINT('Ctrl Pts',(69.3589006596617,240.986139429831,6.33525535658002)) ;
#70914=CARTESIAN_POINT('Ctrl Pts',(69.3617439552097,240.99191114303,6.33298813633262)) ;
#70915=CARTESIAN_POINT('Ctrl Pts',(69.3645109707409,240.997767038799,6.3309675942406)) ;
#70916=CARTESIAN_POINT('Ctrl Pts',(69.3711177208506,241.011749049227,6.32614318449746)) ;
#70917=CARTESIAN_POINT('Ctrl Pts',(69.3772873424095,241.026215350409,6.32272509186126)) ;
#70918=CARTESIAN_POINT('Ctrl Pts',(69.3829030519906,241.040995449201,6.32081869565777)) ;
#70919=CARTESIAN_POINT('Ctrl Pts',(69.3863671653803,241.050112718779,6.31964271379489)) ;
#70920=CARTESIAN_POINT('Ctrl Pts',(69.3896213529679,241.059348834208,6.31904195925508)) ;
#70921=CARTESIAN_POINT('Ctrl Pts',(69.3926471329311,241.06865943203,6.31904116737318)) ;
#70922=CARTESIAN_POINT('Ctrl Pts',(69.3975225423784,241.08366150658,6.31903989142167)) ;
#70923=CARTESIAN_POINT('Ctrl Pts',(69.4018030292884,241.098859895763,6.3205962720868)) ;
#70924=CARTESIAN_POINT('Ctrl Pts',(69.4054500916838,241.114053110503,6.32360639934854)) ;
#70925=CARTESIAN_POINT('Ctrl Pts',(69.4077357611952,241.123574929421,6.32549289191755)) ;
#70926=CARTESIAN_POINT('Ctrl Pts',(69.4097736671126,241.133094421285,6.32795037539676)) ;
#70927=CARTESIAN_POINT('Ctrl Pts',(69.4115646430805,241.142560434417,6.33095327169366)) ;
#70928=CARTESIAN_POINT('Ctrl Pts',(69.4150396945331,241.160927449538,6.33677982622377)) ;
#70929=CARTESIAN_POINT('Ctrl Pts',(69.4175839820238,241.179095664348,6.34465975590413)) ;
#70930=CARTESIAN_POINT('Ctrl Pts',(69.419285579022,241.196845654439,6.35413807111322)) ;
#70931=CARTESIAN_POINT('Ctrl Pts',(69.4198602664029,241.20284043189,6.35733922164867)) ;
#70932=CARTESIAN_POINT('Ctrl Pts',(69.4203392605828,241.208787630448,6.360722690978)) ;
#70933=CARTESIAN_POINT('Ctrl Pts',(69.4207272046842,241.214679245084,6.36427095134432)) ;
#70934=CARTESIAN_POINT('Ctrl Pts',(69.4220878086829,241.235342413832,6.37671546905823)) ;
#70935=CARTESIAN_POINT('Ctrl Pts',(69.4223321688101,241.255328098782,6.39118701019276)) ;
#70936=CARTESIAN_POINT('Ctrl Pts',(69.4216735910866,241.274596981359,6.40719997765687)) ;
#70937=CARTESIAN_POINT('Ctrl Pts',(69.4209847045839,241.294752648119,6.42394988698749)) ;
#70938=CARTESIAN_POINT('Ctrl Pts',(69.4193082317437,241.31412462535,6.44238636507748)) ;
#70939=CARTESIAN_POINT('Ctrl Pts',(69.4168519322734,241.332711197981,6.46195363822342)) ;
#70940=CARTESIAN_POINT('Ctrl Pts',(69.4163524690264,241.336490586459,6.46593244206969)) ;
#70941=CARTESIAN_POINT('Ctrl Pts',(69.4158206373757,241.340237620289,6.46995800094641)) ;
#70942=CARTESIAN_POINT('Ctrl Pts',(69.4152579931402,241.343952456318,6.47402564218845)) ;
#70943=CARTESIAN_POINT('Ctrl Pts',(69.4125278222751,241.361978300102,6.4937634354645)) ;
#70944=CARTESIAN_POINT('Ctrl Pts',(69.4090772342052,241.379237445774,6.51449208817806)) ;
#70945=CARTESIAN_POINT('Ctrl Pts',(69.405050494928,241.395805152101,6.53597027769904)) ;
#70946=CARTESIAN_POINT('Ctrl Pts',(69.4008468772236,241.413100610993,6.55839191752057)) ;
#70947=CARTESIAN_POINT('Ctrl Pts',(69.3960153407041,241.429643264669,6.58163038863598)) ;
#70948=CARTESIAN_POINT('Ctrl Pts',(69.3906659501294,241.445533486518,6.60541115008098)) ;
#70949=CARTESIAN_POINT('Ctrl Pts',(69.3899251894502,241.447733896333,6.60870420800095)) ;
#70950=CARTESIAN_POINT('Ctrl Pts',(69.389174418218,241.449921807944,6.6120076646218)) ;
#70951=CARTESIAN_POINT('Ctrl Pts',(69.3884138526593,241.452097497548,6.61532079094276)) ;
#70952=CARTESIAN_POINT('Ctrl Pts',(69.3817662594347,241.471113740534,6.64427860507523)) ;
#70953=CARTESIAN_POINT('Ctrl Pts',(69.3743746279503,241.489195694726,6.67397512000546)) ;
#70954=CARTESIAN_POINT('Ctrl Pts',(69.366389151171,241.506423764033,6.70426221644862)) ;
#70955=CARTESIAN_POINT('Ctrl Pts',(69.3581585948493,241.524180574135,6.73547884383175)) ;
#70956=CARTESIAN_POINT('Ctrl Pts',(69.3492969611863,241.541031083459,6.7673228596776)) ;
#70957=CARTESIAN_POINT('Ctrl Pts',(69.3399127997696,241.557072117829,6.79963208423623)) ;
#70958=CARTESIAN_POINT('Ctrl Pts',(69.3301475774069,241.573764527582,6.83325328363505)) ;
#70959=CARTESIAN_POINT('Ctrl Pts',(69.3198162940651,241.589581162529,6.86737824012789)) ;
#70960=CARTESIAN_POINT('Ctrl Pts',(69.3089851119557,241.60462816176,6.90182420403309)) ;
#70961=CARTESIAN_POINT('Ctrl Pts',(69.3053399164247,241.609692175438,6.9134168697661)) ;
#70962=CARTESIAN_POINT('Ctrl Pts',(69.3016376626116,241.614668941972,6.92504589391921)) ;
#70963=CARTESIAN_POINT('Ctrl Pts',(69.2978796019434,241.619562210823,6.93670431036293)) ;
#70964=CARTESIAN_POINT('Ctrl Pts',(69.2841507989065,241.637438112838,6.97929438998378)) ;
#70965=CARTESIAN_POINT('Ctrl Pts',(69.2697003402215,241.654174836329,7.02227672706127)) ;
#70966=CARTESIAN_POINT('Ctrl Pts',(69.2546360794563,241.669850154716,7.06555154403451)) ;
#70967=CARTESIAN_POINT('Ctrl Pts',(69.238971885953,241.686149741152,7.11054977643727)) ;
#70968=CARTESIAN_POINT('Ctrl Pts',(69.2226435914711,241.701302627729,7.15586424858313)) ;
#70969=CARTESIAN_POINT('Ctrl Pts',(69.2057177073066,241.715381634963,7.20138278096512)) ;
#70970=CARTESIAN_POINT('Ctrl Pts',(69.1961585686188,241.723332958594,7.22709003263231)) ;
#70971=CARTESIAN_POINT('Ctrl Pts',(69.1864078798304,241.73094141138,7.25286237113867)) ;
#70972=CARTESIAN_POINT('Ctrl Pts',(69.1764712666801,241.73821656493,7.27867958883835)) ;
#70973=CARTESIAN_POINT('Origin',(78.5229277183602,243.60516959767,7.2786795888419)) ;
#70974=CARTESIAN_POINT('',(78.4059643744738,243.767402689815,7.27867958883747)) ;
#70975=CARTESIAN_POINT('Origin',(78.5229277183602,243.60516959767,7.2786795888419)) ;
#70976=CARTESIAN_POINT('',(78.6397340718556,243.728134311011,7.17267980084143)) ;
#70977=CARTESIAN_POINT('Origin',(78.5229277183602,243.60516959767,7.2786795888419)) ;
#70978=CARTESIAN_POINT('Origin',(78.5229277183581,243.605169597668,7.27867958883789)) ;
#70979=CARTESIAN_POINT('Origin',(68.7783628290597,240.159934207678,7.2786795888419)) ;
#70980=CARTESIAN_POINT('',(68.7158628290597,239.969950655759,7.27867958883747)) ;
#70981=CARTESIAN_POINT('Origin',(68.7783628290597,240.159934207678,7.2786795888419)) ;
#70982=CARTESIAN_POINT('',(68.6102252343,240.182155687653,7.17267980084141)) ;
#70983=CARTESIAN_POINT('Origin',(68.7783628290597,240.159934207678,7.2786795888419)) ;
#70984=CARTESIAN_POINT('Origin',(68.7783628290621,240.159934207678,7.27867958883788)) ;
#70985=CARTESIAN_POINT('Origin',(74.5283628290597,239.4,7.2786795888419)) ;
#70986=CARTESIAN_POINT('Origin',(74.5283628290597,239.4,7.17267980084126)) ;
#70987=CARTESIAN_POINT('Origin',(78.7335324267387,243.394564889313,7.27867958886638)) ;
#70988=CARTESIAN_POINT('',(78.8957655186932,243.277601545162,7.27867958819176)) ;
#70989=CARTESIAN_POINT('Origin',(78.7335324267296,243.3945648893,7.27867958812535)) ;
#70990=CARTESIAN_POINT('',(78.8564971400671,243.511371242799,7.17267980084127)) ;
#70991=CARTESIAN_POINT('Origin',(78.7335324267387,243.394564889313,7.27867958886638)) ;
#70992=CARTESIAN_POINT('Origin',(78.7335324267296,243.3945648893,7.2786795888419)) ;
#70993=CARTESIAN_POINT('Origin',(68.7783628290596,238.640065792321,7.27867958884205)) ;
#70994=CARTESIAN_POINT('',(68.7158628290615,238.830049344242,7.27867958883789)) ;
#70995=CARTESIAN_POINT('Origin',(68.7783628290597,238.640065792321,7.27867958883748)) ;
#70996=CARTESIAN_POINT('',(68.6102252343,238.617844312347,7.17267980084126)) ;
#70997=CARTESIAN_POINT('Origin',(68.7783628290596,238.640065792321,7.27867958884205)) ;
#70998=CARTESIAN_POINT('Origin',(68.7783628290597,238.640065792321,7.2786795888419)) ;
#70999=CARTESIAN_POINT('Ctrl Pts',(68.7151564547179,238.829817430435,7.28036646542746)) ;
#71000=CARTESIAN_POINT('Ctrl Pts',(68.7677472638065,238.847047374589,7.16431433428589)) ;
#71001=CARTESIAN_POINT('Ctrl Pts',(68.8699090234134,238.896398863056,6.9345196468735)) ;
#71002=CARTESIAN_POINT('Ctrl Pts',(68.9868866279225,239.002405841546,6.66105002053093)) ;
#71003=CARTESIAN_POINT('Ctrl Pts',(69.0668090557642,239.126720084162,6.46924073836522)) ;
#71004=CARTESIAN_POINT('Ctrl Pts',(69.1061859143773,239.227258632282,6.37321895942679)) ;
#71005=CARTESIAN_POINT('Ctrl Pts',(69.1248724477467,239.323020115618,6.32731193280284)) ;
#71006=CARTESIAN_POINT('Ctrl Pts',(69.1298945349666,239.399963762342,6.31494079700328)) ;
#71007=CARTESIAN_POINT('Ctrl Pts',(69.124876650076,239.476936565362,6.327301195844)) ;
#71008=CARTESIAN_POINT('Ctrl Pts',(69.1062018481551,239.572679465908,6.37317836881852)) ;
#71009=CARTESIAN_POINT('Ctrl Pts',(69.0667835939042,239.673273882465,6.46930552948702)) ;
#71010=CARTESIAN_POINT('Ctrl Pts',(68.9868773192842,239.797597092518,6.66107350241436)) ;
#71011=CARTESIAN_POINT('Ctrl Pts',(68.8698963856411,239.903598102475,6.93455177394916)) ;
#71012=CARTESIAN_POINT('Ctrl Pts',(68.7677473243042,239.952952639913,7.1643141804926)) ;
#71013=CARTESIAN_POINT('Ctrl Pts',(68.7151564542834,239.97018256946,7.28036646653197)) ;
#71014=CARTESIAN_POINT('Ctrl Pts',(68.6719348898594,238.815679885867,7.2514504770069)) ;
#71015=CARTESIAN_POINT('Ctrl Pts',(68.7285208935238,238.829690652319,7.13668797515578)) ;
#71016=CARTESIAN_POINT('Ctrl Pts',(68.8397705467902,238.87467760555,6.90908026728084)) ;
#71017=CARTESIAN_POINT('Ctrl Pts',(68.9695404171102,238.980818841841,6.63766807130544)) ;
#71018=CARTESIAN_POINT('Ctrl Pts',(69.0591237601837,239.110055937278,6.44712401885435)) ;
#71019=CARTESIAN_POINT('Ctrl Pts',(69.1035238771675,239.216163012018,6.35168871470428)) ;
#71020=CARTESIAN_POINT('Ctrl Pts',(69.1246481142455,239.317975797227,6.30605306835811)) ;
#71021=CARTESIAN_POINT('Ctrl Pts',(69.1303309769686,239.399960004748,6.29375414423265)) ;
#71022=CARTESIAN_POINT('Ctrl Pts',(69.1246529708336,239.481987102395,6.30604239722425)) ;
#71023=CARTESIAN_POINT('Ctrl Pts',(69.1035421141245,239.583772178745,6.35164832951223)) ;
#71024=CARTESIAN_POINT('Ctrl Pts',(69.0590949179342,239.689964746438,6.44718853433347)) ;
#71025=CARTESIAN_POINT('Ctrl Pts',(68.9695294166725,239.819176040241,6.63769140569591)) ;
#71026=CARTESIAN_POINT('Ctrl Pts',(68.8397561656441,239.925330127068,6.90911225122715)) ;
#71027=CARTESIAN_POINT('Ctrl Pts',(68.7285209623689,239.970309310713,7.13668782204785)) ;
#71028=CARTESIAN_POINT('Ctrl Pts',(68.6719348893648,239.984320114399,7.25145047810647)) ;
#71029=CARTESIAN_POINT('Ctrl Pts',(68.6093959258621,238.752831004033,7.20122176499298)) ;
#71030=CARTESIAN_POINT('Ctrl Pts',(68.6747498460143,238.767210795544,7.08855056705061)) ;
#71031=CARTESIAN_POINT('Ctrl Pts',(68.8030514227131,238.815306131544,6.8645467034792)) ;
#71032=CARTESIAN_POINT('Ctrl Pts',(68.9521617110681,238.932586154345,6.59660147265197)) ;
#71033=CARTESIAN_POINT('Ctrl Pts',(69.0548300315723,239.076349928799,6.40821950545246)) ;
#71034=CARTESIAN_POINT('Ctrl Pts',(69.1056337366415,239.194724847852,6.31379422957587)) ;
#71035=CARTESIAN_POINT('Ctrl Pts',(69.1297869018418,239.308387963015,6.26862779205968)) ;
#71036=CARTESIAN_POINT('Ctrl Pts',(69.1362827398811,239.39995521031,6.2564538196623)) ;
#71037=CARTESIAN_POINT('Ctrl Pts',(69.1297923775911,239.491555834057,6.26861719768716)) ;
#71038=CARTESIAN_POINT('Ctrl Pts',(69.1056545079565,239.605197565579,6.31375420105852)) ;
#71039=CARTESIAN_POINT('Ctrl Pts',(69.0547968682434,239.723636495491,6.408283325731)) ;
#71040=CARTESIAN_POINT('Ctrl Pts',(68.9521494703146,239.867419347135,6.59662477927506)) ;
#71041=CARTESIAN_POINT('Ctrl Pts',(68.8030349447908,239.984687634551,6.86457837515914)) ;
#71042=CARTESIAN_POINT('Ctrl Pts',(68.6747499248955,240.032789234252,7.08855041543658)) ;
#71043=CARTESIAN_POINT('Ctrl Pts',(68.6093959252955,240.047168995753,7.20122176608181)) ;
#71044=CARTESIAN_POINT('Ctrl Pts',(68.6018591141068,238.657091578019,7.17771964424042)) ;
#71045=CARTESIAN_POINT('Ctrl Pts',(68.6714047962981,238.677908559888,7.06324251803697)) ;
#71046=CARTESIAN_POINT('Ctrl Pts',(68.8067647486738,238.739644581446,6.83622495555726)) ;
#71047=CARTESIAN_POINT('Ctrl Pts',(68.9621528761349,238.876711748343,6.56553452424404)) ;
#71048=CARTESIAN_POINT('Ctrl Pts',(69.0684466966744,239.039506283962,6.37549899432774)) ;
#71049=CARTESIAN_POINT('Ctrl Pts',(69.1208506659138,239.171888309829,6.28031845030118)) ;
#71050=CARTESIAN_POINT('Ctrl Pts',(69.1457255676693,239.298297281133,6.23480457795015)) ;
#71051=CARTESIAN_POINT('Ctrl Pts',(69.1524115152463,239.399951520372,6.22253846320574)) ;
#71052=CARTESIAN_POINT('Ctrl Pts',(69.1457311807739,239.501642692904,6.23479393102029)) ;
#71053=CARTESIAN_POINT('Ctrl Pts',(69.1208719019535,239.62802810922,6.28027817234562)) ;
#71054=CARTESIAN_POINT('Ctrl Pts',(69.0684128446976,239.760480643033,6.37556331663666)) ;
#71055=CARTESIAN_POINT('Ctrl Pts',(68.962140361611,239.923293707433,6.56555781595963)) ;
#71056=CARTESIAN_POINT('Ctrl Pts',(68.8067479265598,240.060349330392,6.83625684756693)) ;
#71057=CARTESIAN_POINT('Ctrl Pts',(68.6714048768271,240.12209146921,7.06324236536902)) ;
#71058=CARTESIAN_POINT('Ctrl Pts',(68.6018591135284,240.142908421772,7.17771964533681)) ;
#71059=CARTESIAN_POINT('Ctrl Pts',(68.6092247447017,238.61751001058,7.17433686958768)) ;
#71060=CARTESIAN_POINT('Ctrl Pts',(68.679299286119,238.640872464225,7.05828606782104)) ;
#71061=CARTESIAN_POINT('Ctrl Pts',(68.8153438440691,238.708069202037,6.82849363480124)) ;
#71062=CARTESIAN_POINT('Ctrl Pts',(68.9709015206617,238.853192530671,6.55502612932433)) ;
#71063=CARTESIAN_POINT('Ctrl Pts',(69.0770671806673,239.0239067636,6.36321815140438)) ;
#71064=CARTESIAN_POINT('Ctrl Pts',(69.1293366859553,239.162186895062,6.26719697702747)) ;
#71065=CARTESIAN_POINT('Ctrl Pts',(69.1541328649434,239.294005437406,6.22129023015348)) ;
#71066=CARTESIAN_POINT('Ctrl Pts',(69.1607961026436,239.39994986084,6.20891916879272)) ;
#71067=CARTESIAN_POINT('Ctrl Pts',(69.1541384307542,239.50593460718,6.2212794932625)) ;
#71068=CARTESIAN_POINT('Ctrl Pts',(69.1293577894806,239.637727426768,6.26715638663095)) ;
#71069=CARTESIAN_POINT('Ctrl Pts',(69.077033458404,239.776084919601,6.36328294224198)) ;
#71070=CARTESIAN_POINT('Ctrl Pts',(68.9708891897341,239.94681152009,6.55504961105578)) ;
#71071=CARTESIAN_POINT('Ctrl Pts',(68.8153271059694,240.091926611612,6.82852576172937)) ;
#71072=CARTESIAN_POINT('Ctrl Pts',(68.6792993662451,240.159127555783,7.05828591402844)) ;
#71073=CARTESIAN_POINT('Ctrl Pts',(68.6092247441262,240.182489989276,7.17433687069216)) ;
#71074=CARTESIAN_POINT('',(69.1585759510679,239.399999978945,6.21304106630657)) ;
#71075=CARTESIAN_POINT('Ctrl Pts',(68.6102252342999,240.182155687653,7.17267980084141)) ;
#71076=CARTESIAN_POINT('Ctrl Pts',(68.6799483073472,240.158806652482,7.05718975930635)) ;
#71077=CARTESIAN_POINT('Ctrl Pts',(68.8156241307394,240.091649533961,6.82800359598836)) ;
#71078=CARTESIAN_POINT('Ctrl Pts',(68.9708891897341,239.94681152009,6.55504961105578)) ;
#71079=CARTESIAN_POINT('Ctrl Pts',(69.077033458404,239.776084919601,6.36328294224198)) ;
#71080=CARTESIAN_POINT('Ctrl Pts',(69.1293577894806,239.637727426768,6.26715638663095)) ;
#71081=CARTESIAN_POINT('Ctrl Pts',(69.1541358935304,239.505948101095,6.22128419047529)) ;
#71082=CARTESIAN_POINT('Ctrl Pts',(69.1585750605836,239.435307046742,6.21304265234076)) ;
#71083=CARTESIAN_POINT('Ctrl Pts',(69.1585759510679,239.399999979053,6.21304106630657)) ;
#71084=CARTESIAN_POINT('Ctrl Pts',(69.1585759510679,239.399999978837,6.21304106630656)) ;
#71085=CARTESIAN_POINT('Ctrl Pts',(69.1585768422728,239.364663979398,6.21303947898959)) ;
#71086=CARTESIAN_POINT('Ctrl Pts',(69.1563556683963,239.329334225001,6.21716334848777)) ;
#71087=CARTESIAN_POINT('Ctrl Pts',(69.1479338201964,239.26105080182,6.23276691687198)) ;
#71088=CARTESIAN_POINT('Ctrl Pts',(69.1293366859554,239.162186895062,6.26719697702748)) ;
#71089=CARTESIAN_POINT('Ctrl Pts',(69.0770671806673,239.0239067636,6.36321815140438)) ;
#71090=CARTESIAN_POINT('Ctrl Pts',(68.9709015206618,238.85319253067,6.55502612932432)) ;
#71091=CARTESIAN_POINT('Ctrl Pts',(68.8156408604242,238.708346295415,6.82797148556704)) ;
#71092=CARTESIAN_POINT('Ctrl Pts',(68.6799483073473,238.641193347518,7.05718975930627)) ;
#71093=CARTESIAN_POINT('Ctrl Pts',(68.6102252343001,238.617844312347,7.17267980084128)) ;
#71094=CARTESIAN_POINT('Ctrl Pts',(68.7158628290615,238.830049344242,7.27867958883784)) ;
#71095=CARTESIAN_POINT('Ctrl Pts',(68.7366797982012,238.836897624306,7.23273869142603)) ;
#71096=CARTESIAN_POINT('Ctrl Pts',(68.7572656540277,238.84492957757,7.18693718631418)) ;
#71097=CARTESIAN_POINT('Ctrl Pts',(68.7775992891298,238.854215072605,7.14139055287856)) ;
#71098=CARTESIAN_POINT('Ctrl Pts',(68.7971739401569,238.863153972315,7.09754401729895)) ;
#71099=CARTESIAN_POINT('Ctrl Pts',(68.8165155389829,238.873255203555,7.05393368154921)) ;
#71100=CARTESIAN_POINT('Ctrl Pts',(68.8355698580483,238.884612920864,7.01066257034807)) ;
#71101=CARTESIAN_POINT('Ctrl Pts',(68.8464800190241,238.891116145867,6.98588630900877)) ;
#71102=CARTESIAN_POINT('Ctrl Pts',(68.8572952869515,238.898031858053,6.96122126250497)) ;
#71103=CARTESIAN_POINT('Ctrl Pts',(68.8679986147481,238.905381426673,6.93668677075398)) ;
#71104=CARTESIAN_POINT('Ctrl Pts',(68.8830401948506,238.915709908359,6.90220800583574)) ;
#71105=CARTESIAN_POINT('Ctrl Pts',(68.897846272571,238.926881718366,6.86798707596825)) ;
#71106=CARTESIAN_POINT('Ctrl Pts',(68.9124023081378,238.939007940948,6.83420344555356)) ;
#71107=CARTESIAN_POINT('Ctrl Pts',(68.9265549103273,238.950798074564,6.80135615828349)) ;
#71108=CARTESIAN_POINT('Ctrl Pts',(68.9404716563316,238.963490988979,6.76892226610576)) ;
#71109=CARTESIAN_POINT('Ctrl Pts',(68.9540953516258,238.977209485407,6.73706672113604)) ;
#71110=CARTESIAN_POINT('Ctrl Pts',(68.9671197548697,238.990324519583,6.7066124681395)) ;
#71111=CARTESIAN_POINT('Ctrl Pts',(68.9798766287053,239.004377499894,6.67668679969608)) ;
#71112=CARTESIAN_POINT('Ctrl Pts',(68.9922696910491,239.019486631773,6.64743384323044)) ;
#71113=CARTESIAN_POINT('Ctrl Pts',(68.9968494259556,239.025070063596,6.63662369944769)) ;
#71114=CARTESIAN_POINT('Ctrl Pts',(69.0013789854125,239.030797788519,6.62590542119213)) ;
#71115=CARTESIAN_POINT('Ctrl Pts',(69.0058516746882,239.036675899092,6.6152862817678)) ;
#71116=CARTESIAN_POINT('Ctrl Pts',(69.016416069623,239.05055986861,6.59020410506638)) ;
#71117=CARTESIAN_POINT('Ctrl Pts',(69.0266678867807,239.06528218644,6.56567501809567)) ;
#71118=CARTESIAN_POINT('Ctrl Pts',(69.0365283781207,239.08098938145,6.54201894628589)) ;
#71119=CARTESIAN_POINT('Ctrl Pts',(69.0455617472285,239.095379018364,6.52034720388181)) ;
#71120=CARTESIAN_POINT('Ctrl Pts',(69.0542665659304,239.110595896997,6.49940815809408)) ;
#71121=CARTESIAN_POINT('Ctrl Pts',(69.0625328641691,239.126755835211,6.47944779037588)) ;
#71122=CARTESIAN_POINT('Ctrl Pts',(69.0632897511035,239.128235487377,6.47762015954337)) ;
#71123=CARTESIAN_POINT('Ctrl Pts',(69.0640429251907,239.129723044254,6.47580073373255)) ;
#71124=CARTESIAN_POINT('Ctrl Pts',(69.06479227953,239.13121859315,6.47398970176958)) ;
#71125=CARTESIAN_POINT('Ctrl Pts',(69.0730519606016,239.147703126922,6.45402778837199)) ;
#71126=CARTESIAN_POINT('Ctrl Pts',(69.0808483160851,239.165153969754,6.43508567072191)) ;
#71127=CARTESIAN_POINT('Ctrl Pts',(69.0879957148478,239.183641424611,6.41770986762872)) ;
#71128=CARTESIAN_POINT('Ctrl Pts',(69.094820068071,239.201293290182,6.40111940978772)) ;
#71129=CARTESIAN_POINT('Ctrl Pts',(69.1010526832419,239.219890795336,6.38595687877681)) ;
#71130=CARTESIAN_POINT('Ctrl Pts',(69.1064898316604,239.239472217782,6.37269798819665)) ;
#71131=CARTESIAN_POINT('Ctrl Pts',(69.1076761643912,239.24374469309,6.36980502764829)) ;
#71132=CARTESIAN_POINT('Ctrl Pts',(69.1088244658108,239.248063899034,6.36700269367533)) ;
#71133=CARTESIAN_POINT('Ctrl Pts',(69.1099323472444,239.252430031787,6.3642959276952)) ;
#71134=CARTESIAN_POINT('Ctrl Pts',(69.1141941375064,239.269225639588,6.35388355995823)) ;
#71135=CARTESIAN_POINT('Ctrl Pts',(69.1178559830534,239.286724581721,6.34488538964452)) ;
#71136=CARTESIAN_POINT('Ctrl Pts',(69.1207549168715,239.304754977569,6.33774916486814)) ;
#71137=CARTESIAN_POINT('Ctrl Pts',(69.1217683854168,239.311058411934,6.33525433752933)) ;
#71138=CARTESIAN_POINT('Ctrl Pts',(69.1226889787148,239.317426522997,6.33298707804794)) ;
#71139=CARTESIAN_POINT('Ctrl Pts',(69.1235110032382,239.323851127572,6.3309665179532)) ;
#71140=CARTESIAN_POINT('Ctrl Pts',(69.1254736522473,239.339190382601,6.32614226982525)) ;
#71141=CARTESIAN_POINT('Ctrl Pts',(69.1268709134684,239.354855134897,6.32272434055556)) ;
#71142=CARTESIAN_POINT('Ctrl Pts',(69.1276444073157,239.370647147276,6.32081810135888)) ;
#71143=CARTESIAN_POINT('Ctrl Pts',(69.1281215532427,239.380388781824,6.31964219766971)) ;
#71144=CARTESIAN_POINT('Ctrl Pts',(69.1283623161023,239.390178572222,6.31904153715748)) ;
#71145=CARTESIAN_POINT('Ctrl Pts',(69.1283628282387,239.399968612813,6.31904085443174)) ;
#71146=CARTESIAN_POINT('Ctrl Pts',(69.1283636534311,239.415743057411,6.31903975437303)) ;
#71147=CARTESIAN_POINT('Ctrl Pts',(69.1277380059827,239.431520354394,6.3205963203152)) ;
#71148=CARTESIAN_POINT('Ctrl Pts',(69.1265115351569,239.44709697861,6.32360663121809)) ;
#71149=CARTESIAN_POINT('Ctrl Pts',(69.125742887679,239.456859080297,6.32549323775971)) ;
#71150=CARTESIAN_POINT('Ctrl Pts',(69.1247393224569,239.466542400804,6.3279508338922)) ;
#71151=CARTESIAN_POINT('Ctrl Pts',(69.1235174398229,239.476098549837,6.33095383885585)) ;
#71152=CARTESIAN_POINT('Ctrl Pts',(69.1211465654452,239.494640779885,6.33678070579572)) ;
#71153=CARTESIAN_POINT('Ctrl Pts',(69.1179518902521,239.512706283228,6.34466100445943)) ;
#71154=CARTESIAN_POINT('Ctrl Pts',(69.1140849924868,239.530113593718,6.35413972745554)) ;
#71155=CARTESIAN_POINT('Ctrl Pts',(69.1127790974153,239.535992239174,6.35734079932138)) ;
#71156=CARTESIAN_POINT('Ctrl Pts',(69.1113969040053,239.541796070096,6.3607241697595)) ;
#71157=CARTESIAN_POINT('Ctrl Pts',(69.1099453007327,239.547518909441,6.3642723138828)) ;
#71158=CARTESIAN_POINT('Ctrl Pts',(69.1048539417821,239.567591218367,6.37671708834856)) ;
#71159=CARTESIAN_POINT('Ctrl Pts',(69.098910326907,239.586674255091,6.3911888892425)) ;
#71160=CARTESIAN_POINT('Ctrl Pts',(69.092329474663,239.604796539636,6.40720210496948)) ;
#71161=CARTESIAN_POINT('Ctrl Pts',(69.0854457626439,239.623752836377,6.42395227067415)) ;
#71162=CARTESIAN_POINT('Ctrl Pts',(69.0778649776355,239.641658609174,6.44238899189171)) ;
#71163=CARTESIAN_POINT('Ctrl Pts',(69.069785243753,239.658576427517,6.46195647864843)) ;
#71164=CARTESIAN_POINT('Ctrl Pts',(69.0681423609093,239.662016391496,6.46593520972473)) ;
#71165=CARTESIAN_POINT('Ctrl Pts',(69.0664786935224,239.665415583934,6.46996069188013)) ;
#71166=CARTESIAN_POINT('Ctrl Pts',(69.0647956726972,239.668774634716,6.47402825272209)) ;
#71167=CARTESIAN_POINT('Ctrl Pts',(69.0566289234863,239.685074210408,6.49376582744493)) ;
#71168=CARTESIAN_POINT('Ctrl Pts',(69.0480139653239,239.700422018716,6.5144941922125)) ;
#71169=CARTESIAN_POINT('Ctrl Pts',(69.039064734617,239.714934221164,6.53597206760508)) ;
#71170=CARTESIAN_POINT('Ctrl Pts',(69.0297224046819,239.730083879028,6.55839336892089)) ;
#71171=CARTESIAN_POINT('Ctrl Pts',(69.0200155328915,239.744323575318,6.58163147222669)) ;
#71172=CARTESIAN_POINT('Ctrl Pts',(69.01001776566,239.757782786127,6.60541188610505)) ;
#71173=CARTESIAN_POINT('Ctrl Pts',(69.0086329381958,239.759647070856,6.6087057985843)) ;
#71174=CARTESIAN_POINT('Ctrl Pts',(69.007242449196,239.761496368199,6.61201011585464)) ;
#71175=CARTESIAN_POINT('Ctrl Pts',(69.0058464190132,239.763331007932,6.61532410844729)) ;
#71176=CARTESIAN_POINT('Ctrl Pts',(68.9936472426615,239.779362963344,6.64428335342889)) ;
#71177=CARTESIAN_POINT('Ctrl Pts',(68.9810291007366,239.794276365259,6.67398141534986)) ;
#71178=CARTESIAN_POINT('Ctrl Pts',(68.968110015568,239.808194086138,6.70427010590999)) ;
#71179=CARTESIAN_POINT('Ctrl Pts',(68.9547944157724,239.82253897193,6.73548842180239)) ;
#71180=CARTESIAN_POINT('Ctrl Pts',(68.9411586577516,239.835826812852,6.76733417804846)) ;
#71181=CARTESIAN_POINT('Ctrl Pts',(68.9272760863257,239.848183236163,6.79964511862253)) ;
#71182=CARTESIAN_POINT('Ctrl Pts',(68.9128297461076,239.861041451658,6.83326820082954)) ;
#71183=CARTESIAN_POINT('Ctrl Pts',(68.898115676083,239.87289172878,6.86739501663498)) ;
#71184=CARTESIAN_POINT('Ctrl Pts',(68.8831640328237,239.883855459624,6.90184272882289)) ;
#71185=CARTESIAN_POINT('Ctrl Pts',(68.878134330881,239.887543636058,6.91343086812699)) ;
#71186=CARTESIAN_POINT('Ctrl Pts',(68.8730773513663,239.891131280772,6.92505532121191)) ;
#71187=CARTESIAN_POINT('Ctrl Pts',(68.8679931270226,239.894622341495,6.93670912783197)) ;
#71188=CARTESIAN_POINT('Ctrl Pts',(68.8494131707771,239.907380188333,6.97929718108381)) ;
#71189=CARTESIAN_POINT('Ctrl Pts',(68.8304990267295,239.918831679828,7.02227724724999)) ;
#71190=CARTESIAN_POINT('Ctrl Pts',(68.8113292278266,239.929084130521,7.06554957763077)) ;
#71191=CARTESIAN_POINT('Ctrl Pts',(68.7913959354002,239.939744915164,7.11054535561578)) ;
#71192=CARTESIAN_POINT('Ctrl Pts',(68.7711855162388,239.949109995399,7.1558571419846)) ;
#71193=CARTESIAN_POINT('Ctrl Pts',(68.7507387129936,239.957269204465,7.20137278869765)) ;
#71194=CARTESIAN_POINT('Ctrl Pts',(68.7391888375968,239.961878132663,7.22708341161682)) ;
#71195=CARTESIAN_POINT('Ctrl Pts',(68.7275627458053,239.966101665732,7.25285908292051)) ;
#71196=CARTESIAN_POINT('Ctrl Pts',(68.7158628290613,239.969950655758,7.27867958883829)) ;
#71197=CARTESIAN_POINT('Origin',(79.6268886667016,242.164965512063,7.2786795888419)) ;
#71198=CARTESIAN_POINT('',(79.5657826988536,242.355402012486,7.27867958883753)) ;
#71199=CARTESIAN_POINT('Origin',(79.6268886667016,242.164965512063,7.2786795888419)) ;
#71200=CARTESIAN_POINT('',(79.7759762964688,242.245816755679,7.17267980084142)) ;
#71201=CARTESIAN_POINT('Origin',(79.6268886667016,242.164965512063,7.2786795888419)) ;
#71202=CARTESIAN_POINT('Origin',(79.6268886666992,242.164965512062,7.27867958883793)) ;
#71203=CARTESIAN_POINT('Origin',(68.824955275583,238.345892662512,7.2786795888419)) ;
#71204=CARTESIAN_POINT('',(68.8242223895095,238.145894005322,7.27867958883747)) ;
#71205=CARTESIAN_POINT('Origin',(68.824955275583,238.345892662512,7.2786795888419)) ;
#71206=CARTESIAN_POINT('',(68.6581801055002,238.31506917167,7.17267980084141)) ;
#71207=CARTESIAN_POINT('Origin',(68.824955275583,238.345892662512,7.2786795888419)) ;
#71208=CARTESIAN_POINT('Origin',(68.8249552755856,238.345892662512,7.27867958883788)) ;
#71209=CARTESIAN_POINT('Origin',(74.5283628290597,239.4,7.2786795888419)) ;
#71210=CARTESIAN_POINT('Origin',(74.5283628290597,239.4,7.17267980084126)) ;
#71211=CARTESIAN_POINT('Origin',(79.7621052129774,241.899588097824,7.27867958884204)) ;
#71212=CARTESIAN_POINT('',(79.8802543914391,241.738216564929,7.27867958883795)) ;
#71213=CARTESIAN_POINT('Origin',(79.7621052129773,241.899588097824,7.27867958883753)) ;
#71214=CARTESIAN_POINT('',(79.9151467531553,241.97267935533,7.17267980084126)) ;
#71215=CARTESIAN_POINT('Origin',(79.7621052129774,241.899588097824,7.27867958884204)) ;
#71216=CARTESIAN_POINT('Origin',(79.7621052129773,241.899588097824,7.2786795888419)) ;
#71217=CARTESIAN_POINT('Origin',(69.294620445142,236.900411902176,7.27867958884205)) ;
#71218=CARTESIAN_POINT('',(69.1764712666803,237.06178343507,7.2786795888379)) ;
#71219=CARTESIAN_POINT('Origin',(69.2946204451421,236.900411902176,7.27867958883748)) ;
#71220=CARTESIAN_POINT('',(69.1415789049641,236.82732064467,7.17267980084126)) ;
#71221=CARTESIAN_POINT('Origin',(69.294620445142,236.900411902176,7.27867958884205)) ;
#71222=CARTESIAN_POINT('Origin',(69.2946204451421,236.900411902176,7.2786795888419)) ;
#71223=CARTESIAN_POINT('Ctrl Pts',(69.1764712666787,237.061783435069,7.27867958884205)) ;
#71224=CARTESIAN_POINT('Ctrl Pts',(69.243148183502,237.110601357313,7.10544023141379)) ;
#71225=CARTESIAN_POINT('Ctrl Pts',(69.3221531999422,237.194392857808,6.875738735788)) ;
#71226=CARTESIAN_POINT('Ctrl Pts',(69.3907109930823,237.344712076154,6.61255350476255)) ;
#71227=CARTESIAN_POINT('Ctrl Pts',(69.4139986922107,237.434159724772,6.49311022572802)) ;
#71228=CARTESIAN_POINT('Ctrl Pts',(69.4226403902003,237.51671011904,6.41124585525348)) ;
#71229=CARTESIAN_POINT('Ctrl Pts',(69.4220357539442,237.583935565768,6.3619402730086)) ;
#71230=CARTESIAN_POINT('Ctrl Pts',(69.408113128478,237.705993381689,6.3017093864378)) ;
#71231=CARTESIAN_POINT('Ctrl Pts',(69.3463002437199,237.856072726253,6.33249341474089)) ;
#71232=CARTESIAN_POINT('Ctrl Pts',(69.2496003997641,237.971560196244,6.4698470585811)) ;
#71233=CARTESIAN_POINT('Ctrl Pts',(69.1354707359804,238.065806393091,6.66035004570858)) ;
#71234=CARTESIAN_POINT('Ctrl Pts',(68.9914670223674,238.129856863735,6.93430623056252)) ;
#71235=CARTESIAN_POINT('Ctrl Pts',(68.8793123588541,238.14569213061,7.16318984183832)) ;
#71236=CARTESIAN_POINT('Ctrl Pts',(68.8242223895094,238.145894005322,7.27867958884204)) ;
#71237=CARTESIAN_POINT('Ctrl Pts',(69.1398244440697,237.03495223438,7.24979207607672)) ;
#71238=CARTESIAN_POINT('Ctrl Pts',(69.2136594228754,237.081063573975,7.07847449697579)) ;
#71239=CARTESIAN_POINT('Ctrl Pts',(69.3029051206822,237.164631115907,6.85078050509009)) ;
#71240=CARTESIAN_POINT('Ctrl Pts',(69.3828266366339,237.320754685321,6.58950105248792)) ;
#71241=CARTESIAN_POINT('Ctrl Pts',(69.4108817593994,237.414984669568,6.47084518025989)) ;
#71242=CARTESIAN_POINT('Ctrl Pts',(69.422335402039,237.502586585413,6.38949218624853)) ;
#71243=CARTESIAN_POINT('Ctrl Pts',(69.4230316106547,237.574170392916,6.34048601917785)) ;
#71244=CARTESIAN_POINT('Ctrl Pts',(69.409808159248,237.70446059159,6.2806080333673)) ;
#71245=CARTESIAN_POINT('Ctrl Pts',(69.3430376940479,237.864409604147,6.3112178366199)) ;
#71246=CARTESIAN_POINT('Ctrl Pts',(69.2371135689013,237.985002035298,6.44773619808466)) ;
#71247=CARTESIAN_POINT('Ctrl Pts',(69.1123412792411,238.081000391347,6.63698036173261)) ;
#71248=CARTESIAN_POINT('Ctrl Pts',(68.9561282905968,238.141140136422,6.90887829015515)) ;
#71249=CARTESIAN_POINT('Ctrl Pts',(68.8366934655611,238.150123165881,7.1355834795928)) ;
#71250=CARTESIAN_POINT('Ctrl Pts',(68.7788035031626,238.146060440786,7.24979207607672)) ;
#71251=CARTESIAN_POINT('Ctrl Pts',(69.099905192383,236.955910305836,7.19960828841391)) ;
#71252=CARTESIAN_POINT('Ctrl Pts',(69.1860064168498,237.006605983873,7.03140700938371)) ;
#71253=CARTESIAN_POINT('Ctrl Pts',(69.2900259465182,237.09923082272,6.80705467385308)) ;
#71254=CARTESIAN_POINT('Ctrl Pts',(69.3832650913571,237.27387614127,6.54899621389332)) ;
#71255=CARTESIAN_POINT('Ctrl Pts',(69.4162520055124,237.379299887585,6.43168582586966)) ;
#71256=CARTESIAN_POINT('Ctrl Pts',(69.4300886371973,237.47734191796,6.35121101255399)) ;
#71257=CARTESIAN_POINT('Ctrl Pts',(69.4314780745408,237.557412263923,6.3027208476791)) ;
#71258=CARTESIAN_POINT('Ctrl Pts',(69.4174156669863,237.703106817915,6.24345333299259)) ;
#71259=CARTESIAN_POINT('Ctrl Pts',(69.342501106197,237.881643096035,6.27376032922433)) ;
#71260=CARTESIAN_POINT('Ctrl Pts',(69.2226188574627,238.015603497768,6.40883966351126)) ;
#71261=CARTESIAN_POINT('Ctrl Pts',(69.0809642347923,238.121495468969,6.59593332022851)) ;
#71262=CARTESIAN_POINT('Ctrl Pts',(68.902901648932,238.186234982861,6.8643640810213)) ;
#71263=CARTESIAN_POINT('Ctrl Pts',(68.7663503411012,238.192939491825,7.08747716850402)) ;
#71264=CARTESIAN_POINT('Ctrl Pts',(68.7000484702344,238.186542756822,7.19960828841391)) ;
#71265=CARTESIAN_POINT('Ctrl Pts',(69.1223464629029,236.862651936505,7.17608503411331)) ;
#71266=CARTESIAN_POINT('Ctrl Pts',(69.2114184263084,236.924421474316,7.00519241449165)) ;
#71267=CARTESIAN_POINT('Ctrl Pts',(69.3172779787112,237.032178811751,6.77809747419061)) ;
#71268=CARTESIAN_POINT('Ctrl Pts',(69.4094503328369,237.228581096615,6.51751159801928)) ;
#71269=CARTESIAN_POINT('Ctrl Pts',(69.4409048676736,237.346030918506,6.39917202871152)) ;
#71270=CARTESIAN_POINT('Ctrl Pts',(69.4527579169206,237.454760983212,6.31803579114758)) ;
#71271=CARTESIAN_POINT('Ctrl Pts',(69.4522076854779,237.543435565293,6.26916026780418)) ;
#71272=CARTESIAN_POINT('Ctrl Pts',(69.4340864408003,237.704639718483,6.20944181386913)) ;
#71273=CARTESIAN_POINT('Ctrl Pts',(69.3522671333801,237.902982353965,6.23997013594573)) ;
#71274=CARTESIAN_POINT('Ctrl Pts',(69.2242009113928,238.05477780945,6.37612467492586)) ;
#71275=CARTESIAN_POINT('Ctrl Pts',(69.0732121226385,238.177710520412,6.56486468658063)) ;
#71276=CARTESIAN_POINT('Ctrl Pts',(68.883092282389,238.259246394865,6.8360410390703)) ;
#71277=CARTESIAN_POINT('Ctrl Pts',(68.7356312735506,238.276769354007,7.0621597362024)) ;
#71278=CARTESIAN_POINT('Ctrl Pts',(68.6633879453144,238.275181010333,7.1760850341133)) ;
#71279=CARTESIAN_POINT('Ctrl Pts',(69.141578904964,236.82732064467,7.17267980084142)) ;
#71280=CARTESIAN_POINT('Ctrl Pts',(69.2302241041771,236.892950071602,6.99944044341316)) ;
#71281=CARTESIAN_POINT('Ctrl Pts',(69.334840073065,237.006158216377,6.76973894778735)) ;
#71282=CARTESIAN_POINT('Ctrl Pts',(69.4244038080695,237.210771326455,6.50655371676194)) ;
#71283=CARTESIAN_POINT('Ctrl Pts',(69.4542517733073,237.332909486872,6.38711043772741)) ;
#71284=CARTESIAN_POINT('Ctrl Pts',(69.4646137832507,237.445912417774,6.30524606725286)) ;
#71285=CARTESIAN_POINT('Ctrl Pts',(69.4628489697551,237.53809374039,6.25594048500798)) ;
#71286=CARTESIAN_POINT('Ctrl Pts',(69.4425255895883,237.705725559621,6.19570959843718)) ;
#71287=CARTESIAN_POINT('Ctrl Pts',(69.3580050351793,237.912593058043,6.22649362674026)) ;
#71288=CARTESIAN_POINT('Ctrl Pts',(69.2275905708934,238.072255835849,6.36384727058048)) ;
#71289=CARTESIAN_POINT('Ctrl Pts',(69.0742642050193,238.202782237888,6.55435025770793)) ;
#71290=CARTESIAN_POINT('Ctrl Pts',(68.8815106963087,238.29188736988,6.8283064425619)) ;
#71291=CARTESIAN_POINT('Ctrl Pts',(68.731705749617,238.314408535778,7.05719005383769)) ;
#71292=CARTESIAN_POINT('Ctrl Pts',(68.6581801055002,238.31506917167,7.17267980084141)) ;
#71293=CARTESIAN_POINT('Ctrl Pts',(68.6581801055002,238.31506917167,7.17267980084144)) ;
#71294=CARTESIAN_POINT('Ctrl Pts',(68.6999525110751,238.314693842072,7.10706616889675)) ;
#71295=CARTESIAN_POINT('Ctrl Pts',(68.7422057617377,238.310890803021,7.04171162773037)) ;
#71296=CARTESIAN_POINT('Ctrl Pts',(68.7848246201634,238.303370652585,6.97698800180934)) ;
#71297=CARTESIAN_POINT('Ctrl Pts',(68.8089147256669,238.299119923586,6.94040328240097)) ;
#71298=CARTESIAN_POINT('Ctrl Pts',(68.833122153762,238.293682517859,6.90402046522006)) ;
#71299=CARTESIAN_POINT('Ctrl Pts',(68.8574309924011,238.287014704168,6.8679090476063)) ;
#71300=CARTESIAN_POINT('Ctrl Pts',(68.8657978603999,238.284719706952,6.85547984566426)) ;
#71301=CARTESIAN_POINT('Ctrl Pts',(68.8741783905198,238.282278268265,6.84308050324332)) ;
#71302=CARTESIAN_POINT('Ctrl Pts',(68.8825729718501,238.279688415001,6.83071258016738)) ;
#71303=CARTESIAN_POINT('Ctrl Pts',(68.9148256813734,238.269737974146,6.78319394705386)) ;
#71304=CARTESIAN_POINT('Ctrl Pts',(68.9472835743097,238.257599262249,6.73613620680623)) ;
#71305=CARTESIAN_POINT('Ctrl Pts',(68.9798286619572,238.242680053236,6.69003521439263)) ;
#71306=CARTESIAN_POINT('Ctrl Pts',(68.9876568819059,238.239091467121,6.67894633018452)) ;
#71307=CARTESIAN_POINT('Ctrl Pts',(68.995490333041,238.235342151787,6.6679128004386)) ;
#71308=CARTESIAN_POINT('Ctrl Pts',(69.0033277607713,238.231424121694,6.65694152576342)) ;
#71309=CARTESIAN_POINT('Ctrl Pts',(69.0332777274343,238.216451751332,6.61501586825413)) ;
#71310=CARTESIAN_POINT('Ctrl Pts',(69.0632828822616,238.199013116527,6.57399853749883)) ;
#71311=CARTESIAN_POINT('Ctrl Pts',(69.0932880711879,238.178638120891,6.53430592114766)) ;
#71312=CARTESIAN_POINT('Ctrl Pts',(69.0996874302936,238.174292642042,6.52584047517086)) ;
#71313=CARTESIAN_POINT('Ctrl Pts',(69.1060869684763,238.169813657528,6.51743528549824)) ;
#71314=CARTESIAN_POINT('Ctrl Pts',(69.1124864583777,238.165196694566,6.50909439154214)) ;
#71315=CARTESIAN_POINT('Ctrl Pts',(69.114322160242,238.163872312835,6.50670179544144)) ;
#71316=CARTESIAN_POINT('Ctrl Pts',(69.1161578518097,238.162536566453,6.50431450491999)) ;
#71317=CARTESIAN_POINT('Ctrl Pts',(69.1179934839805,238.16118927711,6.50193271268924)) ;
#71318=CARTESIAN_POINT('Ctrl Pts',(69.1441271017158,238.142008122402,6.46802349673852)) ;
#71319=CARTESIAN_POINT('Ctrl Pts',(69.1701834997951,238.12052377075,6.43531103830365)) ;
#71320=CARTESIAN_POINT('Ctrl Pts',(69.1960235506317,238.096256908892,6.40437140018978)) ;
#71321=CARTESIAN_POINT('Ctrl Pts',(69.200602813238,238.091956440066,6.39888841067231)) ;
#71322=CARTESIAN_POINT('Ctrl Pts',(69.205175413079,238.087568580314,6.39346109729161)) ;
#71323=CARTESIAN_POINT('Ctrl Pts',(69.2097407553992,238.08309065004,6.38809266614272)) ;
#71324=CARTESIAN_POINT('Ctrl Pts',(69.2155047995749,238.077436969307,6.38131466963642)) ;
#71325=CARTESIAN_POINT('Ctrl Pts',(69.2212571502427,238.071639928937,6.37463063750665)) ;
#71326=CARTESIAN_POINT('Ctrl Pts',(69.2269965636579,238.065694458748,6.36804717288461)) ;
#71327=CARTESIAN_POINT('Ctrl Pts',(69.2381520120765,238.054138506733,6.35525117881787)) ;
#71328=CARTESIAN_POINT('Ctrl Pts',(69.2492584241303,238.04202171314,6.34283511840792)) ;
#71329=CARTESIAN_POINT('Ctrl Pts',(69.2602291524054,238.029272223066,6.33098424685138)) ;
#71330=CARTESIAN_POINT('Ctrl Pts',(69.2762291953482,238.010677979953,6.31370057624549)) ;
#71331=CARTESIAN_POINT('Ctrl Pts',(69.2920266123677,237.990684501173,6.2975066182331)) ;
#71332=CARTESIAN_POINT('Ctrl Pts',(69.3073059712954,237.969089607455,6.28306176861731)) ;
#71333=CARTESIAN_POINT('Ctrl Pts',(69.3170064523572,237.955379552045,6.27389109654915)) ;
#71334=CARTESIAN_POINT('Ctrl Pts',(69.3264982581306,237.94102462448,6.26542539348726)) ;
#71335=CARTESIAN_POINT('Ctrl Pts',(69.3357048535214,237.9259819694,6.25782719378357)) ;
#71336=CARTESIAN_POINT('Ctrl Pts',(69.3461971715583,237.908838572247,6.24916788766498)) ;
#71337=CARTESIAN_POINT('Ctrl Pts',(69.3563194560639,237.890802280141,6.2416363146655)) ;
#71338=CARTESIAN_POINT('Ctrl Pts',(69.3659433718682,237.872119457317,6.23535445238633)) ;
#71339=CARTESIAN_POINT('Ctrl Pts',(69.3766889235219,237.851259212716,6.22834045964418)) ;
#71340=CARTESIAN_POINT('Ctrl Pts',(69.3868213007338,237.829528899656,6.22290107667885)) ;
#71341=CARTESIAN_POINT('Ctrl Pts',(69.3962054482908,237.807176353626,6.21916216383858)) ;
#71342=CARTESIAN_POINT('Ctrl Pts',(69.3977249759491,237.803556918646,6.21855674055017)) ;
#71343=CARTESIAN_POINT('Ctrl Pts',(69.3992248348919,237.799921090119,6.21799596731962)) ;
#71344=CARTESIAN_POINT('Ctrl Pts',(69.400704389067,237.796269834308,6.21748045696162)) ;
#71345=CARTESIAN_POINT('Ctrl Pts',(69.4080873978986,237.778049985144,6.2149080486036)) ;
#71346=CARTESIAN_POINT('Ctrl Pts',(69.4149663679611,237.759443906188,6.2134623227348)) ;
#71347=CARTESIAN_POINT('Ctrl Pts',(69.4212371552491,237.740594005388,6.21324003078939)) ;
#71348=CARTESIAN_POINT('Ctrl Pts',(69.426060889559,237.726093926044,6.21306903514967)) ;
#71349=CARTESIAN_POINT('Ctrl Pts',(69.4305257936821,237.711444249265,6.2136230224309)) ;
#71350=CARTESIAN_POINT('Ctrl Pts',(69.4345108735777,237.696744168001,6.21503461181594)) ;
#71351=CARTESIAN_POINT('Ctrl Pts',(69.4357063419349,237.69233434876,6.21545806893285)) ;
#71352=CARTESIAN_POINT('Ctrl Pts',(69.4368585389515,237.68792033025,6.21595862038417)) ;
#71353=CARTESIAN_POINT('Ctrl Pts',(69.437963971472,237.683505637975,6.21653961743159)) ;
#71354=CARTESIAN_POINT('Ctrl Pts',(69.4416896620956,237.668626595328,6.2184977787954)) ;
#71355=CARTESIAN_POINT('Ctrl Pts',(69.4450076180945,237.653759748461,6.22117270210315)) ;
#71356=CARTESIAN_POINT('Ctrl Pts',(69.4478694000204,237.638976148692,6.22459317008967)) ;
#71357=CARTESIAN_POINT('Ctrl Pts',(69.4502989061332,237.62642563054,6.22749697202036)) ;
#71358=CARTESIAN_POINT('Ctrl Pts',(69.4523999327019,237.613935243742,6.23093747154904)) ;
#71359=CARTESIAN_POINT('Ctrl Pts',(69.4542212766179,237.60156814121,6.2348010738459)) ;
#71360=CARTESIAN_POINT('Ctrl Pts',(69.4573114671906,237.580585446333,6.24135627041758)) ;
#71361=CARTESIAN_POINT('Ctrl Pts',(69.4594928621059,237.559803752785,6.24936900793142)) ;
#71362=CARTESIAN_POINT('Ctrl Pts',(69.4609730875372,237.539562477922,6.25830745765639)) ;
#71363=CARTESIAN_POINT('Ctrl Pts',(69.4627412442874,237.515383899426,6.2689846017476)) ;
#71364=CARTESIAN_POINT('Ctrl Pts',(69.4635077874243,237.491978141513,6.28098058459061)) ;
#71365=CARTESIAN_POINT('Ctrl Pts',(69.4633411171518,237.469303713581,6.29415175647048)) ;
#71366=CARTESIAN_POINT('Ctrl Pts',(69.4632865875771,237.461885312617,6.29846097364117)) ;
#71367=CARTESIAN_POINT('Ctrl Pts',(69.4631324052817,237.45454483693,6.30289591312325)) ;
#71368=CARTESIAN_POINT('Ctrl Pts',(69.4628816398225,237.447279844771,6.30745136656849)) ;
#71369=CARTESIAN_POINT('Ctrl Pts',(69.462471076266,237.435385299853,6.31490974290758)) ;
#71370=CARTESIAN_POINT('Ctrl Pts',(69.4618015271505,237.423693246438,6.3226911622136)) ;
#71371=CARTESIAN_POINT('Ctrl Pts',(69.4609119195854,237.412204661752,6.33072881419273)) ;
#71372=CARTESIAN_POINT('Ctrl Pts',(69.4595971175969,237.395225024232,6.34260812055181)) ;
#71373=CARTESIAN_POINT('Ctrl Pts',(69.4577775214589,237.378689956509,6.35508284132056)) ;
#71374=CARTESIAN_POINT('Ctrl Pts',(69.4555569265135,237.362609472007,6.36796878250284)) ;
#71375=CARTESIAN_POINT('Ctrl Pts',(69.4507548146022,237.327834878683,6.3958350675119)) ;
#71376=CARTESIAN_POINT('Ctrl Pts',(69.4440744559395,237.29518858729,6.42562177225894)) ;
#71377=CARTESIAN_POINT('Ctrl Pts',(69.4359262687737,237.264342959413,6.45673144071841)) ;
#71378=CARTESIAN_POINT('Ctrl Pts',(69.4342394440246,237.257957346584,6.46317171480956)) ;
#71379=CARTESIAN_POINT('Ctrl Pts',(69.4324898504687,237.251649019488,6.4696686866564)) ;
#71380=CARTESIAN_POINT('Ctrl Pts',(69.4306813372517,237.24541523496,6.47621705556352)) ;
#71381=CARTESIAN_POINT('Ctrl Pts',(69.4283565397334,237.237401864274,6.48463481642947)) ;
#71382=CARTESIAN_POINT('Ctrl Pts',(69.425934386871,237.229511324476,6.49313770431927)) ;
#71383=CARTESIAN_POINT('Ctrl Pts',(69.4234232194315,237.221737373948,6.50171478323276)) ;
#71384=CARTESIAN_POINT('Ctrl Pts',(69.422697088201,237.219489452055,6.50419493838598)) ;
#71385=CARTESIAN_POINT('Ctrl Pts',(69.4219633340238,237.217251526371,6.50668140853608)) ;
#71386=CARTESIAN_POINT('Ctrl Pts',(69.4212221518793,237.215023460709,6.50917393353464)) ;
#71387=CARTESIAN_POINT('Ctrl Pts',(69.4097619220254,237.180572894409,6.54771359562661)) ;
#71388=CARTESIAN_POINT('Ctrl Pts',(69.3965230580414,237.148480564374,6.58769691391626)) ;
#71389=CARTESIAN_POINT('Ctrl Pts',(69.3819367159882,237.11836673977,6.62856039271017)) ;
#71390=CARTESIAN_POINT('Ctrl Pts',(69.377526011194,237.109260742525,6.64091693427264)) ;
#71391=CARTESIAN_POINT('Ctrl Pts',(69.3729924469871,237.10033577619,6.65335395529858)) ;
#71392=CARTESIAN_POINT('Ctrl Pts',(69.3683488142593,237.091581581043,6.66585587550309)) ;
#71393=CARTESIAN_POINT('Ctrl Pts',(69.3501266653189,237.057229112367,6.71491484837152)) ;
#71394=CARTESIAN_POINT('Ctrl Pts',(69.3302050449842,237.025505003706,6.76497458145779)) ;
#71395=CARTESIAN_POINT('Ctrl Pts',(69.308820855372,236.996090564452,6.81573937973999)) ;
#71396=CARTESIAN_POINT('Ctrl Pts',(69.304921177765,236.990726469195,6.82499698316901)) ;
#71397=CARTESIAN_POINT('Ctrl Pts',(69.3009730003124,236.985439192709,6.83427803434362)) ;
#71398=CARTESIAN_POINT('Ctrl Pts',(69.2969779405296,236.980226805711,6.84358073996881)) ;
#71399=CARTESIAN_POINT('Ctrl Pts',(69.2935131871895,236.975706313842,6.85164859930998)) ;
#71400=CARTESIAN_POINT('Ctrl Pts',(69.2900131259033,236.971242114419,6.85973283718352)) ;
#71401=CARTESIAN_POINT('Ctrl Pts',(69.2864787978978,236.966832920126,6.86783236707)) ;
#71402=CARTESIAN_POINT('Ctrl Pts',(69.2664829520006,236.941887422852,6.91365634016876)) ;
#71403=CARTESIAN_POINT('Ctrl Pts',(69.2454268139038,236.918699739166,6.95991626883178)) ;
#71404=CARTESIAN_POINT('Ctrl Pts',(69.2234260967364,236.897138360149,7.00647220769083)) ;
#71405=CARTESIAN_POINT('Ctrl Pts',(69.2007985755099,236.874962693889,7.05435453292341)) ;
#71406=CARTESIAN_POINT('Ctrl Pts',(69.177171544277,236.854507667279,7.10255069985114)) ;
#71407=CARTESIAN_POINT('Ctrl Pts',(69.1526704057878,236.835685711672,7.15089895991494)) ;
#71408=CARTESIAN_POINT('Ctrl Pts',(69.1489927835866,236.832860535126,7.15815603634354)) ;
#71409=CARTESIAN_POINT('Ctrl Pts',(69.145295472849,236.830072245688,7.16541651035403)) ;
#71410=CARTESIAN_POINT('Ctrl Pts',(69.1415789049641,236.82732064467,7.17267980084127)) ;
#71411=CARTESIAN_POINT('Ctrl Pts',(69.1764712666787,237.061783435069,7.27867958884205)) ;
#71412=CARTESIAN_POINT('Ctrl Pts',(69.243148183502,237.110601357313,7.10544023141379)) ;
#71413=CARTESIAN_POINT('Ctrl Pts',(69.3221531999422,237.194392857808,6.875738735788)) ;
#71414=CARTESIAN_POINT('Ctrl Pts',(69.3907109930823,237.344712076154,6.61255350476255)) ;
#71415=CARTESIAN_POINT('Ctrl Pts',(69.4139986922107,237.434159724772,6.49311022572802)) ;
#71416=CARTESIAN_POINT('Ctrl Pts',(69.4226403902003,237.51671011904,6.41124585525348)) ;
#71417=CARTESIAN_POINT('Ctrl Pts',(69.4220357539442,237.583935565768,6.3619402730086)) ;
#71418=CARTESIAN_POINT('Ctrl Pts',(69.408113128478,237.705993381689,6.3017093864378)) ;
#71419=CARTESIAN_POINT('Ctrl Pts',(69.3463002437199,237.856072726253,6.33249341474089)) ;
#71420=CARTESIAN_POINT('Ctrl Pts',(69.2496003997641,237.971560196244,6.4698470585811)) ;
#71421=CARTESIAN_POINT('Ctrl Pts',(69.1354707359804,238.065806393091,6.66035004570858)) ;
#71422=CARTESIAN_POINT('Ctrl Pts',(68.9914670223674,238.129856863735,6.93430623056252)) ;
#71423=CARTESIAN_POINT('Ctrl Pts',(68.8793123588541,238.14569213061,7.16318984183832)) ;
#71424=CARTESIAN_POINT('Ctrl Pts',(68.8242223895094,238.145894005322,7.27867958884204)) ;
#71425=CARTESIAN_POINT('Origin',(80.2317703825363,240.454107337488,7.2786795888419)) ;
#71426=CARTESIAN_POINT('',(80.2325032686099,240.654105994678,7.27867958883746)) ;
#71427=CARTESIAN_POINT('Origin',(80.2317703825363,240.454107337488,7.2786795888419)) ;
#71428=CARTESIAN_POINT('',(80.3985455526191,240.48493082833,7.17267980084138)) ;
#71429=CARTESIAN_POINT('Origin',(80.2317703825363,240.454107337488,7.2786795888419)) ;
#71430=CARTESIAN_POINT('Origin',(80.2317703825338,240.454107337488,7.27867958883787)) ;
#71431=CARTESIAN_POINT('Origin',(69.4298369914177,236.635034487937,7.2786795888419)) ;
#71432=CARTESIAN_POINT('',(69.4909429592657,236.444597987514,7.27867958883751)) ;
#71433=CARTESIAN_POINT('Origin',(69.4298369914177,236.635034487937,7.2786795888419)) ;
#71434=CARTESIAN_POINT('',(69.2807493616505,236.554183244321,7.17267980084143)) ;
#71435=CARTESIAN_POINT('Origin',(69.4298369914177,236.635034487937,7.2786795888419)) ;
#71436=CARTESIAN_POINT('Origin',(69.4298369914201,236.635034487938,7.27867958883792)) ;
#71437=CARTESIAN_POINT('Origin',(74.5283628290597,239.4,7.2786795888419)) ;
#71438=CARTESIAN_POINT('Origin',(74.5283628290597,239.4,7.17267980084126)) ;
#71439=CARTESIAN_POINT('Origin',(80.2783628290598,240.159934207678,7.27867958884206)) ;
#71440=CARTESIAN_POINT('',(80.3408628290578,239.969950655758,7.27867958883786)) ;
#71441=CARTESIAN_POINT('Origin',(80.2783628290597,240.159934207678,7.27867958883746)) ;
#71442=CARTESIAN_POINT('',(80.4465004238193,240.182155687653,7.17267980084126)) ;
#71443=CARTESIAN_POINT('Origin',(80.2783628290598,240.159934207678,7.27867958884206)) ;
#71444=CARTESIAN_POINT('Origin',(80.2783628290597,240.159934207678,7.2786795888419)) ;
#71445=CARTESIAN_POINT('Origin',(70.3231932313806,235.405435110687,7.27867958886635)) ;
#71446=CARTESIAN_POINT('',(70.1609601394261,235.522398454837,7.27867958819177)) ;
#71447=CARTESIAN_POINT('Origin',(70.3231932313897,235.405435110699,7.27867958812537)) ;
#71448=CARTESIAN_POINT('',(70.2002285180522,235.288628757201,7.17267980084125)) ;
#71449=CARTESIAN_POINT('Origin',(70.3231932313806,235.405435110687,7.27867958886635)) ;
#71450=CARTESIAN_POINT('Origin',(70.3231932313897,235.405435110699,7.2786795888419)) ;
#71451=CARTESIAN_POINT('Ctrl Pts',(70.1609601392379,235.522398454576,7.27867958886635)) ;
#71452=CARTESIAN_POINT('Ctrl Pts',(70.1931850042782,235.567095701812,7.16316434207535)) ;
#71453=CARTESIAN_POINT('Ctrl Pts',(70.2467521307728,235.666850632939,6.93376990304091)) ;
#71454=CARTESIAN_POINT('Ctrl Pts',(70.2791573181385,235.82106630907,6.66059058867321)) ;
#71455=CARTESIAN_POINT('Ctrl Pts',(70.2719462922848,235.950192751371,6.49243937586827)) ;
#71456=CARTESIAN_POINT('Ctrl Pts',(70.2543651218475,236.031343606776,6.41122181800393)) ;
#71457=CARTESIAN_POINT('Ctrl Pts',(70.2232735078896,236.127109061982,6.335121754773)) ;
#71458=CARTESIAN_POINT('Ctrl Pts',(70.1567428205062,236.241909737955,6.30139298231289)) ;
#71459=CARTESIAN_POINT('Ctrl Pts',(70.0129806384832,236.38232667883,6.38459956034722)) ;
#71460=CARTESIAN_POINT('Ctrl Pts',(69.9044401094434,236.431932501241,6.52710938218576)) ;
#71461=CARTESIAN_POINT('Ctrl Pts',(69.82184001658,236.455045685299,6.65331962753031)) ;
#71462=CARTESIAN_POINT('Ctrl Pts',(69.7565000731658,236.470099247129,6.75725825753585)) ;
#71463=CARTESIAN_POINT('Ctrl Pts',(69.640759497392,236.479083143309,6.96268985033138)) ;
#71464=CARTESIAN_POINT('Ctrl Pts',(69.5434011590231,236.46143041754,7.16318512433996)) ;
#71465=CARTESIAN_POINT('Ctrl Pts',(69.4909429592657,236.444597987514,7.27867958884206)) ;
#71466=CARTESIAN_POINT('Ctrl Pts',(70.1343982367854,235.485555975345,7.24979207610076)) ;
#71467=CARTESIAN_POINT('Ctrl Pts',(70.1717201553335,235.530011742365,7.13555826270375)) ;
#71468=CARTESIAN_POINT('Ctrl Pts',(70.2352127941684,235.631546456137,6.90834410930033)) ;
#71469=CARTESIAN_POINT('Ctrl Pts',(70.2778578331153,235.793397400286,6.63721854494523)) ;
#71470=CARTESIAN_POINT('Ctrl Pts',(70.2749893652713,235.930953158475,6.47017555478502)) ;
#71471=CARTESIAN_POINT('Ctrl Pts',(70.2584811374162,236.017769911042,6.38946600679148)) ;
#71472=CARTESIAN_POINT('Ctrl Pts',(70.2273452442692,236.120398165374,6.31382571916806)) ;
#71473=CARTESIAN_POINT('Ctrl Pts',(70.1570961352955,236.243395649578,6.2802913028328)) ;
#71474=CARTESIAN_POINT('Ctrl Pts',(70.002257580433,236.391500260111,6.36301245408811)) ;
#71475=CARTESIAN_POINT('Ctrl Pts',(69.8847920623921,236.440799947566,6.50464016460755)) ;
#71476=CARTESIAN_POINT('Ctrl Pts',(69.7961700957007,236.461744519509,6.62996437500457)) ;
#71477=CARTESIAN_POINT('Ctrl Pts',(69.726170115545,236.474703621702,6.73315731420172)) ;
#71478=CARTESIAN_POINT('Ctrl Pts',(69.603078658587,236.477799208024,6.9369894242539)) ;
#71479=CARTESIAN_POINT('Ctrl Pts',(69.501498972583,236.452474821217,7.13557881442658)) ;
#71480=CARTESIAN_POINT('Ctrl Pts',(69.447695600056,236.4307210693,7.24979207607674)) ;
#71481=CARTESIAN_POINT('Ctrl Pts',(70.1208580517311,235.398046905423,7.19960828027639)) ;
#71482=CARTESIAN_POINT('Ctrl Pts',(70.1650141283291,235.447937352443,7.08745240215401)) ;
#71483=CARTESIAN_POINT('Ctrl Pts',(70.2404088463949,235.562034042248,6.86383162153399)) ;
#71484=CARTESIAN_POINT('Ctrl Pts',(70.2921760427777,235.744189112754,6.59616799928918)) ;
#71485=CARTESIAN_POINT('Ctrl Pts',(70.2910917260747,235.898794432699,6.43101837867299)) ;
#71486=CARTESIAN_POINT('Ctrl Pts',(70.2735843246182,235.996263311767,6.35118130137054)) ;
#71487=CARTESIAN_POINT('Ctrl Pts',(70.2396455435276,236.111350870535,6.27633391215476)) ;
#71488=CARTESIAN_POINT('Ctrl Pts',(70.1615362719684,236.248921034682,6.2431366136268)) ;
#71489=CARTESIAN_POINT('Ctrl Pts',(69.9878074991475,236.413731031267,6.32501771821064)) ;
#71490=CARTESIAN_POINT('Ctrl Pts',(69.8553150555578,236.467465888111,6.4651280555107)) ;
#71491=CARTESIAN_POINT('Ctrl Pts',(69.7551316491419,236.489433376344,6.5889490867345)) ;
#71492=CARTESIAN_POINT('Ctrl Pts',(69.6759571070458,236.502694500453,6.69087982222723)) ;
#71493=CARTESIAN_POINT('Ctrl Pts',(69.5365048380475,236.503432755258,6.89202712786946)) ;
#71494=CARTESIAN_POINT('Ctrl Pts',(69.4213680030774,236.471458524615,7.08747258003697)) ;
#71495=CARTESIAN_POINT('Ctrl Pts',(69.3602853815846,236.444885377841,7.19960828025282)) ;
#71496=CARTESIAN_POINT('Ctrl Pts',(70.1710194090832,235.31628766108,7.17608503413728)) ;
#71497=CARTESIAN_POINT('Ctrl Pts',(70.214777628573,235.373812834946,7.06213458186475)) ;
#71498=CARTESIAN_POINT('Ctrl Pts',(70.2878736317904,235.503043851011,6.83550821975048)) ;
#71499=CARTESIAN_POINT('Ctrl Pts',(70.3331085651019,235.704853636922,6.56510249374437)) ;
#71500=CARTESIAN_POINT('Ctrl Pts',(70.3248138804196,235.874784619819,6.39850454451589)) ;
#71501=CARTESIAN_POINT('Ctrl Pts',(70.3021011200014,235.981815178004,6.31801009241991)) ;
#71502=CARTESIAN_POINT('Ctrl Pts',(70.2614546651718,236.108252571878,6.24257140290715)) ;
#71503=CARTESIAN_POINT('Ctrl Pts',(70.1736478114485,236.260031613336,6.20912632225173)) ;
#71504=CARTESIAN_POINT('Ctrl Pts',(69.983513761331,236.445249425744,6.29162716702857)) ;
#71505=CARTESIAN_POINT('Ctrl Pts',(69.8401571188674,236.509794674245,6.43287717369066)) ;
#71506=CARTESIAN_POINT('Ctrl Pts',(69.7313643449563,236.539153995676,6.55786810050257)) ;
#71507=CARTESIAN_POINT('Ctrl Pts',(69.645352343298,236.558040720169,6.66078690779107)) ;
#71508=CARTESIAN_POINT('Ctrl Pts',(69.4933529954514,236.567663689091,6.86407978383067)) ;
#71509=CARTESIAN_POINT('Ctrl Pts',(69.3662478807571,236.541692653929,7.0621550826083)) ;
#71510=CARTESIAN_POINT('Ctrl Pts',(69.2980284313689,236.517856659565,7.17608503411333)) ;
#71511=CARTESIAN_POINT('Ctrl Pts',(70.20022851804,235.288628757191,7.17267980086571)) ;
#71512=CARTESIAN_POINT('Ctrl Pts',(70.2429207658929,235.348513784352,7.05716455407471)) ;
#71513=CARTESIAN_POINT('Ctrl Pts',(70.3133732877927,235.482542125275,6.82777011504029)) ;
#71514=CARTESIAN_POINT('Ctrl Pts',(70.3540173856703,235.69095903296,6.55459080067257)) ;
#71515=CARTESIAN_POINT('Ctrl Pts',(70.3415643017227,235.866420668903,6.38643958786764)) ;
#71516=CARTESIAN_POINT('Ctrl Pts',(70.3161098774568,235.977062325867,6.30522203000329)) ;
#71517=CARTESIAN_POINT('Ctrl Pts',(70.2721119966867,236.1079181649,6.22912196677238)) ;
#71518=CARTESIAN_POINT('Ctrl Pts',(70.1799433867558,236.265588695095,6.19539319431226)) ;
#71519=CARTESIAN_POINT('Ctrl Pts',(69.9834029162908,236.459885100479,6.27859977234659)) ;
#71520=CARTESIAN_POINT('Ctrl Pts',(69.8364662050809,236.529661783615,6.42110959418513)) ;
#71521=CARTESIAN_POINT('Ctrl Pts',(69.7250044659152,236.562710994884,6.54731983952968)) ;
#71522=CARTESIAN_POINT('Ctrl Pts',(69.6369109834873,236.584440493439,6.65125846953521)) ;
#71523=CARTESIAN_POINT('Ctrl Pts',(69.4812795913638,236.59873536178,6.85669006233074)) ;
#71524=CARTESIAN_POINT('Ctrl Pts',(69.3508834170229,236.576276518229,7.05718533633934)) ;
#71525=CARTESIAN_POINT('Ctrl Pts',(69.2807493616505,236.554183244321,7.17267980084144)) ;
#71526=CARTESIAN_POINT('Ctrl Pts',(69.2807493616505,236.554183244321,7.17267980084144)) ;
#71527=CARTESIAN_POINT('Ctrl Pts',(69.3319590779197,236.570315069043,7.08834931793388)) ;
#71528=CARTESIAN_POINT('Ctrl Pts',(69.3855949027408,236.581474093001,7.00441091771373)) ;
#71529=CARTESIAN_POINT('Ctrl Pts',(69.4417408216249,236.586783400832,6.92170693026603)) ;
#71530=CARTESIAN_POINT('Ctrl Pts',(69.4539725728908,236.587940067854,6.90368933213478)) ;
#71531=CARTESIAN_POINT('Ctrl Pts',(69.4663235692777,236.588819061917,6.88573016534387)) ;
#71532=CARTESIAN_POINT('Ctrl Pts',(69.4787948641657,236.589411248829,6.86783787638887)) ;
#71533=CARTESIAN_POINT('Ctrl Pts',(69.4873959952969,236.589819664902,6.85549802516093)) ;
#71534=CARTESIAN_POINT('Ctrl Pts',(69.4960552909163,236.590089888067,6.84319004873691)) ;
#71535=CARTESIAN_POINT('Ctrl Pts',(69.5047731716626,236.590218720409,6.83091678535131)) ;
#71536=CARTESIAN_POINT('Ctrl Pts',(69.556483609808,236.590982894298,6.75811746111013)) ;
#71537=CARTESIAN_POINT('Ctrl Pts',(69.6102563665989,236.586769160471,6.68654093637314)) ;
#71538=CARTESIAN_POINT('Ctrl Pts',(69.6663966021717,236.575969671236,6.61755200602656)) ;
#71539=CARTESIAN_POINT('Ctrl Pts',(69.6748967326721,236.574334532607,6.60710646897029)) ;
#71540=CARTESIAN_POINT('Ctrl Pts',(69.683451109302,236.572548502764,6.59672021090978)) ;
#71541=CARTESIAN_POINT('Ctrl Pts',(69.6920607600786,236.57060609939,6.58639791934561)) ;
#71542=CARTESIAN_POINT('Ctrl Pts',(69.7029835120638,236.568141842609,6.57330240204779)) ;
#71543=CARTESIAN_POINT('Ctrl Pts',(69.7139952237171,236.565425892264,6.56030985644741)) ;
#71544=CARTESIAN_POINT('Ctrl Pts',(69.7250718253531,236.562416201434,6.54750568264053)) ;
#71545=CARTESIAN_POINT('Ctrl Pts',(69.7361531518505,236.559405226783,6.53469604705492)) ;
#71546=CARTESIAN_POINT('Ctrl Pts',(69.7472994410321,236.556100272868,6.52207490355897)) ;
#71547=CARTESIAN_POINT('Ctrl Pts',(69.7585650517838,236.552517353318,6.50953957206602)) ;
#71548=CARTESIAN_POINT('Ctrl Pts',(69.7608899925434,236.551777928187,6.50695259265009)) ;
#71549=CARTESIAN_POINT('Ctrl Pts',(69.7632200146727,236.551026664361,6.50436926896037)) ;
#71550=CARTESIAN_POINT('Ctrl Pts',(69.7655549836074,236.550263241167,6.50179017820767)) ;
#71551=CARTESIAN_POINT('Ctrl Pts',(69.7855553820763,236.543724067204,6.47969873109053)) ;
#71552=CARTESIAN_POINT('Ctrl Pts',(69.8058641834356,236.53623717337,6.45803922220507)) ;
#71553=CARTESIAN_POINT('Ctrl Pts',(69.8264406539002,236.527662460389,6.43706326451066)) ;
#71554=CARTESIAN_POINT('Ctrl Pts',(69.8452018191249,236.519844229014,6.41793785577112)) ;
#71555=CARTESIAN_POINT('Ctrl Pts',(69.8641859667403,236.511121916942,6.39937956713362)) ;
#71556=CARTESIAN_POINT('Ctrl Pts',(69.883379872799,236.50135295673,6.38158428357869)) ;
#71557=CARTESIAN_POINT('Ctrl Pts',(69.9025737788576,236.491583996518,6.36378900002375)) ;
#71558=CARTESIAN_POINT('Ctrl Pts',(69.9219774879584,236.480769211382,6.34675558860383)) ;
#71559=CARTESIAN_POINT('Ctrl Pts',(69.941593131925,236.468719349055,6.33070178487188)) ;
#71560=CARTESIAN_POINT('Ctrl Pts',(69.9605431655999,236.457078370189,6.31519272884248)) ;
#71561=CARTESIAN_POINT('Ctrl Pts',(69.979618503998,236.444325329231,6.30066100820867)) ;
#71562=CARTESIAN_POINT('Ctrl Pts',(69.9987383388959,236.430286420514,6.28741717047954)) ;
#71563=CARTESIAN_POINT('Ctrl Pts',(70.0140939925225,236.419011395353,6.27678068821174)) ;
#71564=CARTESIAN_POINT('Ctrl Pts',(70.0294780291067,236.406907548822,6.26697493503162)) ;
#71565=CARTESIAN_POINT('Ctrl Pts',(70.0448397839834,236.393906442639,6.25815306298493)) ;
#71566=CARTESIAN_POINT('Ctrl Pts',(70.060308101801,236.380815149096,6.24926999450349)) ;
#71567=CARTESIAN_POINT('Ctrl Pts',(70.0757532422095,236.366814289963,6.24138525515254)) ;
#71568=CARTESIAN_POINT('Ctrl Pts',(70.0908899939579,236.352010662878,6.23482038635288)) ;
#71569=CARTESIAN_POINT('Ctrl Pts',(70.1033160142712,236.339858110341,6.22943117244389)) ;
#71570=CARTESIAN_POINT('Ctrl Pts',(70.115581139014,236.32708527742,6.22494177541271)) ;
#71571=CARTESIAN_POINT('Ctrl Pts',(70.1275653443907,236.313786509202,6.22144964599584)) ;
#71572=CARTESIAN_POINT('Ctrl Pts',(70.1343467817221,236.306261207322,6.21947357365321)) ;
#71573=CARTESIAN_POINT('Ctrl Pts',(70.1410387242341,236.298566702784,6.21781689625157)) ;
#71574=CARTESIAN_POINT('Ctrl Pts',(70.147623118448,236.2907136989,6.21649820714759)) ;
#71575=CARTESIAN_POINT('Ctrl Pts',(70.1490267954304,236.289039576659,6.21621708583529)) ;
#71576=CARTESIAN_POINT('Ctrl Pts',(70.1504255841125,236.287358685623,6.21595091721346)) ;
#71577=CARTESIAN_POINT('Ctrl Pts',(70.1518191192861,236.285671000608,6.21570025382672)) ;
#71578=CARTESIAN_POINT('Ctrl Pts',(70.16192767474,236.273428713588,6.21388196836604)) ;
#71579=CARTESIAN_POINT('Ctrl Pts',(70.1717615809203,236.260825207069,6.21288083219659)) ;
#71580=CARTESIAN_POINT('Ctrl Pts',(70.1812304076324,236.247940575129,6.21273144315338)) ;
#71581=CARTESIAN_POINT('Ctrl Pts',(70.1834031091985,236.244984088455,6.21269716458667)) ;
#71582=CARTESIAN_POINT('Ctrl Pts',(70.1855564979326,236.242012986854,6.21270766617075)) ;
#71583=CARTESIAN_POINT('Ctrl Pts',(70.1876893200618,236.239028564853,6.21276324896012)) ;
#71584=CARTESIAN_POINT('Ctrl Pts',(70.1994859153622,236.222521788191,6.21307067622421)) ;
#71585=CARTESIAN_POINT('Ctrl Pts',(70.2106516821943,236.205608285263,6.21475861764742)) ;
#71586=CARTESIAN_POINT('Ctrl Pts',(70.2211478113664,236.188515258521,6.21764264372665)) ;
#71587=CARTESIAN_POINT('Ctrl Pts',(70.2324846782147,236.170053084034,6.220757679671)) ;
#71588=CARTESIAN_POINT('Ctrl Pts',(70.2430369254153,236.151370609642,6.22528290282593)) ;
#71589=CARTESIAN_POINT('Ctrl Pts',(70.2526957215038,236.132674355337,6.23114154687197)) ;
#71590=CARTESIAN_POINT('Ctrl Pts',(70.2564754921352,236.125357961835,6.2334342063817)) ;
#71591=CARTESIAN_POINT('Ctrl Pts',(70.260118033631,236.11803973881,6.23593133092263)) ;
#71592=CARTESIAN_POINT('Ctrl Pts',(70.2636152474668,236.110733253645,6.23862924431399)) ;
#71593=CARTESIAN_POINT('Ctrl Pts',(70.2709385177015,236.095433255464,6.2442787555428)) ;
#71594=CARTESIAN_POINT('Ctrl Pts',(70.2777253779092,236.080166897609,6.25069647533058)) ;
#71595=CARTESIAN_POINT('Ctrl Pts',(70.2839124106202,236.065060026814,6.25783535999049)) ;
#71596=CARTESIAN_POINT('Ctrl Pts',(70.2930019121523,236.04286620117,6.26832324749414)) ;
#71597=CARTESIAN_POINT('Ctrl Pts',(70.3007972127425,236.021015255836,6.28036894733972)) ;
#71598=CARTESIAN_POINT('Ctrl Pts',(70.3075542718491,235.99953565987,6.29352856224887)) ;
#71599=CARTESIAN_POINT('Ctrl Pts',(70.3098379004578,235.992276374568,6.29797601085224)) ;
#71600=CARTESIAN_POINT('Ctrl Pts',(70.3120027927952,235.985059868179,6.3025504679656)) ;
#71601=CARTESIAN_POINT('Ctrl Pts',(70.3140583396407,235.977888291778,6.30723419110208)) ;
#71602=CARTESIAN_POINT('Ctrl Pts',(70.3196248424662,235.958467376908,6.31991790012607)) ;
#71603=CARTESIAN_POINT('Ctrl Pts',(70.3243904463304,235.939374283972,6.33340375113264)) ;
#71604=CARTESIAN_POINT('Ctrl Pts',(70.3283435121341,235.92071582897,6.3475713681177)) ;
#71605=CARTESIAN_POINT('Ctrl Pts',(70.3301707656114,235.912091199764,6.35412016560448)) ;
#71606=CARTESIAN_POINT('Ctrl Pts',(70.3318423411922,235.903547471452,6.36080440747604)) ;
#71607=CARTESIAN_POINT('Ctrl Pts',(70.3333637193716,235.895089211632,6.36761024660822)) ;
#71608=CARTESIAN_POINT('Ctrl Pts',(70.3399404610533,235.858525133966,6.39703110100394)) ;
#71609=CARTESIAN_POINT('Ctrl Pts',(70.3437132892228,235.823554781582,6.42872456076543)) ;
#71610=CARTESIAN_POINT('Ctrl Pts',(70.3453514963652,235.789975276158,6.46185814658185)) ;
#71611=CARTESIAN_POINT('Ctrl Pts',(70.3461125296866,235.774375830958,6.47725043868668)) ;
#71612=CARTESIAN_POINT('Ctrl Pts',(70.3464123831586,235.75907715216,6.49295347092891)) ;
#71613=CARTESIAN_POINT('Ctrl Pts',(70.3463158622058,235.74406175549,6.50888324943074)) ;
#71614=CARTESIAN_POINT('Ctrl Pts',(70.3461706709433,235.721474904293,6.53284555589007)) ;
#71615=CARTESIAN_POINT('Ctrl Pts',(70.3451288208109,235.699528711558,6.55732105604831)) ;
#71616=CARTESIAN_POINT('Ctrl Pts',(70.3432478451576,235.678198197327,6.58223895751767)) ;
#71617=CARTESIAN_POINT('Ctrl Pts',(70.3395731031339,235.636526133739,6.63091947048106)) ;
#71618=CARTESIAN_POINT('Ctrl Pts',(70.332883258592,235.597151168654,6.68111805683607)) ;
#71619=CARTESIAN_POINT('Ctrl Pts',(70.3237807975196,235.559733632043,6.73226848360573)) ;
#71620=CARTESIAN_POINT('Ctrl Pts',(70.3180111619245,235.536016359385,6.76469041001147)) ;
#71621=CARTESIAN_POINT('Ctrl Pts',(70.3112713077793,235.513086421843,6.79749490207164)) ;
#71622=CARTESIAN_POINT('Ctrl Pts',(70.3037075134353,235.490865083653,6.83053760674758)) ;
#71623=CARTESIAN_POINT('Ctrl Pts',(70.2907203769847,235.452710747606,6.8872723743532)) ;
#71624=CARTESIAN_POINT('Ctrl Pts',(70.2753055266936,235.416643266994,6.94471046359219)) ;
#71625=CARTESIAN_POINT('Ctrl Pts',(70.2576459683243,235.382564105862,7.00265575482928)) ;
#71626=CARTESIAN_POINT('Ctrl Pts',(70.2404810591012,235.349439511521,7.05897798232704)) ;
#71627=CARTESIAN_POINT('Ctrl Pts',(70.221276258631,235.318152724197,7.11572953305135)) ;
#71628=CARTESIAN_POINT('Ctrl Pts',(70.2002285180487,235.288628757204,7.17267980084144)) ;
#71629=CARTESIAN_POINT('Ctrl Pts',(70.1609601392379,235.522398454576,7.27867958886635)) ;
#71630=CARTESIAN_POINT('Ctrl Pts',(70.1931850042782,235.567095701812,7.16316434207535)) ;
#71631=CARTESIAN_POINT('Ctrl Pts',(70.2467521307728,235.666850632939,6.93376990304091)) ;
#71632=CARTESIAN_POINT('Ctrl Pts',(70.2791573181385,235.82106630907,6.66059058867321)) ;
#71633=CARTESIAN_POINT('Ctrl Pts',(70.2719462922848,235.950192751371,6.49243937586827)) ;
#71634=CARTESIAN_POINT('Ctrl Pts',(70.2543651218475,236.031343606776,6.41122181800393)) ;
#71635=CARTESIAN_POINT('Ctrl Pts',(70.2232735078896,236.127109061982,6.335121754773)) ;
#71636=CARTESIAN_POINT('Ctrl Pts',(70.1567428205062,236.241909737955,6.30139298231289)) ;
#71637=CARTESIAN_POINT('Ctrl Pts',(70.0129806384832,236.38232667883,6.38459956034722)) ;
#71638=CARTESIAN_POINT('Ctrl Pts',(69.9044401094434,236.431932501241,6.52710938218576)) ;
#71639=CARTESIAN_POINT('Ctrl Pts',(69.82184001658,236.455045685299,6.65331962753031)) ;
#71640=CARTESIAN_POINT('Ctrl Pts',(69.7565000731658,236.470099247129,6.75725825753585)) ;
#71641=CARTESIAN_POINT('Ctrl Pts',(69.640759497392,236.479083143309,6.96268985033138)) ;
#71642=CARTESIAN_POINT('Ctrl Pts',(69.5434011590231,236.46143041754,7.16318512433996)) ;
#71643=CARTESIAN_POINT('Ctrl Pts',(69.4909429592657,236.444597987514,7.27867958884206)) ;
#71644=CARTESIAN_POINT('Origin',(80.2783628290597,238.640065792321,7.2786795888419)) ;
#71645=CARTESIAN_POINT('',(80.3408628290597,238.830049344241,7.27867958883748)) ;
#71646=CARTESIAN_POINT('Origin',(80.2783628290597,238.640065792321,7.2786795888419)) ;
#71647=CARTESIAN_POINT('',(80.4465004238194,238.617844312347,7.17267980084142)) ;
#71648=CARTESIAN_POINT('Origin',(80.2783628290597,238.640065792321,7.2786795888419)) ;
#71649=CARTESIAN_POINT('Origin',(80.2783628290572,238.640065792322,7.27867958883786)) ;
#71650=CARTESIAN_POINT('Origin',(70.5337979397592,235.19483040233,7.2786795888419)) ;
#71651=CARTESIAN_POINT('',(70.6507612836456,235.032597310185,7.2786795888375)) ;
#71652=CARTESIAN_POINT('Origin',(70.5337979397592,235.19483040233,7.2786795888419)) ;
#71653=CARTESIAN_POINT('',(70.4169915862637,235.071865688989,7.17267980084143)) ;
#71654=CARTESIAN_POINT('Origin',(70.5337979397592,235.19483040233,7.2786795888419)) ;
#71655=CARTESIAN_POINT('Origin',(70.5337979397612,235.194830402331,7.27867958883792)) ;
#71656=CARTESIAN_POINT('Origin',(74.5283628290597,239.4,7.2786795888419)) ;
#71657=CARTESIAN_POINT('Origin',(74.5283628290597,239.4,7.17267980084126)) ;
#71658=CARTESIAN_POINT('Origin',(80.2317703825364,238.345892662512,7.27867958884205)) ;
#71659=CARTESIAN_POINT('',(80.232503268608,238.145894005322,7.2786795888379)) ;
#71660=CARTESIAN_POINT('Origin',(80.2317703825363,238.345892662512,7.27867958883749)) ;
#71661=CARTESIAN_POINT('',(80.398545552619,238.31506917167,7.17267980084126)) ;
#71662=CARTESIAN_POINT('Origin',(80.2317703825364,238.345892662512,7.27867958884205)) ;
#71663=CARTESIAN_POINT('Origin',(80.2317703825363,238.345892662512,7.2786795888419)) ;
#71664=CARTESIAN_POINT('Origin',(71.763397316992,234.301474162343,7.27867958886637)) ;
#71665=CARTESIAN_POINT('',(71.5729608166685,234.362580130501,7.27867958819176)) ;
#71666=CARTESIAN_POINT('Origin',(71.7633973169967,234.301474162358,7.27867958812535)) ;
#71667=CARTESIAN_POINT('',(71.6825460733849,234.152386532589,7.17267980084127)) ;
#71668=CARTESIAN_POINT('Origin',(71.763397316992,234.301474162343,7.27867958886637)) ;
#71669=CARTESIAN_POINT('Origin',(71.7633973169967,234.301474162358,7.2786795888419)) ;
#71670=CARTESIAN_POINT('Ctrl Pts',(71.5729608165702,234.362580130195,7.27867958886637)) ;
#71671=CARTESIAN_POINT('Ctrl Pts',(71.5897962754558,234.415047769378,7.16316434207538)) ;
#71672=CARTESIAN_POINT('Ctrl Pts',(71.6099156712164,234.526473499131,6.93376990288358)) ;
#71673=CARTESIAN_POINT('Ctrl Pts',(71.5930795710948,234.683155076464,6.66059058845597)) ;
#71674=CARTESIAN_POINT('Ctrl Pts',(71.546319212863,234.80373329132,6.49243937563568)) ;
#71675=CARTESIAN_POINT('Ctrl Pts',(71.5045215327204,234.875479460712,6.41122181777537)) ;
#71676=CARTESIAN_POINT('Ctrl Pts',(71.4453584975031,234.956949983836,6.33512175456427)) ;
#71677=CARTESIAN_POINT('Ctrl Pts',(71.3466086938307,235.045572801762,6.30139298216567)) ;
#71678=CARTESIAN_POINT('Ctrl Pts',(71.1664915127874,235.134692290987,6.38459956020394)) ;
#71679=CARTESIAN_POINT('Ctrl Pts',(71.0479342931672,235.148329363567,6.52710938215577)) ;
#71680=CARTESIAN_POINT('Ctrl Pts',(70.9622345699239,235.144786475434,6.65331962754072)) ;
#71681=CARTESIAN_POINT('Ctrl Pts',(70.8954407845371,235.138912110575,6.75725825755124)) ;
#71682=CARTESIAN_POINT('Ctrl Pts',(70.7825887791445,235.111690498715,6.96268985038042)) ;
#71683=CARTESIAN_POINT('Ctrl Pts',(70.6954504894233,235.064816377666,7.16318512433998)) ;
#71684=CARTESIAN_POINT('Ctrl Pts',(70.6507612836455,235.032597310185,7.2786795888421)) ;
#71685=CARTESIAN_POINT('Ctrl Pts',(71.5590838983549,234.319332770985,7.24979207610078)) ;
#71686=CARTESIAN_POINT('Ctrl Pts',(71.5808415646835,234.37314582499,7.13555826270378)) ;
#71687=CARTESIAN_POINT('Ctrl Pts',(71.6098507007678,234.489331380785,6.90834410923801)) ;
#71688=CARTESIAN_POINT('Ctrl Pts',(71.6003938507359,234.656438817778,6.6372185448683)) ;
#71689=CARTESIAN_POINT('Ctrl Pts',(71.5551587087757,234.786375712703,6.47017555471278)) ;
#71690=CARTESIAN_POINT('Ctrl Pts',(71.5126305991571,234.863842028009,6.38946600672481)) ;
#71691=CARTESIAN_POINT('Ctrl Pts',(71.4513047303754,234.951825777958,6.3138257191277)) ;
#71692=CARTESIAN_POINT('Ctrl Pts',(71.3464855445711,235.047095168322,6.28029130286015)) ;
#71693=CARTESIAN_POINT('Ctrl Pts',(71.1534584863863,235.140103278427,6.36301245411851)) ;
#71694=CARTESIAN_POINT('Ctrl Pts',(71.0265076986766,235.150691226064,6.50464016473808)) ;
#71695=CARTESIAN_POINT('Ctrl Pts',(70.9357509710693,235.143225003883,6.62996437516892)) ;
#71696=CARTESIAN_POINT('Ctrl Pts',(70.8651724509822,235.133918658977,6.73315731436466)) ;
#71697=CARTESIAN_POINT('Ctrl Pts',(70.747148929931,235.098825384429,6.93698942444201)) ;
#71698=CARTESIAN_POINT('Ctrl Pts',(70.658366573421,235.043350611714,7.1355788144266)) ;
#71699=CARTESIAN_POINT('Ctrl Pts',(70.6139188044143,235.006035407734,7.24979207607677)) ;
#71700=CARTESIAN_POINT('Ctrl Pts',(71.573248206895,234.231922552512,7.19960828027642)) ;
#71701=CARTESIAN_POINT('Ctrl Pts',(71.5998261352915,234.293016165325,7.08745240215403)) ;
#71702=CARTESIAN_POINT('Ctrl Pts',(71.6362729570513,234.42482681484,6.86383162135823)) ;
#71703=CARTESIAN_POINT('Ctrl Pts',(71.6292174740789,234.61406352507,6.59616799904429)) ;
#71704=CARTESIAN_POINT('Ctrl Pts',(71.5804105563069,234.760766849778,6.43101837840856)) ;
#71705=CARTESIAN_POINT('Ctrl Pts',(71.5336404880062,234.848055177775,6.35118130110973)) ;
#71706=CARTESIAN_POINT('Ctrl Pts',(71.4657987775582,234.947022290368,6.27633391191204)) ;
#71707=CARTESIAN_POINT('Ctrl Pts',(71.3490009271422,235.053722199109,6.24313661344331)) ;
#71708=CARTESIAN_POINT('Ctrl Pts',(71.1328459558896,235.156780677101,6.32501771803124)) ;
#71709=CARTESIAN_POINT('Ctrl Pts',(70.9902331700443,235.166943146138,6.46512805544576)) ;
#71710=CARTESIAN_POINT('Ctrl Pts',(70.88816476135,235.15687709382,6.58894908671078)) ;
#71711=CARTESIAN_POINT('Ctrl Pts',(70.8087673844567,235.145022893286,6.69087982220983)) ;
#71712=CARTESIAN_POINT('Ctrl Pts',(70.6759122620273,235.102631894295,6.8920271278871)) ;
#71713=CARTESIAN_POINT('Ctrl Pts',(70.5762912057495,235.036643355181,7.08747258003699)) ;
#71714=CARTESIAN_POINT('Ctrl Pts',(70.5264097344936,234.992495222681,7.19960828025285)) ;
#71715=CARTESIAN_POINT('Ctrl Pts',(71.6462194886202,234.169665602295,7.17608503413731)) ;
#71716=CARTESIAN_POINT('Ctrl Pts',(71.6700597720785,234.237897327217,7.06213458186478)) ;
#71717=CARTESIAN_POINT('Ctrl Pts',(71.6996436221789,234.383391234504,6.83550821965688)) ;
#71718=CARTESIAN_POINT('Ctrl Pts',(71.6803019468063,234.589302109655,6.5651024936217)) ;
#71719=CARTESIAN_POINT('Ctrl Pts',(71.6199016712978,234.748352879764,6.39850454439136)) ;
#71720=CARTESIAN_POINT('Ctrl Pts',(71.5652262910956,234.843126360614,6.31801009230045)) ;
#71721=CARTESIAN_POINT('Ctrl Pts',(71.4874979119008,234.950815022676,6.24257140281179)) ;
#71722=CARTESIAN_POINT('Ctrl Pts',(71.3570863282151,235.068031659091,6.20912632222179)) ;
#71723=CARTESIAN_POINT('Ctrl Pts',(71.1190226491792,235.185429613822,6.29162716700193)) ;
#71724=CARTESIAN_POINT('Ctrl Pts',(70.962736801447,235.202516154191,6.43287717376783)) ;
#71725=CARTESIAN_POINT('Ctrl Pts',(70.8501961956108,235.196819712128,6.55786810061549)) ;
#71726=CARTESIAN_POINT('Ctrl Pts',(70.7625576021184,235.188202884286,6.66078690790468)) ;
#71727=CARTESIAN_POINT('Ctrl Pts',(70.6150239709294,235.150384489946,6.86407978397195)) ;
#71728=CARTESIAN_POINT('Ctrl Pts',(70.5021653146945,235.086406927003,7.06215508260831)) ;
#71729=CARTESIAN_POINT('Ctrl Pts',(70.444650490152,235.042656580033,7.17608503411336)) ;
#71730=CARTESIAN_POINT('Ctrl Pts',(71.6825460733761,234.152386532576,7.17267980086574)) ;
#71731=CARTESIAN_POINT('Ctrl Pts',(71.7046433227907,234.222533208,7.05716455407474)) ;
#71732=CARTESIAN_POINT('Ctrl Pts',(71.7302306178125,234.371772761628,6.82777011488293)) ;
#71733=CARTESIAN_POINT('Ctrl Pts',(71.7044810855518,234.582548736796,6.55459080045533)) ;
#71734=CARTESIAN_POINT('Ctrl Pts',(71.6384168715341,234.745574454467,6.38643958763504)) ;
#71735=CARTESIAN_POINT('Ctrl Pts',(71.5800181231714,234.842935073619,6.30522202977473)) ;
#71736=CARTESIAN_POINT('Ctrl Pts',(71.4977369738496,234.953790279167,6.22912196656362)) ;
#71737=CARTESIAN_POINT('Ctrl Pts',(71.3613565433507,235.075262197541,6.19539319416503)) ;
#71738=CARTESIAN_POINT('Ctrl Pts',(71.1143945569827,235.199314714521,6.27859977220329)) ;
#71739=CARTESIAN_POINT('Ctrl Pts',(70.9530872593356,235.220270342818,6.42110959415512)) ;
#71740=CARTESIAN_POINT('Ctrl Pts',(70.8368680780374,235.217258438914,6.54731983954008)) ;
#71741=CARTESIAN_POINT('Ctrl Pts',(70.7463714132023,235.210702036941,6.65125846955059)) ;
#71742=CARTESIAN_POINT('Ctrl Pts',(70.5939398063231,235.176204519588,6.85669006237978)) ;
#71743=CARTESIAN_POINT('Ctrl Pts',(70.4768658395408,235.114550256101,7.05718533633935)) ;
#71744=CARTESIAN_POINT('Ctrl Pts',(70.4169915862637,235.071865688989,7.17267980084146)) ;
#71745=CARTESIAN_POINT('Ctrl Pts',(70.4169915862637,235.071865688989,7.17267980084144)) ;
#71746=CARTESIAN_POINT('Ctrl Pts',(70.4607099053372,235.103032633416,7.08834933200133)) ;
#71747=CARTESIAN_POINT('Ctrl Pts',(70.5082722694194,235.130219873369,7.00441094571219)) ;
#71748=CARTESIAN_POINT('Ctrl Pts',(70.5600295350521,235.152619366136,6.92170697164805)) ;
#71749=CARTESIAN_POINT('Ctrl Pts',(70.5713052003606,235.15749924494,6.90368935963091)) ;
#71750=CARTESIAN_POINT('Ctrl Pts',(70.5827800804835,235.162151889495,6.88573017903702)) ;
#71751=CARTESIAN_POINT('Ctrl Pts',(70.5944579998749,235.166568938161,6.86783787638139)) ;
#71752=CARTESIAN_POINT('Ctrl Pts',(70.6025119541606,235.169615260612,6.85549802517807)) ;
#71753=CARTESIAN_POINT('Ctrl Pts',(70.6106639301175,235.172548127615,6.84319004877812)) ;
#71754=CARTESIAN_POINT('Ctrl Pts',(70.618915316007,235.175364627756,6.83091678541572)) ;
#71755=CARTESIAN_POINT('Ctrl Pts',(70.6678587106083,235.19207080047,6.75811747874931)) ;
#71756=CARTESIAN_POINT('Ctrl Pts',(70.7203017431665,235.204679995143,6.68654097097228)) ;
#71757=CARTESIAN_POINT('Ctrl Pts',(70.7770314899421,235.211757358392,6.61755205602087)) ;
#71758=CARTESIAN_POINT('Ctrl Pts',(70.7856208934466,235.212828936041,6.60710650211769)) ;
#71759=CARTESIAN_POINT('Ctrl Pts',(70.7943085163447,235.213773770197,6.59672022739229)) ;
#71760=CARTESIAN_POINT('Ctrl Pts',(70.8030970304804,235.214586964518,6.5863979193675)) ;
#71761=CARTESIAN_POINT('Ctrl Pts',(70.8142466821517,235.215618633044,6.57330240206598)) ;
#71762=CARTESIAN_POINT('Ctrl Pts',(70.8255587170839,235.216438416814,6.56030985646277)) ;
#71763=CARTESIAN_POINT('Ctrl Pts',(70.8370232368604,235.216998888888,6.54750568265232)) ;
#71764=CARTESIAN_POINT('Ctrl Pts',(70.8484926469705,235.217559600038,6.53469604706237)) ;
#71765=CARTESIAN_POINT('Ctrl Pts',(70.8601146848551,235.217860794865,6.52207490356155)) ;
#71766=CARTESIAN_POINT('Ctrl Pts',(70.8719361004024,235.217934501056,6.50953957206406)) ;
#71767=CARTESIAN_POINT('Ctrl Pts',(70.8743757454206,235.217949712173,6.50695259261839)) ;
#71768=CARTESIAN_POINT('Ctrl Pts',(70.8768238814666,235.217955234252,6.50436926889872)) ;
#71769=CARTESIAN_POINT('Ctrl Pts',(70.8792804796558,235.217950720732,6.5017901781165)) ;
#71770=CARTESIAN_POINT('Ctrl Pts',(70.9003227040899,235.217912059745,6.47969873177633)) ;
#71771=CARTESIAN_POINT('Ctrl Pts',(70.9219510986209,235.217067365371,6.45803922365016)) ;
#71772=CARTESIAN_POINT('Ctrl Pts',(70.94417021616,235.21527080788,6.43706326666271)) ;
#71773=CARTESIAN_POINT('Ctrl Pts',(70.9644291113308,235.213632746881,6.41793785752039)) ;
#71774=CARTESIAN_POINT('Ctrl Pts',(70.9851794516754,235.211203759364,6.39937956849862)) ;
#71775=CARTESIAN_POINT('Ctrl Pts',(71.0064527162314,235.207844169209,6.38158428458251)) ;
#71776=CARTESIAN_POINT('Ctrl Pts',(71.0277259807874,235.204484579055,6.3637890006664)) ;
#71777=CARTESIAN_POINT('Ctrl Pts',(71.0495219575831,235.20019518297,6.34675558890809)) ;
#71778=CARTESIAN_POINT('Ctrl Pts',(71.0719011562713,235.194796650121,6.33070178486451)) ;
#71779=CARTESIAN_POINT('Ctrl Pts',(71.0935209676707,235.189581304225,6.31519273020627)) ;
#71780=CARTESIAN_POINT('Ctrl Pts',(71.1156035969373,235.183347045925,6.30066101074671)) ;
#71781=CARTESIAN_POINT('Ctrl Pts',(71.1381258998109,235.175903605113,6.287417173937)) ;
#71782=CARTESIAN_POINT('Ctrl Pts',(71.1562141705429,235.169925576431,6.27678069031052)) ;
#71783=CARTESIAN_POINT('Ctrl Pts',(71.1745855550277,235.163168062437,6.26697493593538)) ;
#71784=CARTESIAN_POINT('Ctrl Pts',(71.1932130168892,235.155550318177,6.25815306292166)) ;
#71785=CARTESIAN_POINT('Ctrl Pts',(71.2119696935569,235.14787973122,6.24926999442026)) ;
#71786=CARTESIAN_POINT('Ctrl Pts',(71.2309853984281,235.139336933751,6.2413852550664)) ;
#71787=CARTESIAN_POINT('Ctrl Pts',(71.2499558771897,235.129935361234,6.23482038629555)) ;
#71788=CARTESIAN_POINT('Ctrl Pts',(71.2655290706333,235.122217448085,6.22943117221267)) ;
#71789=CARTESIAN_POINT('Ctrl Pts',(71.2811409204754,235.11385989374,6.22494177505686)) ;
#71790=CARTESIAN_POINT('Ctrl Pts',(71.2966481230571,235.104915336306,6.22144964558793)) ;
#71791=CARTESIAN_POINT('Ctrl Pts',(71.3054230987959,235.099853928611,6.21947357342371)) ;
#71792=CARTESIAN_POINT('Ctrl Pts',(71.3141652464035,235.094603944233,6.21781689615633)) ;
#71793=CARTESIAN_POINT('Ctrl Pts',(71.3228540885002,235.089169983791,6.21649820714117)) ;
#71794=CARTESIAN_POINT('Ctrl Pts',(71.324706396824,235.088011558992,6.21621708583501)) ;
#71795=CARTESIAN_POINT('Ctrl Pts',(71.3265561477709,235.086845186119,6.21595091721855)) ;
#71796=CARTESIAN_POINT('Ctrl Pts',(71.3284030017896,235.085670728364,6.21570025383654)) ;
#71797=CARTESIAN_POINT('Ctrl Pts',(71.3417998851196,235.077151336275,6.21388196822763)) ;
#71798=CARTESIAN_POINT('Ctrl Pts',(71.355047184409,235.068203532669,6.2128808320335)) ;
#71799=CARTESIAN_POINT('Ctrl Pts',(71.3680341449888,235.0588755471,6.21273144306716)) ;
#71800=CARTESIAN_POINT('Ctrl Pts',(71.3710141106076,235.056735163589,6.21269716453211)) ;
#71801=CARTESIAN_POINT('Ctrl Pts',(71.3739802249021,235.054574912477,6.21270766611658)) ;
#71802=CARTESIAN_POINT('Ctrl Pts',(71.376930895434,235.052395637495,6.21276324887439)) ;
#71803=CARTESIAN_POINT('Ctrl Pts',(71.3932509988059,235.040342108444,6.21307067606536)) ;
#71804=CARTESIAN_POINT('Ctrl Pts',(71.4090968339605,235.027706822968,6.21475861749067)) ;
#71805=CARTESIAN_POINT('Ctrl Pts',(71.4243612817605,235.014693870785,6.21764264357176)) ;
#71806=CARTESIAN_POINT('Ctrl Pts',(71.4408484138844,235.00063857938,6.22075768053023)) ;
#71807=CARTESIAN_POINT('Ctrl Pts',(71.456657404311,234.986131309192,6.22528290568737)) ;
#71808=CARTESIAN_POINT('Ctrl Pts',(71.4716209298653,234.971334841834,6.23114155254727)) ;
#71809=CARTESIAN_POINT('Ctrl Pts',(71.4774765901959,234.965544556208,6.23343421050972)) ;
#71810=CARTESIAN_POINT('Ctrl Pts',(71.4832023034251,234.959710124551,6.23593133315564)) ;
#71811=CARTESIAN_POINT('Ctrl Pts',(71.4887861748817,234.953841947605,6.23862924430743)) ;
#71812=CARTESIAN_POINT('Ctrl Pts',(71.5004789781708,234.941553799636,6.24427875551742)) ;
#71813=CARTESIAN_POINT('Ctrl Pts',(71.5116512297788,234.929131885705,6.2506964752804)) ;
#71814=CARTESIAN_POINT('Ctrl Pts',(71.52220372733,234.91667629609,6.25783535991065)) ;
#71815=CARTESIAN_POINT('Ctrl Pts',(71.5377066262744,234.898377524056,6.26832324739526)) ;
#71816=CARTESIAN_POINT('Ctrl Pts',(71.5518727111388,234.880004920488,6.28036894721856)) ;
#71817=CARTESIAN_POINT('Ctrl Pts',(71.5649366164117,234.861664656893,6.293528562104)) ;
#71818=CARTESIAN_POINT('Ctrl Pts',(71.5693517188205,234.855466346335,6.29797601071645)) ;
#71819=CARTESIAN_POINT('Ctrl Pts',(71.5736406769129,234.849272029415,6.30255046783972)) ;
#71820=CARTESIAN_POINT('Ctrl Pts',(71.5778117571322,234.843086653838,6.30723419098684)) ;
#71821=CARTESIAN_POINT('Ctrl Pts',(71.589107208696,234.826336410121,6.31991790004191)) ;
#71822=CARTESIAN_POINT('Ctrl Pts',(71.5995396575293,234.809650452202,6.33340375108472)) ;
#71823=CARTESIAN_POINT('Ctrl Pts',(71.6090650262337,234.793126771453,6.34757136811092)) ;
#71824=CARTESIAN_POINT('Ctrl Pts',(71.6134680045255,234.785488914075,6.35412016555376)) ;
#71825=CARTESIAN_POINT('Ctrl Pts',(71.6176979245902,234.777879890904,6.36080440737922)) ;
#71826=CARTESIAN_POINT('Ctrl Pts',(71.6217585872235,234.770305739548,6.36761024646398)) ;
#71827=CARTESIAN_POINT('Ctrl Pts',(71.6393123616443,234.737563560173,6.39703110084805)) ;
#71828=CARTESIAN_POINT('Ctrl Pts',(71.6537069676523,234.705470646685,6.42872456059852)) ;
#71829=CARTESIAN_POINT('Ctrl Pts',(71.6656416330752,234.674040873088,6.46185814640417)) ;
#71830=CARTESIAN_POINT('Ctrl Pts',(71.6711859124497,234.659440091304,6.47725043851097)) ;
#71831=CARTESIAN_POINT('Ctrl Pts',(71.6761986417932,234.644982842956,6.49295347075555)) ;
#71832=CARTESIAN_POINT('Ctrl Pts',(71.6807468576651,234.630672525488,6.50888324926009)) ;
#71833=CARTESIAN_POINT('Ctrl Pts',(71.6875884934589,234.609146286856,6.53284555577163)) ;
#71834=CARTESIAN_POINT('Ctrl Pts',(71.6933793816343,234.587952267802,6.55732105598457)) ;
#71835=CARTESIAN_POINT('Ctrl Pts',(71.6981819588895,234.567084489756,6.5822389575114)) ;
#71836=CARTESIAN_POINT('Ctrl Pts',(71.7075644473025,234.526316444743,6.63091947006312)) ;
#71837=CARTESIAN_POINT('Ctrl Pts',(71.7133695604041,234.486801352293,6.68111805597746)) ;
#71838=CARTESIAN_POINT('Ctrl Pts',(71.7162752602129,234.448402345422,6.73226848229616)) ;
#71839=CARTESIAN_POINT('Ctrl Pts',(71.7181170510495,234.424062962952,6.76469040908816)) ;
#71840=CARTESIAN_POINT('Ctrl Pts',(71.7187928092504,234.400172566665,6.79749490154681)) ;
#71841=CARTESIAN_POINT('Ctrl Pts',(71.7184659844885,234.376701476897,6.83053760662836)) ;
#71842=CARTESIAN_POINT('Ctrl Pts',(71.7179048219905,234.336401301076,6.88727237427162)) ;
#71843=CARTESIAN_POINT('Ctrl Pts',(71.7143898926252,234.297335637882,6.94471046355436)) ;
#71844=CARTESIAN_POINT('Ctrl Pts',(71.7081256945041,234.259467325945,7.00265575483063)) ;
#71845=CARTESIAN_POINT('Ctrl Pts',(71.7020369583204,234.222659715993,7.0589779823287)) ;
#71846=CARTESIAN_POINT('Ctrl Pts',(71.693440256672,234.186969603319,7.11572953305254)) ;
#71847=CARTESIAN_POINT('Ctrl Pts',(71.6825460733806,234.152386532591,7.17267980084152)) ;
#71848=CARTESIAN_POINT('Ctrl Pts',(71.5729608165702,234.362580130195,7.27867958886637)) ;
#71849=CARTESIAN_POINT('Ctrl Pts',(71.5897962754558,234.415047769378,7.16316434207538)) ;
#71850=CARTESIAN_POINT('Ctrl Pts',(71.6099156712164,234.526473499131,6.93376990288358)) ;
#71851=CARTESIAN_POINT('Ctrl Pts',(71.5930795710948,234.683155076464,6.66059058845597)) ;
#71852=CARTESIAN_POINT('Ctrl Pts',(71.546319212863,234.80373329132,6.49243937563568)) ;
#71853=CARTESIAN_POINT('Ctrl Pts',(71.5045215327204,234.875479460712,6.41122181777537)) ;
#71854=CARTESIAN_POINT('Ctrl Pts',(71.4453584975031,234.956949983836,6.33512175456427)) ;
#71855=CARTESIAN_POINT('Ctrl Pts',(71.3466086938307,235.045572801762,6.30139298216567)) ;
#71856=CARTESIAN_POINT('Ctrl Pts',(71.1664915127874,235.134692290987,6.38459956020394)) ;
#71857=CARTESIAN_POINT('Ctrl Pts',(71.0479342931672,235.148329363567,6.52710938215577)) ;
#71858=CARTESIAN_POINT('Ctrl Pts',(70.9622345699239,235.144786475434,6.65331962754072)) ;
#71859=CARTESIAN_POINT('Ctrl Pts',(70.8954407845371,235.138912110575,6.75725825755124)) ;
#71860=CARTESIAN_POINT('Ctrl Pts',(70.7825887791445,235.111690498715,6.96268985038042)) ;
#71861=CARTESIAN_POINT('Ctrl Pts',(70.6954504894233,235.064816377666,7.16318512433998)) ;
#71862=CARTESIAN_POINT('Ctrl Pts',(70.6507612836455,235.032597310185,7.2786795888421)) ;
#71863=CARTESIAN_POINT('Origin',(79.7621052129773,236.900411902176,7.2786795888419)) ;
#71864=CARTESIAN_POINT('',(79.8802543914407,237.061783435069,7.27867958883751)) ;
#71865=CARTESIAN_POINT('Origin',(79.7621052129773,236.900411902176,7.2786795888419)) ;
#71866=CARTESIAN_POINT('',(79.9151467531554,236.82732064467,7.17267980084143)) ;
#71867=CARTESIAN_POINT('Origin',(79.7621052129773,236.900411902176,7.2786795888419)) ;
#71868=CARTESIAN_POINT('Origin',(79.7621052129753,236.900411902177,7.27867958883791)) ;
#71869=CARTESIAN_POINT('Origin',(72.0287747312354,234.166257616082,7.2786795888419)) ;
#71870=CARTESIAN_POINT('',(72.1901462641291,234.048108437619,7.27867958883748)) ;
#71871=CARTESIAN_POINT('Origin',(72.0287747312355,234.166257616082,7.2786795888419)) ;
#71872=CARTESIAN_POINT('',(71.9556834737297,234.013216075904,7.1726798008414)) ;
#71873=CARTESIAN_POINT('Origin',(72.0287747312354,234.166257616082,7.2786795888419)) ;
#71874=CARTESIAN_POINT('Origin',(72.028774731237,234.166257616084,7.2786795888379)) ;
#71875=CARTESIAN_POINT('Origin',(74.5283628290597,239.4,7.2786795888419)) ;
#71876=CARTESIAN_POINT('Origin',(74.5283628290597,239.4,7.17267980084127)) ;
#71877=CARTESIAN_POINT('Origin',(79.6268886667165,236.635034487932,7.27867958886636)) ;
#71878=CARTESIAN_POINT('',(79.5657826985583,236.444597987609,7.27867958819178)) ;
#71879=CARTESIAN_POINT('Origin',(79.6268886667016,236.635034487937,7.27867958812537)) ;
#71880=CARTESIAN_POINT('',(79.775976296471,236.554183244325,7.17267980084126)) ;
#71881=CARTESIAN_POINT('Origin',(79.6268886667165,236.635034487932,7.27867958886636)) ;
#71882=CARTESIAN_POINT('Origin',(79.6268886667016,236.635034487937,7.2786795888419)) ;
#71883=CARTESIAN_POINT('Origin',(73.474255491572,233.696592446523,7.27867958884206)) ;
#71884=CARTESIAN_POINT('',(73.2742568343815,233.695859560452,7.2786795888379)) ;
#71885=CARTESIAN_POINT('Origin',(73.474255491572,233.696592446523,7.27867958883749)) ;
#71886=CARTESIAN_POINT('',(73.4434320007296,233.529817276441,7.17267980084128)) ;
#71887=CARTESIAN_POINT('Origin',(73.474255491572,233.696592446523,7.27867958884206)) ;
#71888=CARTESIAN_POINT('Origin',(73.474255491572,233.696592446523,7.2786795888419)) ;
#71889=CARTESIAN_POINT('Ctrl Pts',(73.2742568343815,233.69585956045,7.27867958884206)) ;
#71890=CARTESIAN_POINT('Ctrl Pts',(73.2740549596697,233.750949529716,7.16318984200169)) ;
#71891=CARTESIAN_POINT('Ctrl Pts',(73.2587365790027,233.863147817193,6.93380129444964)) ;
#71892=CARTESIAN_POINT('Ctrl Pts',(73.1943130298186,234.006881253322,6.66079578040121)) ;
#71893=CARTESIAN_POINT('Ctrl Pts',(73.1125662143234,234.107132168956,6.49260105919638)) ;
#71894=CARTESIAN_POINT('Ctrl Pts',(73.0506452553059,234.162420516523,6.41145403426995)) ;
#71895=CARTESIAN_POINT('Ctrl Pts',(72.9691982052928,234.221689136819,6.33519282548988)) ;
#71896=CARTESIAN_POINT('Ctrl Pts',(72.8478698697775,234.275176193887,6.30217004615784)) ;
#71897=CARTESIAN_POINT('Ctrl Pts',(72.723618971598,234.293644522184,6.35347099290516)) ;
#71898=CARTESIAN_POINT('Ctrl Pts',(72.6451468245962,234.294029054113,6.41180850518493)) ;
#71899=CARTESIAN_POINT('Ctrl Pts',(72.5625951046027,234.285547981313,6.49328289149882)) ;
#71900=CARTESIAN_POINT('Ctrl Pts',(72.4375721749348,234.252605836027,6.66117410704378)) ;
#71901=CARTESIAN_POINT('Ctrl Pts',(72.3009698631611,234.174128957134,6.93432838635655)) ;
#71902=CARTESIAN_POINT('Ctrl Pts',(72.2226915456342,234.092559715514,7.16318668385647)) ;
#71903=CARTESIAN_POINT('Ctrl Pts',(72.1901462641291,234.048108437619,7.27867958884204)) ;
#71904=CARTESIAN_POINT('Ctrl Pts',(73.2744232698453,233.650440674103,7.24979207607673)) ;
#71905=CARTESIAN_POINT('Ctrl Pts',(73.2784859949353,233.708330636419,7.13558347975436)) ;
#71906=CARTESIAN_POINT('Ctrl Pts',(73.2701535035563,233.827800206243,6.90837543967858)) ;
#71907=CARTESIAN_POINT('Ctrl Pts',(73.2095239949662,233.983720993006,6.63742243131242)) ;
#71908=CARTESIAN_POINT('Ctrl Pts',(73.1263364797546,234.093345744578,6.47033622807258)) ;
#71909=CARTESIAN_POINT('Ctrl Pts',(73.0619522577372,234.153844863798,6.38969679257593)) ;
#71910=CARTESIAN_POINT('Ctrl Pts',(72.9764379699748,234.218648084035,6.31389624857319)) ;
#71911=CARTESIAN_POINT('Ctrl Pts',(72.8472724531709,234.27654322756,6.28106387226434)) ;
#71912=CARTESIAN_POINT('Ctrl Pts',(72.7146084425558,234.294866821401,6.33206532553425)) ;
#71913=CARTESIAN_POINT('Ctrl Pts',(72.6310406400458,234.293688802942,6.39004922954425)) ;
#71914=CARTESIAN_POINT('Ctrl Pts',(72.543443716397,234.282416742709,6.47101436009728)) ;
#71915=CARTESIAN_POINT('Ctrl Pts',(72.4117100575662,234.242768487736,6.63779863647138)) ;
#71916=CARTESIAN_POINT('Ctrl Pts',(72.2710645809142,234.152174672608,6.90889868284266)) ;
#71917=CARTESIAN_POINT('Ctrl Pts',(72.1940559565118,234.060684934228,7.13558035664306)) ;
#71918=CARTESIAN_POINT('Ctrl Pts',(72.1633150634402,234.01146161501,7.24979207607672)) ;
#71919=CARTESIAN_POINT('Ctrl Pts',(73.3149055858816,233.571685641175,7.19960828841392)) ;
#71920=CARTESIAN_POINT('Ctrl Pts',(73.3213023208757,233.637987511948,7.08747716866263)) ;
#71921=CARTESIAN_POINT('Ctrl Pts',(73.3152112594166,233.774618048049,6.86386304009817)) ;
#71922=CARTESIAN_POINT('Ctrl Pts',(73.2500249475578,233.952315913544,6.59637000664605)) ;
#71923=CARTESIAN_POINT('Ctrl Pts',(73.158257430726,234.076786632763,6.43117772982988)) ;
#71924=CARTESIAN_POINT('Ctrl Pts',(73.0868032929897,234.145311645297,6.35141005998548)) ;
#71925=CARTESIAN_POINT('Ctrl Pts',(72.9916981507112,234.218557730749,6.27640397003883)) ;
#71926=CARTESIAN_POINT('Ctrl Pts',(72.8475995469222,234.283579186381,6.24390204216934)) ;
#71927=CARTESIAN_POINT('Ctrl Pts',(72.6992543275143,234.303453400385,6.29438512175569)) ;
#71928=CARTESIAN_POINT('Ctrl Pts',(72.605779290744,234.301415798299,6.35175959624848)) ;
#71929=CARTESIAN_POINT('Ctrl Pts',(72.507738968611,234.287787061284,6.43185018953203)) ;
#71930=CARTESIAN_POINT('Ctrl Pts',(72.3603935603073,234.241172455663,6.59674275110135)) ;
#71931=CARTESIAN_POINT('Ctrl Pts',(72.2031972386972,234.135653153317,6.86438198127782)) ;
#71932=CARTESIAN_POINT('Ctrl Pts',(72.1180702535969,234.028943179651,7.08747410236134)) ;
#71933=CARTESIAN_POINT('Ctrl Pts',(72.0842731348961,233.971542363323,7.1996082884139)) ;
#71934=CARTESIAN_POINT('Ctrl Pts',(73.4035438393931,233.535025116255,7.17608503411332)) ;
#71935=CARTESIAN_POINT('Ctrl Pts',(73.4051321830648,233.607268444389,7.06215973636355)) ;
#71936=CARTESIAN_POINT('Ctrl Pts',(73.3882813088143,233.754794547639,6.83553949296448)) ;
#71937=CARTESIAN_POINT('Ctrl Pts',(73.3062624638023,233.944548706618,6.56530588838826)) ;
#71938=CARTESIAN_POINT('Ctrl Pts',(73.1996503539424,234.077181947362,6.39866484639538)) ;
#71939=CARTESIAN_POINT('Ctrl Pts',(73.1183663427792,234.150381296654,6.31824032527891)) ;
#71940=CARTESIAN_POINT('Ctrl Pts',(73.011160084709,234.228870150154,6.24264180022651)) ;
#71941=CARTESIAN_POINT('Ctrl Pts',(72.8508725252478,234.299674522912,6.20989694476306)) ;
#71942=CARTESIAN_POINT('Ctrl Pts',(72.6867266829953,234.323853007396,6.26076252232513)) ;
#71943=CARTESIAN_POINT('Ctrl Pts',(72.5832167238411,234.324067353368,6.31859191036259)) ;
#71944=CARTESIAN_POINT('Ctrl Pts',(72.4744843130502,234.312428441163,6.39934128183629)) ;
#71945=CARTESIAN_POINT('Ctrl Pts',(72.3103311568753,234.26793932169,6.56568114913269)) ;
#71946=CARTESIAN_POINT('Ctrl Pts',(72.1324342534315,234.162555555409,6.83606168702106)) ;
#71947=CARTESIAN_POINT('Ctrl Pts',(72.0321944574505,234.053364942797,7.06215662099925)) ;
#71948=CARTESIAN_POINT('Ctrl Pts',(71.9910147655643,233.993983633843,7.1760850341133)) ;
#71949=CARTESIAN_POINT('Ctrl Pts',(73.4434320007296,233.52981727644,7.17267980084142)) ;
#71950=CARTESIAN_POINT('Ctrl Pts',(73.4427713648384,233.603342920453,7.05719005400105)) ;
#71951=CARTESIAN_POINT('Ctrl Pts',(73.4209606328348,233.753197403932,6.827801506449)) ;
#71952=CARTESIAN_POINT('Ctrl Pts',(73.3313468227806,233.945597739259,6.55479599240056)) ;
#71953=CARTESIAN_POINT('Ctrl Pts',(73.2181183729435,234.080261564928,6.38660127119577)) ;
#71954=CARTESIAN_POINT('Ctrl Pts',(73.1324946015359,234.154770746277,6.30545424626932)) ;
#71955=CARTESIAN_POINT('Ctrl Pts',(73.0199781972657,234.234864355979,6.22919303748926)) ;
#71956=CARTESIAN_POINT('Ctrl Pts',(72.8527043400124,234.307871726469,6.19617025815722)) ;
#71957=CARTESIAN_POINT('Ctrl Pts',(72.6819787802051,234.334286679362,6.24747120490454)) ;
#71958=CARTESIAN_POINT('Ctrl Pts',(72.5743809047495,234.335919683504,6.30580871718431)) ;
#71959=CARTESIAN_POINT('Ctrl Pts',(72.4613734565605,234.325771256962,6.38728310349819)) ;
#71960=CARTESIAN_POINT('Ctrl Pts',(72.2906661705782,234.283529574643,6.55517431904313)) ;
#71961=CARTESIAN_POINT('Ctrl Pts',(72.1050805550541,234.180466586174,6.82832859835594)) ;
#71962=CARTESIAN_POINT('Ctrl Pts',(71.9994364250301,234.072312875397,7.05718689585584)) ;
#71963=CARTESIAN_POINT('Ctrl Pts',(71.9556834737297,234.013216075904,7.17267980084141)) ;
#71964=CARTESIAN_POINT('Ctrl Pts',(71.9556834737297,234.013216075904,7.17267980084141)) ;
#71965=CARTESIAN_POINT('Ctrl Pts',(71.9775380676966,234.042734920217,7.11499110854748)) ;
#71966=CARTESIAN_POINT('Ctrl Pts',(72.00168629204,234.071039609707,7.0574911746497)) ;
#71967=CARTESIAN_POINT('Ctrl Pts',(72.0283121753549,234.097913331845,7.00044364508764)) ;
#71968=CARTESIAN_POINT('Ctrl Pts',(72.0463388677926,234.116107820189,6.96182039050547)) ;
#71969=CARTESIAN_POINT('Ctrl Pts',(72.0655008578513,234.13364659012,6.92340451249123)) ;
#71970=CARTESIAN_POINT('Ctrl Pts',(72.0858489590221,234.15046595221,6.88527679966823)) ;
#71971=CARTESIAN_POINT('Ctrl Pts',(72.0955555209196,234.158489215797,6.86708891071367)) ;
#71972=CARTESIAN_POINT('Ctrl Pts',(72.1055316863788,234.16634874434,6.84896683649129)) ;
#71973=CARTESIAN_POINT('Ctrl Pts',(72.115786645653,234.174040756174,6.83091231686833)) ;
#71974=CARTESIAN_POINT('Ctrl Pts',(72.1793344697666,234.221706534458,6.71903225895876)) ;
#71975=CARTESIAN_POINT('Ctrl Pts',(72.2535635063277,234.26292178182,6.60978900838434)) ;
#71976=CARTESIAN_POINT('Ctrl Pts',(72.343325143251,234.2927507782,6.50942604602813)) ;
#71977=CARTESIAN_POINT('Ctrl Pts',(72.3809678070854,234.305259940485,6.46733758393119)) ;
#71978=CARTESIAN_POINT('Ctrl Pts',(72.4213378420412,234.315764249845,6.42681718884272)) ;
#71979=CARTESIAN_POINT('Ctrl Pts',(72.4651746871031,234.323195626295,6.3893990922628)) ;
#71980=CARTESIAN_POINT('Ctrl Pts',(72.4736237817096,234.324627946586,6.38218714446975)) ;
#71981=CARTESIAN_POINT('Ctrl Pts',(72.4822016825239,234.325946132109,6.37509039685455)) ;
#71982=CARTESIAN_POINT('Ctrl Pts',(72.4909136875768,234.327142557127,6.36811979451503)) ;
#71983=CARTESIAN_POINT('Ctrl Pts',(72.506400120543,234.329269318501,6.35572887357221)) ;
#71984=CARTESIAN_POINT('Ctrl Pts',(72.5223103024083,234.331011329692,6.34373656253294)) ;
#71985=CARTESIAN_POINT('Ctrl Pts',(72.5386357642041,234.33230514034,6.33226488075079)) ;
#71986=CARTESIAN_POINT('Ctrl Pts',(72.5507341861932,234.333263953474,6.32376348282031)) ;
#71987=CARTESIAN_POINT('Ctrl Pts',(72.5630662071469,234.333977025601,6.31554417524479)) ;
#71988=CARTESIAN_POINT('Ctrl Pts',(72.575626098791,234.33441784388,6.30765908514812)) ;
#71989=CARTESIAN_POINT('Ctrl Pts',(72.6051375771739,234.335453617075,6.28913180222824)) ;
#71990=CARTESIAN_POINT('Ctrl Pts',(72.6359049160563,234.334983592938,6.2724556364998)) ;
#71991=CARTESIAN_POINT('Ctrl Pts',(72.6679687998726,234.332593398481,6.25836820375113)) ;
#71992=CARTESIAN_POINT('Ctrl Pts',(72.680889243656,234.331630247127,6.25269154012778)) ;
#71993=CARTESIAN_POINT('Ctrl Pts',(72.694019862766,234.330355709935,6.24743472601835)) ;
#71994=CARTESIAN_POINT('Ctrl Pts',(72.7072883464412,234.328754661154,6.2426686581949)) ;
#71995=CARTESIAN_POINT('Ctrl Pts',(72.7143126179355,234.327907073623,6.24014552479311)) ;
#71996=CARTESIAN_POINT('Ctrl Pts',(72.7213755301905,234.326967996892,6.23775989279003)) ;
#71997=CARTESIAN_POINT('Ctrl Pts',(72.7284664014194,234.325935319766,6.23552201762156)) ;
#71998=CARTESIAN_POINT('Ctrl Pts',(72.7357423661804,234.324875686593,6.23322572703334)) ;
#71999=CARTESIAN_POINT('Ctrl Pts',(72.7430560512114,234.323716350896,6.23108229789024)) ;
#72000=CARTESIAN_POINT('Ctrl Pts',(72.7504018230615,234.32245331508,6.22910244381318)) ;
#72001=CARTESIAN_POINT('Ctrl Pts',(72.7662299130018,234.319731825098,6.22483641036702)) ;
#72002=CARTESIAN_POINT('Ctrl Pts',(72.7822005848587,234.316529935791,6.22133160592553)) ;
#72003=CARTESIAN_POINT('Ctrl Pts',(72.798211826618,234.312812791759,6.21871235430216)) ;
#72004=CARTESIAN_POINT('Ctrl Pts',(72.8048606278438,234.311269216803,6.21762468829436)) ;
#72005=CARTESIAN_POINT('Ctrl Pts',(72.8115173655257,234.309636512685,6.2166896807269)) ;
#72006=CARTESIAN_POINT('Ctrl Pts',(72.8181709115136,234.307913070068,6.21591686669063)) ;
#72007=CARTESIAN_POINT('Ctrl Pts',(72.837047957555,234.303023420897,6.21372428454407)) ;
#72008=CARTESIAN_POINT('Ctrl Pts',(72.8558939618855,234.297403478447,6.21284016126948)) ;
#72009=CARTESIAN_POINT('Ctrl Pts',(72.8744943463362,234.291170524958,6.21317725828574)) ;
#72010=CARTESIAN_POINT('Ctrl Pts',(72.8915027733682,234.285471033375,6.21348550406523)) ;
#72011=CARTESIAN_POINT('Ctrl Pts',(72.9083106447413,234.27925859489,6.21481277495926)) ;
#72012=CARTESIAN_POINT('Ctrl Pts',(72.9247998340907,234.272613244744,6.21708308597247)) ;
#72013=CARTESIAN_POINT('Ctrl Pts',(72.9442413098504,234.264778086141,6.21975988199892)) ;
#72014=CARTESIAN_POINT('Ctrl Pts',(72.9632457496712,234.256340047346,6.22374636219899)) ;
#72015=CARTESIAN_POINT('Ctrl Pts',(72.9816154090083,234.247380942209,6.2289966565276)) ;
#72016=CARTESIAN_POINT('Ctrl Pts',(72.9880616494754,234.244237032732,6.23083907827009)) ;
#72017=CARTESIAN_POINT('Ctrl Pts',(72.9944292805357,234.241028994714,6.23283728580596)) ;
#72018=CARTESIAN_POINT('Ctrl Pts',(73.0007083082323,234.237760516865,6.2349897519224)) ;
#72019=CARTESIAN_POINT('Ctrl Pts',(73.0194856569107,234.227986177398,6.24142667316875)) ;
#72020=CARTESIAN_POINT('Ctrl Pts',(73.0376043277885,234.217735081624,6.24908212275534)) ;
#72021=CARTESIAN_POINT('Ctrl Pts',(73.0548238897132,234.207125592467,6.25787622350305)) ;
#72022=CARTESIAN_POINT('Ctrl Pts',(73.0756315647307,234.194305359092,6.26850278829196)) ;
#72023=CARTESIAN_POINT('Ctrl Pts',(73.0951264737041,234.180961642225,6.28079280784326)) ;
#72024=CARTESIAN_POINT('Ctrl Pts',(73.1135027160114,234.167300408393,6.29423878512697)) ;
#72025=CARTESIAN_POINT('Ctrl Pts',(73.1192898960236,234.162998113177,6.29847329018414)) ;
#72026=CARTESIAN_POINT('Ctrl Pts',(73.1249658256639,234.158664500401,6.30282225079387)) ;
#72027=CARTESIAN_POINT('Ctrl Pts',(73.1305357448685,234.154306431645,6.30726934661585)) ;
#72028=CARTESIAN_POINT('Ctrl Pts',(73.1399823771323,234.146915108466,6.31481166048607)) ;
#72029=CARTESIAN_POINT('Ctrl Pts',(73.1491242321405,234.139453369777,6.3226363299253)) ;
#72030=CARTESIAN_POINT('Ctrl Pts',(73.1579468348379,234.131936426963,6.33072042621225)) ;
#72031=CARTESIAN_POINT('Ctrl Pts',(73.1708502985423,234.12094255111,6.34254379020126)) ;
#72032=CARTESIAN_POINT('Ctrl Pts',(73.1831308047004,234.109832984206,6.35489353170787)) ;
#72033=CARTESIAN_POINT('Ctrl Pts',(73.1947996145563,234.098652078751,6.36768106647146)) ;
#72034=CARTESIAN_POINT('Ctrl Pts',(73.2322011063735,234.062814444146,6.40866835504048)) ;
#72035=CARTESIAN_POINT('Ctrl Pts',(73.2633187933714,234.026243273988,6.4541543849551)) ;
#72036=CARTESIAN_POINT('Ctrl Pts',(73.2900031699536,233.989653097423,6.5017061491635)) ;
#72037=CARTESIAN_POINT('Ctrl Pts',(73.2913623326756,233.987789385005,6.50412818758281)) ;
#72038=CARTESIAN_POINT('Ctrl Pts',(73.2927099386585,233.985925520695,6.50655576541892)) ;
#72039=CARTESIAN_POINT('Ctrl Pts',(73.2940462311482,233.984061599677,6.50898856002465)) ;
#72040=CARTESIAN_POINT('Ctrl Pts',(73.3245036847171,233.941578170117,6.56443804381528)) ;
#72041=CARTESIAN_POINT('Ctrl Pts',(73.3490786188089,233.899066190412,6.62259797169379)) ;
#72042=CARTESIAN_POINT('Ctrl Pts',(73.3689099777686,233.856725100102,6.68241697443128)) ;
#72043=CARTESIAN_POINT('Ctrl Pts',(73.3849820467182,233.822410309864,6.73089651324879)) ;
#72044=CARTESIAN_POINT('Ctrl Pts',(73.3979401376789,233.788207585212,6.78046537481758)) ;
#72045=CARTESIAN_POINT('Ctrl Pts',(73.4084145403143,233.754217734094,6.83056538013866)) ;
#72046=CARTESIAN_POINT('Ctrl Pts',(73.4110048032138,233.745812228465,6.84295483942932)) ;
#72047=CARTESIAN_POINT('Ctrl Pts',(73.4134432575565,233.737419716346,6.85537680140795)) ;
#72048=CARTESIAN_POINT('Ctrl Pts',(73.415733427501,233.729040807646,6.86782833608266)) ;
#72049=CARTESIAN_POINT('Ctrl Pts',(73.4309142280092,233.673499714833,6.95036555755346)) ;
#72050=CARTESIAN_POINT('Ctrl Pts',(73.4395025790421,233.618495791153,7.03432129089791)) ;
#72051=CARTESIAN_POINT('Ctrl Pts',(73.4423703243965,233.564227299757,7.11885358141502)) ;
#72052=CARTESIAN_POINT('Ctrl Pts',(73.4429782186783,233.552723661349,7.13677243043561)) ;
#72053=CARTESIAN_POINT('Ctrl Pts',(73.4433292491485,233.541253040478,7.1547171768976)) ;
#72054=CARTESIAN_POINT('Ctrl Pts',(73.4434320007295,233.52981727644,7.17267980084087)) ;
#72055=CARTESIAN_POINT('Ctrl Pts',(73.2742568343815,233.69585956045,7.27867958884206)) ;
#72056=CARTESIAN_POINT('Ctrl Pts',(73.2740549596697,233.750949529716,7.16318984200169)) ;
#72057=CARTESIAN_POINT('Ctrl Pts',(73.2587365790027,233.863147817193,6.93380129444964)) ;
#72058=CARTESIAN_POINT('Ctrl Pts',(73.1943130298186,234.006881253322,6.66079578040121)) ;
#72059=CARTESIAN_POINT('Ctrl Pts',(73.1125662143234,234.107132168956,6.49260105919638)) ;
#72060=CARTESIAN_POINT('Ctrl Pts',(73.0506452553059,234.162420516523,6.41145403426995)) ;
#72061=CARTESIAN_POINT('Ctrl Pts',(72.9691982052928,234.221689136819,6.33519282548988)) ;
#72062=CARTESIAN_POINT('Ctrl Pts',(72.8478698697775,234.275176193887,6.30217004615784)) ;
#72063=CARTESIAN_POINT('Ctrl Pts',(72.723618971598,234.293644522184,6.35347099290516)) ;
#72064=CARTESIAN_POINT('Ctrl Pts',(72.6451468245962,234.294029054113,6.41180850518493)) ;
#72065=CARTESIAN_POINT('Ctrl Pts',(72.5625951046027,234.285547981313,6.49328289149882)) ;
#72066=CARTESIAN_POINT('Ctrl Pts',(72.4375721749348,234.252605836027,6.66117410704378)) ;
#72067=CARTESIAN_POINT('Ctrl Pts',(72.3009698631611,234.174128957134,6.93432838635655)) ;
#72068=CARTESIAN_POINT('Ctrl Pts',(72.2226915456342,234.092559715514,7.16318668385647)) ;
#72069=CARTESIAN_POINT('Ctrl Pts',(72.1901462641291,234.048108437619,7.27867958884204)) ;
#72070=CARTESIAN_POINT('Origin',(78.7335324267296,235.405435110699,7.2786795888419)) ;
#72071=CARTESIAN_POINT('',(78.8957655188746,235.522398454586,7.27867958883752)) ;
#72072=CARTESIAN_POINT('Origin',(78.7335324267296,235.405435110699,7.2786795888419)) ;
#72073=CARTESIAN_POINT('',(78.8564971400703,235.288628757204,7.17267980084146)) ;
#72074=CARTESIAN_POINT('Origin',(78.7335324267296,235.405435110699,7.2786795888419)) ;
#72075=CARTESIAN_POINT('Origin',(78.7335324267282,235.405435110702,7.27867958883793)) ;
#72076=CARTESIAN_POINT('Origin',(73.7684286213811,233.65,7.2786795888419)) ;
#72077=CARTESIAN_POINT('',(73.9584121733008,233.5875,7.27867958883753)) ;
#72078=CARTESIAN_POINT('Origin',(73.7684286213811,233.65,7.2786795888419)) ;
#72079=CARTESIAN_POINT('',(73.7462071414064,233.48186240524,7.17267980084138)) ;
#72080=CARTESIAN_POINT('Origin',(73.7684286213811,233.65,7.2786795888419)) ;
#72081=CARTESIAN_POINT('Origin',(73.7684286213819,233.650000000002,7.27867958883792)) ;
#72082=CARTESIAN_POINT('Origin',(74.5283628290597,239.4,7.2786795888419)) ;
#72083=CARTESIAN_POINT('Origin',(74.5283628290597,239.4,7.17267980084128)) ;
#72084=CARTESIAN_POINT('Origin',(78.5229277183728,235.194830402321,7.27867958886636)) ;
#72085=CARTESIAN_POINT('',(78.4059643742222,235.032597310366,7.27867958819179)) ;
#72086=CARTESIAN_POINT('Origin',(78.5229277183602,235.19483040233,7.27867958812537)) ;
#72087=CARTESIAN_POINT('',(78.6397340718589,235.071865688993,7.17267980084126)) ;
#72088=CARTESIAN_POINT('Origin',(78.5229277183728,235.194830402321,7.27867958886636)) ;
#72089=CARTESIAN_POINT('Origin',(78.5229277183602,235.19483040233,7.2786795888419)) ;
#72090=CARTESIAN_POINT('Origin',(75.2882970367382,233.65,7.27867958884202)) ;
#72091=CARTESIAN_POINT('',(75.098313484818,233.587500000002,7.27867958883787)) ;
#72092=CARTESIAN_POINT('Origin',(75.2882970367382,233.65,7.27867958883749)) ;
#72093=CARTESIAN_POINT('',(75.3105185167129,233.48186240524,7.17267980084126)) ;
#72094=CARTESIAN_POINT('Origin',(75.2882970367382,233.65,7.27867958884202)) ;
#72095=CARTESIAN_POINT('Origin',(75.2882970367382,233.65,7.2786795888419)) ;
#72096=CARTESIAN_POINT('Ctrl Pts',(75.0983134848186,233.5875,7.27867958884202)) ;
#72097=CARTESIAN_POINT('Ctrl Pts',(75.0810977099062,233.63983142507,7.16318954730697)) ;
#72098=CARTESIAN_POINT('Ctrl Pts',(75.0318577462829,233.741804969875,6.93380038570087)) ;
#72099=CARTESIAN_POINT('Ctrl Pts',(74.9261707880323,233.858595877082,6.66079423640237)) ;
#72100=CARTESIAN_POINT('Ctrl Pts',(74.8174451204396,233.928679077915,6.49259931810746)) ;
#72101=CARTESIAN_POINT('Ctrl Pts',(74.7414693009496,233.962126737956,6.41145241095834)) ;
#72102=CARTESIAN_POINT('Ctrl Pts',(74.6456929341906,233.99332587631,6.33519154784912)) ;
#72103=CARTESIAN_POINT('Ctrl Pts',(74.5137737498694,234.006702012445,6.30217015984433)) ;
#72104=CARTESIAN_POINT('Ctrl Pts',(74.3898972177444,233.985870163199,6.35347266041592)) ;
#72105=CARTESIAN_POINT('Ctrl Pts',(74.3151471323012,233.961986344105,6.4118109039499)) ;
#72106=CARTESIAN_POINT('Ctrl Pts',(74.2392567867269,233.928410119706,6.4932861327103)) ;
#72107=CARTESIAN_POINT('Ctrl Pts',(74.1305331522724,233.858445916787,6.66117766958715)) ;
#72108=CARTESIAN_POINT('Ctrl Pts',(74.0248674005834,233.741596368342,6.93433448515046)) ;
#72109=CARTESIAN_POINT('Ctrl Pts',(73.9756279482132,233.63983142507,7.16318954730701)) ;
#72110=CARTESIAN_POINT('Ctrl Pts',(73.9584121733007,233.5875,7.27867958884203)) ;
#72111=CARTESIAN_POINT('Ctrl Pts',(75.1125069820977,233.544355503564,7.24979207607669)) ;
#72112=CARTESIAN_POINT('Ctrl Pts',(75.0984818453212,233.600667724241,7.13558318832874)) ;
#72113=CARTESIAN_POINT('Ctrl Pts',(75.0536389656137,233.711715621496,6.90837460070416)) ;
#72114=CARTESIAN_POINT('Ctrl Pts',(74.9477942437258,233.841269933359,6.63742098993475)) ;
#72115=CARTESIAN_POINT('Ctrl Pts',(74.8348016731915,233.919823032627,6.4703346030079)) ;
#72116=CARTESIAN_POINT('Ctrl Pts',(74.7548728956437,233.957465240244,6.38969528531651)) ;
#72117=CARTESIAN_POINT('Ctrl Pts',(74.6535180161129,233.992671246009,6.31389508883174)) ;
#72118=CARTESIAN_POINT('Ctrl Pts',(74.5127829922739,234.007817842091,6.28106410226516)) ;
#72119=CARTESIAN_POINT('Ctrl Pts',(74.3809498631099,233.984248460513,6.33206709849415)) ;
#72120=CARTESIAN_POINT('Ctrl Pts',(74.3018363988415,233.957303882483,6.39005172782796)) ;
#72121=CARTESIAN_POINT('Ctrl Pts',(74.2220102801505,233.919514179975,6.47101769533025)) ;
#72122=CARTESIAN_POINT('Ctrl Pts',(74.1089767078142,233.841098288102,6.63780226952725)) ;
#72123=CARTESIAN_POINT('Ctrl Pts',(74.0032101259291,233.711475333851,6.90890481997371)) ;
#72124=CARTESIAN_POINT('Ctrl Pts',(73.9582438127981,233.600667724241,7.13558318832878)) ;
#72125=CARTESIAN_POINT('Ctrl Pts',(73.9442186760216,233.544355503564,7.24979207607671)) ;
#72126=CARTESIAN_POINT('Ctrl Pts',(75.1753446132139,233.481964767775,7.19960830183853)) ;
#72127=CARTESIAN_POINT('Ctrl Pts',(75.1609398281288,233.546998459783,7.08747689596276)) ;
#72128=CARTESIAN_POINT('Ctrl Pts',(75.1129255576136,233.675059882258,6.86386215376673)) ;
#72129=CARTESIAN_POINT('Ctrl Pts',(74.9960174923802,233.823917230629,6.59636848724759)) ;
#72130=CARTESIAN_POINT('Ctrl Pts',(74.8702771117857,233.913938281557,6.43117601138465)) ;
#72131=CARTESIAN_POINT('Ctrl Pts',(74.7811442493929,233.957028829249,6.35140845594426)) ;
#72132=CARTESIAN_POINT('Ctrl Pts',(74.668058857727,233.997300700229,6.27640270416242)) ;
#72133=CARTESIAN_POINT('Ctrl Pts',(74.5109193901771,234.014610130897,6.24390214489264)) ;
#72134=CARTESIAN_POINT('Ctrl Pts',(74.3636933974101,233.987669619988,6.29438675335505)) ;
#72135=CARTESIAN_POINT('Ctrl Pts',(74.2754232494263,233.956845980595,6.35176194667064)) ;
#72136=CARTESIAN_POINT('Ctrl Pts',(74.1863931543353,233.913587695583,6.43185336540903)) ;
#72137=CARTESIAN_POINT('Ctrl Pts',(74.0606647370925,233.823722161856,6.59674624426879)) ;
#72138=CARTESIAN_POINT('Ctrl Pts',(73.9437696527188,233.674789559215,6.86438794160944)) ;
#72139=CARTESIAN_POINT('Ctrl Pts',(73.8957858299905,233.546998459783,7.0874768959628)) ;
#72140=CARTESIAN_POINT('Ctrl Pts',(73.8813810449054,233.481964767775,7.19960830183855)) ;
#72141=CARTESIAN_POINT('Ctrl Pts',(75.2709733099442,233.474489235504,7.17608503411327)) ;
#72142=CARTESIAN_POINT('Ctrl Pts',(75.2501594453092,233.543687725245,7.06215944566083)) ;
#72143=CARTESIAN_POINT('Ctrl Pts',(75.1885450487657,233.678786595009,6.83553863585668)) ;
#72144=CARTESIAN_POINT('Ctrl Pts',(75.0519026388913,233.833908676329,6.56530442100143)) ;
#72145=CARTESIAN_POINT('Ctrl Pts',(74.9095217874548,233.927105534872,6.39866319155849)) ;
#72146=CARTESIAN_POINT('Ctrl Pts',(74.8095956592821,233.971604040945,6.31823878756062)) ;
#72147=CARTESIAN_POINT('Ctrl Pts',(74.6833812504254,234.013122629692,6.24264060772189)) ;
#72148=CARTESIAN_POINT('Ctrl Pts',(74.5090580770188,234.030929268947,6.20989713631634)) ;
#72149=CARTESIAN_POINT('Ctrl Pts',(74.3454747092792,234.003199674091,6.26076425322068)) ;
#72150=CARTESIAN_POINT('Ctrl Pts',(74.2469649068908,233.971416787748,6.31859436504268)) ;
#72151=CARTESIAN_POINT('Ctrl Pts',(74.147151148607,233.926746883521,6.39934457097928)) ;
#72152=CARTESIAN_POINT('Ctrl Pts',(74.0047808590601,233.833708884127,6.56568474185533)) ;
#72153=CARTESIAN_POINT('Ctrl Pts',(73.8681563771895,233.678508252996,6.83606777892758)) ;
#72154=CARTESIAN_POINT('Ctrl Pts',(73.8065662128101,233.543687725245,7.06215944566088)) ;
#72155=CARTESIAN_POINT('Ctrl Pts',(73.7857523481751,233.474489235504,7.1760850341133)) ;
#72156=CARTESIAN_POINT('Ctrl Pts',(75.3105185167129,233.48186240524,7.17267980084138)) ;
#72157=CARTESIAN_POINT('Ctrl Pts',(75.2871694815419,233.551585478288,7.05718975930633)) ;
#72158=CARTESIAN_POINT('Ctrl Pts',(75.2201184690921,233.687366037109,6.82780059770023)) ;
#72159=CARTESIAN_POINT('Ctrl Pts',(75.0754350826972,233.842657781476,6.55479444840173)) ;
#72160=CARTESIAN_POINT('Ctrl Pts',(74.9261342046016,233.935741266691,6.38659953010682)) ;
#72161=CARTESIAN_POINT('Ctrl Pts',(74.821675936371,233.980144435879,6.3054526229577)) ;
#72162=CARTESIAN_POINT('Ctrl Pts',(74.6899153511409,234.021548309364,6.22919175984848)) ;
#72163=CARTESIAN_POINT('Ctrl Pts',(74.5082670156342,234.039291236966,6.1961703718437)) ;
#72164=CARTESIAN_POINT('Ctrl Pts',(74.3377348599184,234.011655409264,6.24747287241529)) ;
#72165=CARTESIAN_POINT('Ctrl Pts',(74.2348988344899,233.979958513117,6.30581111594926)) ;
#72166=CARTESIAN_POINT('Ctrl Pts',(74.1305586930738,233.935385084639,6.38728634470966)) ;
#72167=CARTESIAN_POINT('Ctrl Pts',(73.9812605807285,233.842459203332,6.55517788158652)) ;
#72168=CARTESIAN_POINT('Ctrl Pts',(73.8366065041384,233.687089813394,6.82833469714983)) ;
#72169=CARTESIAN_POINT('Ctrl Pts',(73.7695561765774,233.551585478287,7.05718975930638)) ;
#72170=CARTESIAN_POINT('Ctrl Pts',(73.7462071414064,233.48186240524,7.1726798008414)) ;
#72171=CARTESIAN_POINT('Ctrl Pts',(73.7462071414064,233.48186240524,7.17267980084137)) ;
#72172=CARTESIAN_POINT('Ctrl Pts',(73.7695561765774,233.551585478287,7.05718975930636)) ;
#72173=CARTESIAN_POINT('Ctrl Pts',(73.8366065041384,233.687089813395,6.82833469714981)) ;
#72174=CARTESIAN_POINT('Ctrl Pts',(73.9812605807285,233.842459203331,6.55517788158652)) ;
#72175=CARTESIAN_POINT('Ctrl Pts',(74.1305586930738,233.935385084639,6.38728634470966)) ;
#72176=CARTESIAN_POINT('Ctrl Pts',(74.2348988344899,233.979958513118,6.30581111594926)) ;
#72177=CARTESIAN_POINT('Ctrl Pts',(74.3377348599184,234.011655409263,6.24747287241529)) ;
#72178=CARTESIAN_POINT('Ctrl Pts',(74.5082670156342,234.039291236967,6.1961703718437)) ;
#72179=CARTESIAN_POINT('Ctrl Pts',(74.689915351141,234.021548309363,6.22919175984849)) ;
#72180=CARTESIAN_POINT('Ctrl Pts',(74.821675936371,233.98014443588,6.3054526229577)) ;
#72181=CARTESIAN_POINT('Ctrl Pts',(74.9261342046016,233.93574126669,6.38659953010682)) ;
#72182=CARTESIAN_POINT('Ctrl Pts',(75.0754350826972,233.842657781477,6.55479444840175)) ;
#72183=CARTESIAN_POINT('Ctrl Pts',(75.220118469092,233.687366037109,6.82780059770018)) ;
#72184=CARTESIAN_POINT('Ctrl Pts',(75.2871694815419,233.551585478288,7.05718975930624)) ;
#72185=CARTESIAN_POINT('Ctrl Pts',(75.3105185167129,233.48186240524,7.17267980084124)) ;
#72186=CARTESIAN_POINT('Ctrl Pts',(75.0983134848186,233.5875,7.27867958884202)) ;
#72187=CARTESIAN_POINT('Ctrl Pts',(75.0810977099062,233.63983142507,7.16318954730697)) ;
#72188=CARTESIAN_POINT('Ctrl Pts',(75.0318577462829,233.741804969875,6.93380038570087)) ;
#72189=CARTESIAN_POINT('Ctrl Pts',(74.9261707880323,233.858595877082,6.66079423640237)) ;
#72190=CARTESIAN_POINT('Ctrl Pts',(74.8174451204396,233.928679077915,6.49259931810746)) ;
#72191=CARTESIAN_POINT('Ctrl Pts',(74.7414693009496,233.962126737956,6.41145241095834)) ;
#72192=CARTESIAN_POINT('Ctrl Pts',(74.6456929341906,233.99332587631,6.33519154784912)) ;
#72193=CARTESIAN_POINT('Ctrl Pts',(74.5137737498694,234.006702012445,6.30217015984433)) ;
#72194=CARTESIAN_POINT('Ctrl Pts',(74.3898972177444,233.985870163199,6.35347266041592)) ;
#72195=CARTESIAN_POINT('Ctrl Pts',(74.3151471323012,233.961986344105,6.4118109039499)) ;
#72196=CARTESIAN_POINT('Ctrl Pts',(74.2392567867269,233.928410119706,6.4932861327103)) ;
#72197=CARTESIAN_POINT('Ctrl Pts',(74.1305331522724,233.858445916787,6.66117766958715)) ;
#72198=CARTESIAN_POINT('Ctrl Pts',(74.0248674005834,233.741596368342,6.93433448515046)) ;
#72199=CARTESIAN_POINT('Ctrl Pts',(73.9756279482132,233.63983142507,7.16318954730701)) ;
#72200=CARTESIAN_POINT('Ctrl Pts',(73.9584121733007,233.5875,7.27867958884203)) ;
#72201=CARTESIAN_POINT('Origin',(77.2933283411226,234.301474162358,7.2786795888419)) ;
#72202=CARTESIAN_POINT('',(77.4837648415456,234.362580130206,7.27867958883759)) ;
#72203=CARTESIAN_POINT('Origin',(77.2933283411226,234.301474162358,7.2786795888419)) ;
#72204=CARTESIAN_POINT('',(77.3741795847386,234.152386532591,7.17267980084137)) ;
#72205=CARTESIAN_POINT('Origin',(77.2933283411226,234.301474162358,7.2786795888419)) ;
#72206=CARTESIAN_POINT('Origin',(77.2933283411219,234.30147416236,7.27867958883799)) ;
#72207=CARTESIAN_POINT('Origin',(75.5824701665474,233.696592446523,7.2786795888419)) ;
#72208=CARTESIAN_POINT('',(75.7824688237379,233.69585956045,7.27867958883755)) ;
#72209=CARTESIAN_POINT('Origin',(75.5824701665474,233.696592446523,7.2786795888419)) ;
#72210=CARTESIAN_POINT('',(75.6132936573898,233.529817276441,7.17267980084132)) ;
#72211=CARTESIAN_POINT('Origin',(75.5824701665474,233.696592446523,7.2786795888419)) ;
#72212=CARTESIAN_POINT('Origin',(75.5824701665474,233.696592446526,7.27867958883797)) ;
#72213=CARTESIAN_POINT('Origin',(74.5283628290597,239.4,7.2786795888419)) ;
#72214=CARTESIAN_POINT('Origin',(74.5283628290597,239.4,7.17267980084126)) ;
#72215=CARTESIAN_POINT('Origin',(77.027950926884,234.166257616082,7.27867958884205)) ;
#72216=CARTESIAN_POINT('',(76.8665793939892,234.04810843762,7.278679588838)) ;
#72217=CARTESIAN_POINT('Origin',(77.0279509268839,234.166257616082,7.27867958883759)) ;
#72218=CARTESIAN_POINT('',(77.1010421843897,234.013216075904,7.17267980084126)) ;
#72219=CARTESIAN_POINT('Origin',(77.027950926884,234.166257616082,7.27867958884205)) ;
#72220=CARTESIAN_POINT('Origin',(77.0279509268839,234.166257616082,7.2786795888419)) ;
#72221=CARTESIAN_POINT('Ctrl Pts',(76.8665793939903,234.048108437619,7.27867958884205)) ;
#72222=CARTESIAN_POINT('Ctrl Pts',(76.8340341124953,234.0925597155,7.16318668389241)) ;
#72223=CARTESIAN_POINT('Ctrl Pts',(76.7556911392885,234.174326892791,6.93379514728806)) ;
#72224=CARTESIAN_POINT('Ctrl Pts',(76.6190866745073,234.252741595594,6.66079114111062)) ;
#72225=CARTESIAN_POINT('Ctrl Pts',(76.4940251112423,234.285796227647,6.49259672460371)) ;
#72226=CARTESIAN_POINT('Ctrl Pts',(76.4114318303287,234.2941286283,6.41145063262659)) ;
#72227=CARTESIAN_POINT('Ctrl Pts',(76.3107018814125,234.294203813326,6.33519065213031)) ;
#72228=CARTESIAN_POINT('Ctrl Pts',(76.1811060983148,234.266159399846,6.30217089588981)) ;
#72229=CARTESIAN_POINT('Ctrl Pts',(76.0697307124536,234.208067009127,6.35347440234159)) ;
#72230=CARTESIAN_POINT('Ctrl Pts',(76.0060201171914,234.162253139921,6.4118128891193)) ;
#72231=CARTESIAN_POINT('Ctrl Pts',(75.9442201811444,234.106868936771,6.4932882288145)) ;
#72232=CARTESIAN_POINT('Ctrl Pts',(75.8624384710468,234.006731853917,6.66117946366231)) ;
#72233=CARTESIAN_POINT('Ctrl Pts',(75.7980532024828,233.862949209186,6.93433560993259)) ;
#72234=CARTESIAN_POINT('Ctrl Pts',(75.7826706984499,233.750949529794,7.16318984183889)) ;
#72235=CARTESIAN_POINT('Ctrl Pts',(75.7824688237379,233.69585956045,7.27867958884195)) ;
#72236=CARTESIAN_POINT('Ctrl Pts',(76.8934105946792,234.01146161501,7.24979207607672)) ;
#72237=CARTESIAN_POINT('Ctrl Pts',(76.8626697016171,234.060684934213,7.1355803566786)) ;
#72238=CARTESIAN_POINT('Ctrl Pts',(76.7857043976302,234.152441111515,6.90836936466691)) ;
#72239=CARTESIAN_POINT('Ctrl Pts',(76.6450057114788,234.242945622551,6.63741785480387)) ;
#72240=CARTESIAN_POINT('Ctrl Pts',(76.5132686922221,234.282736999639,6.47033195643384)) ;
#72241=CARTESIAN_POINT('Ctrl Pts',(76.4256197164491,234.29383707081,6.38969344711358)) ;
#72242=CARTESIAN_POINT('Ctrl Pts',(76.3183460791628,234.295999096524,6.31389412481953)) ;
#72243=CARTESIAN_POINT('Ctrl Pts',(76.1798188650716,234.266914151536,6.28106475682608)) ;
#72244=CARTESIAN_POINT('Ctrl Pts',(76.0617223233092,234.203759460484,6.33206875395753)) ;
#72245=CARTESIAN_POINT('Ctrl Pts',(75.9948077770194,234.153686282076,6.39005362566642)) ;
#72246=CARTESIAN_POINT('Ctrl Pts',(75.9305667724029,234.093078609259,6.47101970243042)) ;
#72247=CARTESIAN_POINT('Ctrl Pts',(75.8472978214838,233.983571719713,6.63780398898495)) ;
#72248=CARTESIAN_POINT('Ctrl Pts',(75.7867638696866,233.827609742269,6.90890587698616)) ;
#72249=CARTESIAN_POINT('Ctrl Pts',(75.7782396631783,233.708330636501,7.13558347959336)) ;
#72250=CARTESIAN_POINT('Ctrl Pts',(75.782302388274,233.650440674103,7.24979207607662)) ;
#72251=CARTESIAN_POINT('Ctrl Pts',(76.9724525410908,233.971542437522,7.19960831977766)) ;
#72252=CARTESIAN_POINT('Ctrl Pts',(76.9386554224005,234.028943253832,7.08747413375999)) ;
#72253=CARTESIAN_POINT('Ctrl Pts',(76.8534162817674,234.135900487607,6.86385705380188)) ;
#72254=CARTESIAN_POINT('Ctrl Pts',(76.6962307517854,234.241344408245,6.59636547374966)) ;
#72255=CARTESIAN_POINT('Ctrl Pts',(76.54882599141,234.288103136327,6.43117348883828)) ;
#72256=CARTESIAN_POINT('Ctrl Pts',(76.4507397668635,234.301540606073,6.35140673253532)) ;
#72257=CARTESIAN_POINT('Ctrl Pts',(76.3307442874739,234.30489556795,6.27640184858989)) ;
#72258=CARTESIAN_POINT('Ctrl Pts',(76.1759471961323,234.272798261829,6.24390289678572)) ;
#72259=CARTESIAN_POINT('Ctrl Pts',(76.0442530152415,234.201680740727,6.29438849455214)) ;
#72260=CARTESIAN_POINT('Ctrl Pts',(75.9698286986536,234.145088782522,6.35176392641701)) ;
#72261=CARTESIAN_POINT('Ctrl Pts',(75.8985241358216,234.076436004797,6.43185545307777)) ;
#72262=CARTESIAN_POINT('Ctrl Pts',(75.8067198650261,233.952116925724,6.59674803075384)) ;
#72263=CARTESIAN_POINT('Ctrl Pts',(75.7415691250071,233.774351527382,6.86438906719111)) ;
#72264=CARTESIAN_POINT('Ctrl Pts',(75.7354232791666,233.637987561567,7.08747719986831)) ;
#72265=CARTESIAN_POINT('Ctrl Pts',(75.7418200141697,233.5716856907,7.19960831977756)) ;
#72266=CARTESIAN_POINT('Ctrl Pts',(77.0657108925551,233.993983633843,7.17608503411331)) ;
#72267=CARTESIAN_POINT('Ctrl Pts',(77.0245312006817,234.053364942779,7.0621566210347)) ;
#72268=CARTESIAN_POINT('Ctrl Pts',(76.9241827243705,234.16281243188,6.83553342683033)) ;
#72269=CARTESIAN_POINT('Ctrl Pts',(76.746292915967,234.2681161407,6.56530131356024)) ;
#72270=CARTESIAN_POINT('Ctrl Pts',(76.582080718942,234.312753012577,6.39866057413136)) ;
#72271=CARTESIAN_POINT('Ctrl Pts',(76.473294405035,234.32419420694,6.31823697659248)) ;
#72272=CARTESIAN_POINT('Ctrl Pts',(76.3404272191003,234.32467775301,6.24263966949842)) ;
#72273=CARTESIAN_POINT('Ctrl Pts',(76.1691338319105,234.287743240048,6.20989781362796)) ;
#72274=CARTESIAN_POINT('Ctrl Pts',(76.0221267858857,234.21082056027,6.26076592844773)) ;
#72275=CARTESIAN_POINT('Ctrl Pts',(75.9382604527896,234.150152089044,6.31859628173874)) ;
#72276=CARTESIAN_POINT('Ctrl Pts',(75.8571362822314,234.076824457925,6.39934659681402)) ;
#72277=CARTESIAN_POINT('Ctrl Pts',(75.7504850514437,233.944345605192,6.56568647657609)) ;
#72278=CARTESIAN_POINT('Ctrl Pts',(75.6685075209583,233.754522270794,6.83606885194659)) ;
#72279=CARTESIAN_POINT('Ctrl Pts',(75.6515934750524,233.607268444491,7.06215973620294)) ;
#72280=CARTESIAN_POINT('Ctrl Pts',(75.6531818187263,233.535025116255,7.1760850341132)) ;
#72281=CARTESIAN_POINT('Ctrl Pts',(77.1010421843897,234.013216075904,7.17267980084142)) ;
#72282=CARTESIAN_POINT('Ctrl Pts',(77.0572892331029,234.072312875378,7.05718689589178)) ;
#72283=CARTESIAN_POINT('Ctrl Pts',(76.9515594887745,234.180728684329,6.82779535928743)) ;
#72284=CARTESIAN_POINT('Ctrl Pts',(76.765969850139,234.283708967173,6.55479135310999)) ;
#72285=CARTESIAN_POINT('Ctrl Pts',(76.5952113296033,234.326099607554,6.38659693660311)) ;
#72286=CARTESIAN_POINT('Ctrl Pts',(76.4821441508519,234.336049621713,6.30545084462598)) ;
#72287=CARTESIAN_POINT('Ctrl Pts',(76.3440376762746,234.334710204215,6.22919086412971)) ;
#72288=CARTESIAN_POINT('Ctrl Pts',(76.1657973375852,234.295451506702,6.19617110788921)) ;
#72289=CARTESIAN_POINT('Ctrl Pts',(76.012152659647,234.216470723001,6.247474614341)) ;
#72290=CARTESIAN_POINT('Ctrl Pts',(75.9241452928115,234.154547163083,6.3058131011187)) ;
#72291=CARTESIAN_POINT('Ctrl Pts',(75.8386864850542,234.079912563388,6.38728844081392)) ;
#72292=CARTESIAN_POINT('Ctrl Pts',(75.7254118872703,233.945399523016,6.55517967566167)) ;
#72293=CARTESIAN_POINT('Ctrl Pts',(75.6358499337627,233.752934411719,6.82833582193194)) ;
#72294=CARTESIAN_POINT('Ctrl Pts',(75.6139542932819,233.603342920557,7.05719005383824)) ;
#72295=CARTESIAN_POINT('Ctrl Pts',(75.6132936573898,233.529817276441,7.17267980084131)) ;
#72296=CARTESIAN_POINT('Ctrl Pts',(75.6132936573898,233.529817276441,7.17267980084131)) ;
#72297=CARTESIAN_POINT('Ctrl Pts',(75.6136811483567,233.572943184788,7.10494016653924)) ;
#72298=CARTESIAN_POINT('Ctrl Pts',(75.6176122445359,233.616573569928,7.03746115712619)) ;
#72299=CARTESIAN_POINT('Ctrl Pts',(75.6255308442543,233.660599858183,6.97066813692428)) ;
#72300=CARTESIAN_POINT('Ctrl Pts',(75.6289443535501,233.679578484399,6.94187534483236)) ;
#72301=CARTESIAN_POINT('Ctrl Pts',(75.6330982419626,233.698630602532,6.91320997325321)) ;
#72302=CARTESIAN_POINT('Ctrl Pts',(75.6380250264329,233.717747190309,6.88470563298376)) ;
#72303=CARTESIAN_POINT('Ctrl Pts',(75.6411351900574,233.729815044361,6.86671151069543)) ;
#72304=CARTESIAN_POINT('Ctrl Pts',(75.6445532067144,233.741908437271,6.84878174976668)) ;
#72305=CARTESIAN_POINT('Ctrl Pts',(75.648288414344,233.754029561188,6.83091815065467)) ;
#72306=CARTESIAN_POINT('Ctrl Pts',(75.6716820890904,233.829944385364,6.7190380976912)) ;
#72307=CARTESIAN_POINT('Ctrl Pts',(75.7075083786311,233.906918899165,6.6097947220493)) ;
#72308=CARTESIAN_POINT('Ctrl Pts',(75.762593318097,233.983811578595,6.50943151975669)) ;
#72309=CARTESIAN_POINT('Ctrl Pts',(75.7856514095903,234.015998206277,6.46742032897639)) ;
#72310=CARTESIAN_POINT('Ctrl Pts',(75.8120819738222,234.048166034233,6.42697146264465)) ;
#72311=CARTESIAN_POINT('Ctrl Pts',(75.8431042190517,234.079888023935,6.38961057401096)) ;
#72312=CARTESIAN_POINT('Ctrl Pts',(75.8491515604238,234.086071770446,6.3823276051007)) ;
#72313=CARTESIAN_POINT('Ctrl Pts',(75.8553733890211,234.092238603552,6.37516193216405)) ;
#72314=CARTESIAN_POINT('Ctrl Pts',(75.8617787258407,234.098385380411,6.36812481495593)) ;
#72315=CARTESIAN_POINT('Ctrl Pts',(75.8814155988188,234.117229584832,6.34655108969537)) ;
#72316=CARTESIAN_POINT('Ctrl Pts',(75.9027719322721,234.135881745757,6.32618883113316)) ;
#72317=CARTESIAN_POINT('Ctrl Pts',(75.9260354228183,234.154064060967,6.30766344904101)) ;
#72318=CARTESIAN_POINT('Ctrl Pts',(75.9493016230525,234.172248494018,6.28913590914689)) ;
#72319=CARTESIAN_POINT('Ctrl Pts',(75.974468907875,234.18995289281,6.27245946560264)) ;
#72320=CARTESIAN_POINT('Ctrl Pts',(76.0018137681245,234.206865984575,6.25837165899619)) ;
#72321=CARTESIAN_POINT('Ctrl Pts',(76.0128320016159,234.213680881139,6.25269517203829)) ;
#72322=CARTESIAN_POINT('Ctrl Pts',(76.0242032579975,234.22036742268,6.24743847065808)) ;
#72323=CARTESIAN_POINT('Ctrl Pts',(76.0358779409522,234.226870878186,6.24267244279208)) ;
#72324=CARTESIAN_POINT('Ctrl Pts',(76.0420504804806,234.23030933012,6.24015258889024)) ;
#72325=CARTESIAN_POINT('Ctrl Pts',(76.0483078300303,234.233696619766,6.23776986110493)) ;
#72326=CARTESIAN_POINT('Ctrl Pts',(76.0546426194486,234.237024792671,6.23553447411149)) ;
#72327=CARTESIAN_POINT('Ctrl Pts',(76.0656791909796,234.242823188782,6.23163994710773)) ;
#72328=CARTESIAN_POINT('Ctrl Pts',(76.0769749732387,234.248455064872,6.22818372039071)) ;
#72329=CARTESIAN_POINT('Ctrl Pts',(76.0885070092412,234.253881919748,6.22522266061593)) ;
#72330=CARTESIAN_POINT('Ctrl Pts',(76.1023829873427,234.260411809128,6.22165975111902)) ;
#72331=CARTESIAN_POINT('Ctrl Pts',(76.116598572473,234.266643535812,6.21881469107473)) ;
#72332=CARTESIAN_POINT('Ctrl Pts',(76.1310985238889,234.272500575675,6.21679454309188)) ;
#72333=CARTESIAN_POINT('Ctrl Pts',(76.1333376264178,234.273405027862,6.21648258904959)) ;
#72334=CARTESIAN_POINT('Ctrl Pts',(76.1355833747657,234.274300487348,6.21619033071521)) ;
#72335=CARTESIAN_POINT('Ctrl Pts',(76.1378354138322,234.275186615266,6.21591817623244)) ;
#72336=CARTESIAN_POINT('Ctrl Pts',(76.1559817557798,234.282326802329,6.21372522657167)) ;
#72337=CARTESIAN_POINT('Ctrl Pts',(76.1745322866635,234.288857900258,6.21284080371351)) ;
#72338=CARTESIAN_POINT('Ctrl Pts',(76.1932444556825,234.294748660884,6.21317766952897)) ;
#72339=CARTESIAN_POINT('Ctrl Pts',(76.2103563728474,234.300135647704,6.21348572681106)) ;
#72340=CARTESIAN_POINT('Ctrl Pts',(76.2276075834206,234.304989663888,6.2148130177342)) ;
#72341=CARTESIAN_POINT('Ctrl Pts',(76.2448554373945,234.309306022186,6.21708354113517)) ;
#72342=CARTESIAN_POINT('Ctrl Pts',(76.2651911446345,234.314395130595,6.21976055238733)) ;
#72343=CARTESIAN_POINT('Ctrl Pts',(76.2855276520082,234.318739484644,6.22374748057868)) ;
#72344=CARTESIAN_POINT('Ctrl Pts',(76.3056568399921,234.32228904216,6.22899842713304)) ;
#72345=CARTESIAN_POINT('Ctrl Pts',(76.3127180447779,234.323534206771,6.23084042935237)) ;
#72346=CARTESIAN_POINT('Ctrl Pts',(76.3197533595581,234.324681337781,6.23283813295313)) ;
#72347=CARTESIAN_POINT('Ctrl Pts',(76.3267525396858,234.32572754817,6.23499001125318)) ;
#72348=CARTESIAN_POINT('Ctrl Pts',(76.3476867356452,234.328856710857,6.24142617108782)) ;
#72349=CARTESIAN_POINT('Ctrl Pts',(76.3683683305024,234.331213157323,6.2490806240269)) ;
#72350=CARTESIAN_POINT('Ctrl Pts',(76.3885333174352,234.332751329204,6.2578735309604)) ;
#72351=CARTESIAN_POINT('Ctrl Pts',(76.4129027393853,234.334610212611,6.2684997743566)) ;
#72352=CARTESIAN_POINT('Ctrl Pts',(76.436517835923,234.335273938245,6.28078953588881)) ;
#72353=CARTESIAN_POINT('Ctrl Pts',(76.4594145442388,234.335023230649,6.29423529210409)) ;
#72354=CARTESIAN_POINT('Ctrl Pts',(76.4666253803013,234.334944275571,6.29846974984659)) ;
#72355=CARTESIAN_POINT('Ctrl Pts',(76.4737646201994,234.334774589698,6.3028186680162)) ;
#72356=CARTESIAN_POINT('Ctrl Pts',(76.4808324691104,234.334522804414,6.30726572519078)) ;
#72357=CARTESIAN_POINT('Ctrl Pts',(76.4928214739417,234.334095707707,6.3148091504426)) ;
#72358=CARTESIAN_POINT('Ctrl Pts',(76.5046052294152,234.333432418532,6.32263503033504)) ;
#72359=CARTESIAN_POINT('Ctrl Pts',(76.5161630752768,234.332536734824,6.33072042872202)) ;
#72360=CARTESIAN_POINT('Ctrl Pts',(76.533062389186,234.331227110148,6.34254250067724)) ;
#72361=CARTESIAN_POINT('Ctrl Pts',(76.5495258068277,234.3294578278,6.35489082553211)) ;
#72362=CARTESIAN_POINT('Ctrl Pts',(76.5655363846225,234.327271369833,6.36767686175465)) ;
#72363=CARTESIAN_POINT('Ctrl Pts',(76.6168616972201,234.320262213757,6.40866522047711)) ;
#72364=CARTESIAN_POINT('Ctrl Pts',(76.6635341884214,234.308965735347,6.45415276711694)) ;
#72365=CARTESIAN_POINT('Ctrl Pts',(76.706630938113,234.295047867349,6.501706150284)) ;
#72366=CARTESIAN_POINT('Ctrl Pts',(76.7088245661434,234.294339446747,6.5041266213173)) ;
#72367=CARTESIAN_POINT('Ctrl Pts',(76.7110089459639,234.293624119443,6.50655262448272)) ;
#72368=CARTESIAN_POINT('Ctrl Pts',(76.7131842181064,234.292902105009,6.50898383770951)) ;
#72369=CARTESIAN_POINT('Ctrl Pts',(76.7627696395436,234.276443755138,6.56440344709885)) ;
#72370=CARTESIAN_POINT('Ctrl Pts',(76.8076178592959,234.25650836791,6.62253062439344)) ;
#72371=CARTESIAN_POINT('Ctrl Pts',(76.8485317332352,234.233925379128,6.68231570506646)) ;
#72372=CARTESIAN_POINT('Ctrl Pts',(76.8817296004144,234.215601348918,6.73082583076176)) ;
#72373=CARTESIAN_POINT('Ctrl Pts',(76.91233859002,234.195535005202,6.78042711783452)) ;
#72374=CARTESIAN_POINT('Ctrl Pts',(76.9408102796966,234.174179291345,6.83056026478223)) ;
#72375=CARTESIAN_POINT('Ctrl Pts',(76.9478474826703,234.168900907984,6.84295142016449)) ;
#72376=CARTESIAN_POINT('Ctrl Pts',(76.9547541967589,234.163543783773,6.85537508796248)) ;
#72377=CARTESIAN_POINT('Ctrl Pts',(76.9615329145985,234.15811048499,6.86782833575028)) ;
#72378=CARTESIAN_POINT('Ctrl Pts',(77.0061519430116,234.122347304027,6.94979838230172)) ;
#72379=CARTESIAN_POINT('Ctrl Pts',(77.0452003554324,234.083189875681,7.03316975346642)) ;
#72380=CARTESIAN_POINT('Ctrl Pts',(77.0792533061722,234.041297979296,7.11711563024325)) ;
#72381=CARTESIAN_POINT('Ctrl Pts',(77.0867564620173,234.032067606585,7.13561208891489)) ;
#72382=CARTESIAN_POINT('Ctrl Pts',(77.0940172741218,234.022704572136,7.15413642788044)) ;
#72383=CARTESIAN_POINT('Ctrl Pts',(77.1010421843897,234.013216075904,7.17267980084131)) ;
#72384=CARTESIAN_POINT('Ctrl Pts',(76.8665793939903,234.048108437619,7.27867958884205)) ;
#72385=CARTESIAN_POINT('Ctrl Pts',(76.8340341124953,234.0925597155,7.16318668389241)) ;
#72386=CARTESIAN_POINT('Ctrl Pts',(76.7556911392885,234.174326892791,6.93379514728806)) ;
#72387=CARTESIAN_POINT('Ctrl Pts',(76.6190866745073,234.252741595594,6.66079114111062)) ;
#72388=CARTESIAN_POINT('Ctrl Pts',(76.4940251112423,234.285796227647,6.49259672460371)) ;
#72389=CARTESIAN_POINT('Ctrl Pts',(76.4114318303287,234.2941286283,6.41145063262659)) ;
#72390=CARTESIAN_POINT('Ctrl Pts',(76.3107018814125,234.294203813326,6.33519065213031)) ;
#72391=CARTESIAN_POINT('Ctrl Pts',(76.1811060983148,234.266159399846,6.30217089588981)) ;
#72392=CARTESIAN_POINT('Ctrl Pts',(76.0697307124536,234.208067009127,6.35347440234159)) ;
#72393=CARTESIAN_POINT('Ctrl Pts',(76.0060201171914,234.162253139921,6.4118128891193)) ;
#72394=CARTESIAN_POINT('Ctrl Pts',(75.9442201811444,234.106868936771,6.4932882288145)) ;
#72395=CARTESIAN_POINT('Ctrl Pts',(75.8624384710468,234.006731853917,6.66117946366231)) ;
#72396=CARTESIAN_POINT('Ctrl Pts',(75.7980532024828,233.862949209186,6.93433560993259)) ;
#72397=CARTESIAN_POINT('Ctrl Pts',(75.7826706984499,233.750949529794,7.16318984183889)) ;
#72398=CARTESIAN_POINT('Ctrl Pts',(75.7824688237379,233.69585956045,7.27867958884195)) ;
#72399=CARTESIAN_POINT('Origin',(74.5283628290597,239.4,7.2786795888419)) ;
#72400=CARTESIAN_POINT('Origin',(74.5283628290597,239.4,7.17267980084126)) ;
#72401=CARTESIAN_POINT('Origin',(77.0279509268839,234.166257616082,16.0213203435596)) ;
#72402=CARTESIAN_POINT('',(76.8665793939903,234.048108437619,16.0254384350469)) ;
#72403=CARTESIAN_POINT('',(76.8665793939903,234.048108437619,16.0213203435596)) ;
#72404=CARTESIAN_POINT('Ctrl Pts',(77.1141436199122,233.985783740775,16.2213203435596)) ;
#72405=CARTESIAN_POINT('Ctrl Pts',(77.1135321137219,233.985491690941,16.2206540664685)) ;
#72406=CARTESIAN_POINT('Ctrl Pts',(77.1129191197593,233.985202747452,16.2199877856837)) ;
#72407=CARTESIAN_POINT('Ctrl Pts',(77.0934911866169,233.976165511075,16.1989219658753)) ;
#72408=CARTESIAN_POINT('Ctrl Pts',(77.0732014734155,233.970288661947,16.1784289743533)) ;
#72409=CARTESIAN_POINT('Ctrl Pts',(77.0319798567454,233.965272578478,16.1396302535167)) ;
#72410=CARTESIAN_POINT('Ctrl Pts',(77.0108918072688,233.965813478537,16.1210537744675)) ;
#72411=CARTESIAN_POINT('Ctrl Pts',(76.9671930590858,233.974342228868,16.0855257633)) ;
#72412=CARTESIAN_POINT('Ctrl Pts',(76.944270848093,233.982813988936,16.068487609488)) ;
#72413=CARTESIAN_POINT('Ctrl Pts',(76.9062880703046,234.006370689004,16.0440628922443)) ;
#72414=CARTESIAN_POINT('Ctrl Pts',(76.8907647861873,234.019226794601,16.0353723462237)) ;
#72415=CARTESIAN_POINT('Ctrl Pts',(76.8733833952847,234.039215229877,16.0279192770514)) ;
#72416=CARTESIAN_POINT('Ctrl Pts',(76.8698946334441,234.043580388592,16.0265673132456)) ;
#72417=CARTESIAN_POINT('Ctrl Pts',(76.8665793939901,234.048108437619,16.0254384350468)) ;
#72418=CARTESIAN_POINT('Origin',(75.5824701665474,233.696592446523,16.0213203435596)) ;
#72419=CARTESIAN_POINT('',(75.7824688237379,233.69585956045,16.0254384350469)) ;
#72420=CARTESIAN_POINT('',(75.7824688237379,233.69585956045,16.0213203435596)) ;
#72421=CARTESIAN_POINT('Ctrl Pts',(75.7824688237379,233.69585956045,16.0254384350469)) ;
#72422=CARTESIAN_POINT('Ctrl Pts',(75.7823954804048,233.675844760517,16.0294645582753)) ;
#72423=CARTESIAN_POINT('Ctrl Pts',(75.7793263768937,233.656704801068,16.0362204083692)) ;
#72424=CARTESIAN_POINT('Ctrl Pts',(75.7670900599968,233.616042723181,16.056050217191)) ;
#72425=CARTESIAN_POINT('Ctrl Pts',(75.7565172414146,233.595758150279,16.070223718736)) ;
#72426=CARTESIAN_POINT('Ctrl Pts',(75.7284792865434,233.557458099226,16.1046945816758)) ;
#72427=CARTESIAN_POINT('Ctrl Pts',(75.7098594549003,233.540583950888,16.1258672215767)) ;
#72428=CARTESIAN_POINT('Ctrl Pts',(75.6683571515081,233.514199267903,16.1708720249642)) ;
#72429=CARTESIAN_POINT('Ctrl Pts',(75.6449193023295,233.505011527087,16.1951765216887)) ;
#72430=CARTESIAN_POINT('Ctrl Pts',(75.6201508361424,233.500172930197,16.2199877856672)) ;
#72431=CARTESIAN_POINT('Ctrl Pts',(75.6194850768967,233.50004638158,16.2206540664837)) ;
#72432=CARTESIAN_POINT('Ctrl Pts',(75.6188186954263,233.499923220541,16.2213203435596)) ;
#72433=CARTESIAN_POINT('Ctrl Pts',(78.4059643744832,235.032597310178,7.27867958886636)) ;
#72434=CARTESIAN_POINT('Ctrl Pts',(78.3389185036295,235.080934607739,7.10540671867987)) ;
#72435=CARTESIAN_POINT('Ctrl Pts',(78.234821145,235.130175045901,6.8757228796813)) ;
#72436=CARTESIAN_POINT('Ctrl Pts',(78.0706643466897,235.148929220103,6.61251961592784)) ;
#72437=CARTESIAN_POINT('Ctrl Pts',(77.9784150954104,235.143436282111,6.49309971889691)) ;
#72438=CARTESIAN_POINT('Ctrl Pts',(77.8972265351195,235.126146469199,6.41122237377758)) ;
#72439=CARTESIAN_POINT('Ctrl Pts',(77.8334871500539,235.1048001745,6.36192442727363)) ;
#72440=CARTESIAN_POINT('Ctrl Pts',(77.7217018252731,235.053842764399,6.30168464935698)) ;
#72441=CARTESIAN_POINT('Ctrl Pts',(77.5980687835801,234.948679457524,6.33246526297836)) ;
#72442=CARTESIAN_POINT('Ctrl Pts',(77.5181116348167,234.821023036642,6.4698168706527)) ;
#72443=CARTESIAN_POINT('Ctrl Pts',(77.4637464544563,234.683353081259,6.66032498688208)) ;
#72444=CARTESIAN_POINT('Ctrl Pts',(77.447328463511,234.526604137613,6.93427994562925)) ;
#72445=CARTESIAN_POINT('Ctrl Pts',(77.4669324115197,234.415038329963,7.1631851243399)) ;
#72446=CARTESIAN_POINT('Ctrl Pts',(77.4837648415456,234.362580130206,7.27867958884201)) ;
#72447=CARTESIAN_POINT('Ctrl Pts',(78.4428068537144,235.006035407726,7.24979207610077)) ;
#72448=CARTESIAN_POINT('Ctrl Pts',(78.3761232031844,235.062018285548,7.07844135600527)) ;
#72449=CARTESIAN_POINT('Ctrl Pts',(78.2690741390837,235.121066834892,6.85076492565332)) ;
#72450=CARTESIAN_POINT('Ctrl Pts',(78.095885173777,235.14883561158,6.58946758288809)) ;
#72451=CARTESIAN_POINT('Ctrl Pts',(77.9976154072437,235.146398293685,6.47083493132605)) ;
#72452=CARTESIAN_POINT('Ctrl Pts',(77.9107531594458,235.130222234622,6.38946905227889)) ;
#72453=CARTESIAN_POINT('Ctrl Pts',(77.8424673215011,235.108766275007,6.34047046809846)) ;
#72454=CARTESIAN_POINT('Ctrl Pts',(77.722636167835,235.05593023867,6.28058364221613)) ;
#72455=CARTESIAN_POINT('Ctrl Pts',(77.5911482552061,234.943002197512,6.31119003477298)) ;
#72456=CARTESIAN_POINT('Ctrl Pts',(77.5091860379167,234.804995268577,6.44770636852286)) ;
#72457=CARTESIAN_POINT('Ctrl Pts',(77.4564431115047,234.656661721284,6.63695559928427)) ;
#72458=CARTESIAN_POINT('Ctrl Pts',(77.4475171063426,234.48950940537,6.90885232947085)) ;
#72459=CARTESIAN_POINT('Ctrl Pts',(77.4758880078429,234.373136143523,7.13557881442652)) ;
#72460=CARTESIAN_POINT('Ctrl Pts',(77.4976417597599,234.319332770996,7.24979207607669)) ;
#72461=CARTESIAN_POINT('Ctrl Pts',(78.5303159124148,234.992495366521,7.19960833957127)) ;
#72462=CARTESIAN_POINT('Ctrl Pts',(78.4554802418853,235.058729481418,7.0313745223877)) ;
#72463=CARTESIAN_POINT('Ctrl Pts',(78.3352528450103,235.129028614954,6.80703932187651)) ;
#72464=CARTESIAN_POINT('Ctrl Pts',(78.1403320618317,235.163740445657,6.54896323857508)) ;
#72465=CARTESIAN_POINT('Ctrl Pts',(78.0298946126099,235.162534045408,6.43167577284028)) ;
#72466=CARTESIAN_POINT('Ctrl Pts',(77.9323657714883,235.145398507738,6.35118822945158)) ;
#72467=CARTESIAN_POINT('Ctrl Pts',(77.8557956985622,235.121979552267,6.30270555414491)) ;
#72468=CARTESIAN_POINT('Ctrl Pts',(77.7215728499806,235.063585748907,6.24342928702186)) ;
#72469=CARTESIAN_POINT('Ctrl Pts',(77.5749239465817,234.937168605196,6.27373289217854)) ;
#72470=CARTESIAN_POINT('Ctrl Pts',(77.4845607759043,234.781755560483,6.40881021948315)) ;
#72471=CARTESIAN_POINT('Ctrl Pts',(77.4276253550398,234.614308272085,6.59590889111905)) ;
#72472=CARTESIAN_POINT('Ctrl Pts',(77.4210763090117,234.424954269108,6.86433848773879)) ;
#72473=CARTESIAN_POINT('Ctrl Pts',(77.4569041711037,234.293005229142,7.08747263933178)) ;
#72474=CARTESIAN_POINT('Ctrl Pts',(77.4834773178775,234.231922607649,7.19960833954764)) ;
#72475=CARTESIAN_POINT('Ctrl Pts',(78.6120751679795,235.042656580024,7.17608503413729)) ;
#72476=CARTESIAN_POINT('Ctrl Pts',(78.5257874071805,235.108293909258,7.00515935572851)) ;
#72477=CARTESIAN_POINT('Ctrl Pts',(78.3906006573324,235.175667031547,6.77808190130018)) ;
#72478=CARTESIAN_POINT('Ctrl Pts',(78.1753161685454,235.202640673185,6.51747818540342)) ;
#72479=CARTESIAN_POINT('Ctrl Pts',(78.0539168452354,235.196261529505,6.39916177246118)) ;
#72480=CARTESIAN_POINT('Ctrl Pts',(77.9468350659121,235.173936329358,6.31801268447563)) ;
#72481=CARTESIAN_POINT('Ctrl Pts',(77.8626823795979,235.146014398301,6.269144723575)) ;
#72482=CARTESIAN_POINT('Ctrl Pts',(77.7149629217121,235.07896759255,6.2094174531271)) ;
#72483=CARTESIAN_POINT('Ctrl Pts',(77.5516109111798,234.939863263764,6.23994237498883)) ;
#72484=CARTESIAN_POINT('Ctrl Pts',(77.4468142355107,234.771155243331,6.37609489248998)) ;
#72485=CARTESIAN_POINT('Ctrl Pts',(77.3765566725479,234.589564664911,6.56483996405531)) ;
#72486=CARTESIAN_POINT('Ctrl Pts',(77.3577590685433,234.383553168869,6.83601511990593)) ;
#72487=CARTESIAN_POINT('Ctrl Pts',(77.3866701751303,234.237885051697,7.06215508260823)) ;
#72488=CARTESIAN_POINT('Ctrl Pts',(77.4105061694942,234.169665602309,7.17608503411327)) ;
#72489=CARTESIAN_POINT('Ctrl Pts',(78.6397340718682,235.07186568898,7.17267980086572)) ;
#72490=CARTESIAN_POINT('Ctrl Pts',(78.5499065311274,235.13590406076,6.99940693067923)) ;
#72491=CARTESIAN_POINT('Ctrl Pts',(78.4099204444132,235.200410168681,6.76972309168069)) ;
#72492=CARTESIAN_POINT('Ctrl Pts',(78.187632684868,235.222365326873,6.5065198279272)) ;
#72493=CARTESIAN_POINT('Ctrl Pts',(78.0622716858111,235.213009993023,6.38709993089628)) ;
#72494=CARTESIAN_POINT('Ctrl Pts',(77.9515865903972,235.187946097367,6.30522258577693)) ;
#72495=CARTESIAN_POINT('Ctrl Pts',(77.86447454918,235.157785697904,6.25592463927299)) ;
#72496=CARTESIAN_POINT('Ctrl Pts',(77.7113224120971,235.08665818323,6.19568486135635)) ;
#72497=CARTESIAN_POINT('Ctrl Pts',(77.5406975816401,234.942350518612,6.22646547497773)) ;
#72498=CARTESIAN_POINT('Ctrl Pts',(77.429144135509,234.768977939852,6.36381708265207)) ;
#72499=CARTESIAN_POINT('Ctrl Pts',(77.3523868997445,234.582817627175,6.55432519888145)) ;
#72500=CARTESIAN_POINT('Ctrl Pts',(77.327204290906,234.371962310836,6.82828015762859)) ;
#72501=CARTESIAN_POINT('Ctrl Pts',(77.3520863108302,234.222520587963,7.05718533633927)) ;
#72502=CARTESIAN_POINT('Ctrl Pts',(77.3741795847386,234.152386532591,7.17267980084138)) ;
#72503=CARTESIAN_POINT('Ctrl Pts',(77.3741795847386,234.152386532591,7.17267980084132)) ;
#72504=CARTESIAN_POINT('Ctrl Pts',(77.3616101223674,234.192287697697,7.106971869474)) ;
#72505=CARTESIAN_POINT('Ctrl Pts',(77.3521598145269,234.233709426668,7.04152334195408)) ;
#72506=CARTESIAN_POINT('Ctrl Pts',(77.3461415055067,234.276630953922,6.97670888987274)) ;
#72507=CARTESIAN_POINT('Ctrl Pts',(77.3427531126356,234.300796379205,6.94021743909526)) ;
#72508=CARTESIAN_POINT('Ctrl Pts',(77.3404515536967,234.325437412815,6.90392730454654)) ;
#72509=CARTESIAN_POINT('Ctrl Pts',(77.3392831405174,234.350552376217,6.86790768240443)) ;
#72510=CARTESIAN_POINT('Ctrl Pts',(77.3388797538195,234.359223146399,6.85547215301052)) ;
#72511=CARTESIAN_POINT('Ctrl Pts',(77.3386116782838,234.367952282434,6.84306652227551)) ;
#72512=CARTESIAN_POINT('Ctrl Pts',(77.338480649152,234.376740738638,6.83069237265686)) ;
#72513=CARTESIAN_POINT('Ctrl Pts',(77.3379770938846,234.410515467598,6.7831375416669)) ;
#72514=CARTESIAN_POINT('Ctrl Pts',(77.3394958704025,234.445163335056,6.73604483330478)) ;
#72515=CARTESIAN_POINT('Ctrl Pts',(77.343636060906,234.480754703633,6.68991055366433)) ;
#72516=CARTESIAN_POINT('Ctrl Pts',(77.3445932458965,234.488983195477,6.67924460967454)) ;
#72517=CARTESIAN_POINT('Ctrl Pts',(77.3456903680287,234.497262242329,6.66862989410104)) ;
#72518=CARTESIAN_POINT('Ctrl Pts',(77.34693451014,234.505592968877,6.65807253999053)) ;
#72519=CARTESIAN_POINT('Ctrl Pts',(77.3518801742937,234.538708941152,6.61610536654)) ;
#72520=CARTESIAN_POINT('Ctrl Pts',(77.3591521949255,234.572639578347,6.57504372092637)) ;
#72521=CARTESIAN_POINT('Ctrl Pts',(77.3692148632958,234.607477534717,6.5353038730101)) ;
#72522=CARTESIAN_POINT('Ctrl Pts',(77.3714459871851,234.615201907006,6.52649263917198)) ;
#72523=CARTESIAN_POINT('Ctrl Pts',(77.3738141831599,234.622971045816,6.51774638628193)) ;
#72524=CARTESIAN_POINT('Ctrl Pts',(77.3763243098519,234.630786261121,6.50906965173452)) ;
#72525=CARTESIAN_POINT('Ctrl Pts',(77.3770145717788,234.632935373989,6.50668362893874)) ;
#72526=CARTESIAN_POINT('Ctrl Pts',(77.3777155795123,234.63508796889,6.50430287822882)) ;
#72527=CARTESIAN_POINT('Ctrl Pts',(77.3784275163327,234.637244054133,6.50192759076481)) ;
#72528=CARTESIAN_POINT('Ctrl Pts',(77.3885926649084,234.668028986472,6.46801285382404)) ;
#72529=CARTESIAN_POINT('Ctrl Pts',(77.4009736446465,234.699452872062,6.43529517311966)) ;
#72530=CARTESIAN_POINT('Ctrl Pts',(77.4160710196623,234.731531497338,6.4043522398541)) ;
#72531=CARTESIAN_POINT('Ctrl Pts',(77.4185087934634,234.736711234357,6.39935588307255)) ;
#72532=CARTESIAN_POINT('Ctrl Pts',(77.4210173606465,234.741908148382,6.39440579852665)) ;
#72533=CARTESIAN_POINT('Ctrl Pts',(77.4235987954642,234.747122436193,6.38950441826156)) ;
#72534=CARTESIAN_POINT('Ctrl Pts',(77.4274281313007,234.754857382293,6.38223364350942)) ;
#72535=CARTESIAN_POINT('Ctrl Pts',(77.4314176194649,234.762630344498,6.37507015782897)) ;
#72536=CARTESIAN_POINT('Ctrl Pts',(77.4355736599342,234.770441778795,6.36802208736112)) ;
#72537=CARTESIAN_POINT('Ctrl Pts',(77.4431151830721,234.784616355036,6.35523270600096)) ;
#72538=CARTESIAN_POINT('Ctrl Pts',(77.4512052664404,234.798917493541,6.3428233691989)) ;
#72539=CARTESIAN_POINT('Ctrl Pts',(77.4599388214992,234.813284958107,6.33097919152505)) ;
#72540=CARTESIAN_POINT('Ctrl Pts',(77.4727287173272,234.834325459239,6.31363392976204)) ;
#72541=CARTESIAN_POINT('Ctrl Pts',(77.4869207989778,234.855607065859,6.2973856652023)) ;
#72542=CARTESIAN_POINT('Ctrl Pts',(77.5028075979575,234.876890083662,6.2829000606871)) ;
#72543=CARTESIAN_POINT('Ctrl Pts',(77.5128022833951,234.89027963233,6.27378689316436)) ;
#72544=CARTESIAN_POINT('Ctrl Pts',(77.52346710991,234.903669696134,6.26537131953454)) ;
#72545=CARTESIAN_POINT('Ctrl Pts',(77.5348655206898,234.917001932592,6.25781298087135)) ;
#72546=CARTESIAN_POINT('Ctrl Pts',(77.5479220204083,234.932273565183,6.24915515579955)) ;
#72547=CARTESIAN_POINT('Ctrl Pts',(77.5619406209771,234.947469595829,6.24162312159313)) ;
#72548=CARTESIAN_POINT('Ctrl Pts',(77.5767273170561,234.962392577957,6.23533841590271)) ;
#72549=CARTESIAN_POINT('Ctrl Pts',(77.5931271779032,234.978943593074,6.22836807592698)) ;
#72550=CARTESIAN_POINT('Ctrl Pts',(77.610533619044,234.995184164585,6.22295448141433)) ;
#72551=CARTESIAN_POINT('Ctrl Pts',(77.6287531529318,235.01091373282,6.21921752589672)) ;
#72552=CARTESIAN_POINT('Ctrl Pts',(77.631852838839,235.013589801334,6.21858175835048)) ;
#72553=CARTESIAN_POINT('Ctrl Pts',(77.6349761614252,235.016251058131,6.21799458776082)) ;
#72554=CARTESIAN_POINT('Ctrl Pts',(77.6381222895719,235.018896483061,6.21745669291191)) ;
#72555=CARTESIAN_POINT('Ctrl Pts',(77.654656351138,235.032799164904,6.2146298574706)) ;
#72556=CARTESIAN_POINT('Ctrl Pts',(77.6718229084934,235.046267967594,6.21316348490088)) ;
#72557=CARTESIAN_POINT('Ctrl Pts',(77.6894823515512,235.059110451571,6.21318607169313)) ;
#72558=CARTESIAN_POINT('Ctrl Pts',(77.7048365201591,235.070276469869,6.21320570999176)) ;
#72559=CARTESIAN_POINT('Ctrl Pts',(77.7205882506528,235.080940505187,6.21441169855859)) ;
#72560=CARTESIAN_POINT('Ctrl Pts',(77.7365768790082,235.090876830127,6.21693669735049)) ;
#72561=CARTESIAN_POINT('Ctrl Pts',(77.7376569000736,235.091548022178,6.21710725931645)) ;
#72562=CARTESIAN_POINT('Ctrl Pts',(77.7387379880425,235.092215887671,6.21728382721156)) ;
#72563=CARTESIAN_POINT('Ctrl Pts',(77.7398200874826,235.092880354597,6.2174664363144)) ;
#72564=CARTESIAN_POINT('Ctrl Pts',(77.7508744945164,235.0996683517,6.21933191676467)) ;
#72565=CARTESIAN_POINT('Ctrl Pts',(77.7619927080453,235.106176198894,6.22169249857145)) ;
#72566=CARTESIAN_POINT('Ctrl Pts',(77.7731573385193,235.112355623372,6.22458829330823)) ;
#72567=CARTESIAN_POINT('Ctrl Pts',(77.7879486527031,235.120542352806,6.22842474896731)) ;
#72568=CARTESIAN_POINT('Ctrl Pts',(77.8028220367511,235.128153742158,6.23320001862001)) ;
#72569=CARTESIAN_POINT('Ctrl Pts',(77.8176165123455,235.135214037743,6.23871136915441)) ;
#72570=CARTESIAN_POINT('Ctrl Pts',(77.833003966678,235.142557317685,6.24444362063687)) ;
#72571=CARTESIAN_POINT('Ctrl Pts',(77.848419888985,235.149315531718,6.2510693938749)) ;
#72572=CARTESIAN_POINT('Ctrl Pts',(77.8636522359854,235.155531306993,6.25830795380365)) ;
#72573=CARTESIAN_POINT('Ctrl Pts',(77.8854684142047,235.164433707991,6.26867521457129)) ;
#72574=CARTESIAN_POINT('Ctrl Pts',(77.9069060915642,235.172221298945,6.28029834834182)) ;
#72575=CARTESIAN_POINT('Ctrl Pts',(77.927961829551,235.178948105379,6.29304763982214)) ;
#72576=CARTESIAN_POINT('Ctrl Pts',(77.9356336646272,235.181399073831,6.29769295131094)) ;
#72577=CARTESIAN_POINT('Ctrl Pts',(77.9432550757436,235.183709627116,6.30248760576134)) ;
#72578=CARTESIAN_POINT('Ctrl Pts',(77.9508268025495,235.185883737378,6.30742481813906)) ;
#72579=CARTESIAN_POINT('Ctrl Pts',(77.9701099120664,235.191420599359,6.31999854265769)) ;
#72580=CARTESIAN_POINT('Ctrl Pts',(77.9890694837187,235.196070917094,6.33349709476029)) ;
#72581=CARTESIAN_POINT('Ctrl Pts',(78.0076268293722,235.200005114599,6.34759111946657)) ;
#72582=CARTESIAN_POINT('Ctrl Pts',(78.0163745748408,235.2018596556,6.35423490048245)) ;
#72583=CARTESIAN_POINT('Ctrl Pts',(78.0250425173661,235.203549292818,6.36102798943507)) ;
#72584=CARTESIAN_POINT('Ctrl Pts',(78.0336233074686,235.205088399391,6.36794163166575)) ;
#72585=CARTESIAN_POINT('Ctrl Pts',(78.0699367923575,235.211601823283,6.3971998281341)) ;
#72586=CARTESIAN_POINT('Ctrl Pts',(78.1046886470117,235.215413254151,6.42861607705246)) ;
#72587=CARTESIAN_POINT('Ctrl Pts',(78.1380455613265,235.21707104078,6.46147659275002)) ;
#72588=CARTESIAN_POINT('Ctrl Pts',(78.1538675906542,235.217857370967,6.47706316764065)) ;
#72589=CARTESIAN_POINT('Ctrl Pts',(78.1693759091666,235.218160283575,6.49297483602705)) ;
#72590=CARTESIAN_POINT('Ctrl Pts',(78.184588856189,235.218043521371,6.50913654336621)) ;
#72591=CARTESIAN_POINT('Ctrl Pts',(78.2070668421853,235.217870998639,6.53301637616342)) ;
#72592=CARTESIAN_POINT('Ctrl Pts',(78.2288998377486,235.216781901257,6.55744192341381)) ;
#72593=CARTESIAN_POINT('Ctrl Pts',(78.2501404992287,235.214912122256,6.58226166134351)) ;
#72594=CARTESIAN_POINT('Ctrl Pts',(78.2735769892242,235.212849048236,6.6096472274769)) ;
#72595=CARTESIAN_POINT('Ctrl Pts',(78.296297808578,235.209804393606,6.63755574293694)) ;
#72596=CARTESIAN_POINT('Ctrl Pts',(78.3183648534066,235.205949915774,6.66580368541426)) ;
#72597=CARTESIAN_POINT('Ctrl Pts',(78.3568347764113,235.199230327059,6.71504889158392)) ;
#72598=CARTESIAN_POINT('Ctrl Pts',(78.3933163504242,235.19004732315,6.76532387402165)) ;
#72599=CARTESIAN_POINT('Ctrl Pts',(78.4280131127771,235.178728979788,6.81629655261704)) ;
#72600=CARTESIAN_POINT('Ctrl Pts',(78.4315249867773,235.177583380225,6.82145581280564)) ;
#72601=CARTESIAN_POINT('Ctrl Pts',(78.43501855861,235.176415944776,6.82662222069363)) ;
#72602=CARTESIAN_POINT('Ctrl Pts',(78.4384940288008,235.175227040323,6.83179543193681)) ;
#72603=CARTESIAN_POINT('Ctrl Pts',(78.4743358912824,235.162966095017,6.88514577470656)) ;
#72604=CARTESIAN_POINT('Ctrl Pts',(78.508254558857,235.148418773849,6.93921964827946)) ;
#72605=CARTESIAN_POINT('Ctrl Pts',(78.5404913241743,235.132011538704,6.99367466100287)) ;
#72606=CARTESIAN_POINT('Ctrl Pts',(78.5422638099616,235.131109413729,6.99666878076482)) ;
#72607=CARTESIAN_POINT('Ctrl Pts',(78.5440312099124,235.13020167882,6.99966405277532)) ;
#72608=CARTESIAN_POINT('Ctrl Pts',(78.5457935638897,235.129288409307,7.00266042012063)) ;
#72609=CARTESIAN_POINT('Ctrl Pts',(78.5725232220026,235.115436832295,7.0481063837325)) ;
#72610=CARTESIAN_POINT('Ctrl Pts',(78.59805570937,235.100254606844,7.09382974369312)) ;
#72611=CARTESIAN_POINT('Ctrl Pts',(78.6224329066999,235.083850652226,7.13971415669166)) ;
#72612=CARTESIAN_POINT('Ctrl Pts',(78.6282662782212,235.07992524766,7.15069412393042)) ;
#72613=CARTESIAN_POINT('Ctrl Pts',(78.6340332765776,235.075929806123,7.16168324953904)) ;
#72614=CARTESIAN_POINT('Ctrl Pts',(78.6397340718556,235.071865688989,7.17267980084157)) ;
#72615=CARTESIAN_POINT('Ctrl Pts',(78.4059643744832,235.032597310178,7.27867958886636)) ;
#72616=CARTESIAN_POINT('Ctrl Pts',(78.3389185036295,235.080934607739,7.10540671867987)) ;
#72617=CARTESIAN_POINT('Ctrl Pts',(78.234821145,235.130175045901,6.8757228796813)) ;
#72618=CARTESIAN_POINT('Ctrl Pts',(78.0706643466897,235.148929220103,6.61251961592784)) ;
#72619=CARTESIAN_POINT('Ctrl Pts',(77.9784150954104,235.143436282111,6.49309971889691)) ;
#72620=CARTESIAN_POINT('Ctrl Pts',(77.8972265351195,235.126146469199,6.41122237377758)) ;
#72621=CARTESIAN_POINT('Ctrl Pts',(77.8334871500539,235.1048001745,6.36192442727363)) ;
#72622=CARTESIAN_POINT('Ctrl Pts',(77.7217018252731,235.053842764399,6.30168464935698)) ;
#72623=CARTESIAN_POINT('Ctrl Pts',(77.5980687835801,234.948679457524,6.33246526297836)) ;
#72624=CARTESIAN_POINT('Ctrl Pts',(77.5181116348167,234.821023036642,6.4698168706527)) ;
#72625=CARTESIAN_POINT('Ctrl Pts',(77.4637464544563,234.683353081259,6.66032498688208)) ;
#72626=CARTESIAN_POINT('Ctrl Pts',(77.447328463511,234.526604137613,6.93427994562925)) ;
#72627=CARTESIAN_POINT('Ctrl Pts',(77.4669324115197,234.415038329963,7.1631851243399)) ;
#72628=CARTESIAN_POINT('Ctrl Pts',(77.4837648415456,234.362580130206,7.27867958884201)) ;
#72629=CARTESIAN_POINT('Origin',(77.2933283411226,234.301474162358,16.0213203435596)) ;
#72630=CARTESIAN_POINT('',(77.4837648415456,234.362580130206,16.0254384350469)) ;
#72631=CARTESIAN_POINT('',(77.4837648415456,234.362580130206,16.0213203435596)) ;
#72632=CARTESIAN_POINT('Ctrl Pts',(77.4837648415456,234.362580130206,16.0254384350469)) ;
#72633=CARTESIAN_POINT('Ctrl Pts',(77.4898800012088,234.343522259972,16.0294645582753)) ;
#72634=CARTESIAN_POINT('Ctrl Pts',(77.492875683057,234.324370671673,16.0362204083692)) ;
#72635=CARTESIAN_POINT('Ctrl Pts',(77.4938035272304,234.281917507663,16.056050217191)) ;
#72636=CARTESIAN_POINT('Ctrl Pts',(77.4900164569724,234.259358551804,16.0702237187361)) ;
#72637=CARTESIAN_POINT('Ctrl Pts',(77.4751861439491,234.214268834133,16.1046945816763)) ;
#72638=CARTESIAN_POINT('Ctrl Pts',(77.4626920303345,234.192466720987,16.1258672215778)) ;
#72639=CARTESIAN_POINT('Ctrl Pts',(77.4313743096848,234.15454847925,16.1708720249663)) ;
#72640=CARTESIAN_POINT('Ctrl Pts',(77.4119227585275,234.138567724759,16.1951765216655)) ;
#72641=CARTESIAN_POINT('Ctrl Pts',(77.3898617560505,234.126312068692,16.2199877856737)) ;
#72642=CARTESIAN_POINT('Ctrl Pts',(77.3892676870572,234.125985982886,16.2206540664817)) ;
#72643=CARTESIAN_POINT('Ctrl Pts',(77.3886719794696,234.125662926577,16.2213203435596)) ;
#72644=CARTESIAN_POINT('Origin',(74.5283628290597,239.4,16.2213203435596)) ;
#72645=CARTESIAN_POINT('',(75.7840731199179,233.737563098327,16.0213203435596)) ;
#72646=CARTESIAN_POINT('Ctrl Pts',(75.7824688237379,233.69585956045,16.0254384350468)) ;
#72647=CARTESIAN_POINT('Ctrl Pts',(75.7825092685165,233.706896612048,16.0232182514845)) ;
#72648=CARTESIAN_POINT('Ctrl Pts',(75.7828565073841,233.718128254652,16.0218983740811)) ;
#72649=CARTESIAN_POINT('Ctrl Pts',(75.7836951033986,233.732160271511,16.0213707571522)) ;
#72650=CARTESIAN_POINT('Ctrl Pts',(75.7838750549479,233.734863451389,16.0213203435596)) ;
#72651=CARTESIAN_POINT('Ctrl Pts',(75.784073119918,233.737563098327,16.0213203435596)) ;
#72652=CARTESIAN_POINT('',(76.8407687665842,234.080904326852,16.0213203435596)) ;
#72653=CARTESIAN_POINT('Origin',(74.5283628290597,239.4,16.0213203435596)) ;
#72654=CARTESIAN_POINT('Ctrl Pts',(76.8407687665842,234.080904326852,16.0213203435596)) ;
#72655=CARTESIAN_POINT('Ctrl Pts',(76.8480493410532,234.072287741056,16.0213203435596)) ;
#72656=CARTESIAN_POINT('Ctrl Pts',(76.8550882213081,234.063461822359,16.0221950109068)) ;
#72657=CARTESIAN_POINT('Ctrl Pts',(76.8634346692571,234.052374031266,16.0244263118334)) ;
#72658=CARTESIAN_POINT('Ctrl Pts',(76.865018268209,234.050240667937,16.0249068532759)) ;
#72659=CARTESIAN_POINT('Ctrl Pts',(76.8665793939903,234.048108437619,16.0254384350468)) ;
#72660=CARTESIAN_POINT('Origin',(75.2882970367382,233.65,16.0213203435596)) ;
#72661=CARTESIAN_POINT('',(75.0983134848186,233.5875,16.0254384350469)) ;
#72662=CARTESIAN_POINT('',(75.0983134848186,233.5875,16.0213203435596)) ;
#72663=CARTESIAN_POINT('Ctrl Pts',(75.3145016645892,233.451724137931,16.2213203435596)) ;
#72664=CARTESIAN_POINT('Ctrl Pts',(75.3138298392977,233.45163534784,16.2206540664858)) ;
#72665=CARTESIAN_POINT('Ctrl Pts',(75.3131575589563,233.451549971806,16.2199877856686)) ;
#72666=CARTESIAN_POINT('Ctrl Pts',(75.291887836757,233.448958610743,16.1989219660293)) ;
#72667=CARTESIAN_POINT('Ctrl Pts',(75.2707751266654,233.449639261295,16.1784289743322)) ;
#72668=CARTESIAN_POINT('Ctrl Pts',(75.2300209844512,233.457606862526,16.1396302534681)) ;
#72669=CARTESIAN_POINT('Ctrl Pts',(75.2101322048779,233.46463785473,16.1210537744074)) ;
#72670=CARTESIAN_POINT('Ctrl Pts',(75.1712077544563,233.486252834152,16.0855257632413)) ;
#72671=CARTESIAN_POINT('Ctrl Pts',(75.1520253541674,233.501393309518,16.06848760944)) ;
#72672=CARTESIAN_POINT('Ctrl Pts',(75.1231810065142,233.535534386453,16.0440628922134)) ;
#72673=CARTESIAN_POINT('Ctrl Pts',(75.1123902411184,233.552558228057,16.0353723462)) ;
#72674=CARTESIAN_POINT('Ctrl Pts',(75.102036322246,233.576939504834,16.0279192770417)) ;
#72675=CARTESIAN_POINT('Ctrl Pts',(75.1000672207974,233.582169104154,16.0265673132415)) ;
#72676=CARTESIAN_POINT('Ctrl Pts',(75.0983134848186,233.5875,16.0254384350468)) ;
#72677=CARTESIAN_POINT('Origin',(74.5283628290597,239.4,7.2786795888419)) ;
#72678=CARTESIAN_POINT('Origin',(74.5283628290597,239.4,7.17267980084126)) ;
#72679=CARTESIAN_POINT('Origin',(78.5229277183602,235.19483040233,16.0213203435596)) ;
#72680=CARTESIAN_POINT('',(78.4059643744738,235.032597310185,16.0254384350469)) ;
#72681=CARTESIAN_POINT('',(78.4059643744738,235.032597310185,16.0213203435596)) ;
#72682=CARTESIAN_POINT('Ctrl Pts',(78.6606713352325,235.049824554134,16.2213203435594)) ;
#72683=CARTESIAN_POINT('Ctrl Pts',(78.6601800066574,235.049357832441,16.2206540664819)) ;
#72684=CARTESIAN_POINT('Ctrl Pts',(78.6596863032101,235.048893605308,16.2199877856694)) ;
#72685=CARTESIAN_POINT('Ctrl Pts',(78.6440019003139,235.034295121153,16.1989219660103)) ;
#72686=CARTESIAN_POINT('Ctrl Pts',(78.6265212826879,235.022436039381,16.1784289743341)) ;
#72687=CARTESIAN_POINT('Ctrl Pts',(78.5888672505516,235.004927280419,16.1396302534752)) ;
#72688=CARTESIAN_POINT('Ctrl Pts',(78.568644176356,234.99892514128,16.1210537744168)) ;
#72689=CARTESIAN_POINT('Ctrl Pts',(78.5244486683382,234.993532809052,16.0855257632509)) ;
#72690=CARTESIAN_POINT('Ctrl Pts',(78.5000304323776,234.994506578931,16.0684876094478)) ;
#72691=CARTESIAN_POINT('Ctrl Pts',(78.4566272434126,235.005173008213,16.0440628922183)) ;
#72692=CARTESIAN_POINT('Ctrl Pts',(78.4378909677921,235.012602932619,16.0353723462039)) ;
#72693=CARTESIAN_POINT('Ctrl Pts',(78.4151835165405,235.02624191906,16.0279192770432)) ;
#72694=CARTESIAN_POINT('Ctrl Pts',(78.4105165986467,235.029315344993,16.0265673132422)) ;
#72695=CARTESIAN_POINT('Ctrl Pts',(78.4059643744738,235.032597310185,16.0254384350468)) ;
#72696=CARTESIAN_POINT('Origin',(74.5283628290597,239.4,16.2213203435596)) ;
#72697=CARTESIAN_POINT('',(77.4724035159522,234.40273830644,16.0213203435596)) ;
#72698=CARTESIAN_POINT('Ctrl Pts',(77.4837648415455,234.362580130206,16.0254384350468)) ;
#72699=CARTESIAN_POINT('Ctrl Pts',(77.4803926703042,234.373089488173,16.0232182514845)) ;
#72700=CARTESIAN_POINT('Ctrl Pts',(77.4772521456526,234.383878717771,16.0218983740811)) ;
#72701=CARTESIAN_POINT('Ctrl Pts',(77.473713566182,234.397483099261,16.0213707571522)) ;
#72702=CARTESIAN_POINT('Ctrl Pts',(77.4730493817544,234.400109584186,16.0213203435596)) ;
#72703=CARTESIAN_POINT('Ctrl Pts',(77.4724035159521,234.40273830644,16.0213203435596)) ;
#72704=CARTESIAN_POINT('',(78.3712825219709,235.055812131844,16.0213203435596)) ;
#72705=CARTESIAN_POINT('Origin',(74.5283628290597,239.4,16.0213203435596)) ;
#72706=CARTESIAN_POINT('Ctrl Pts',(78.3712825219707,235.055812131844,16.0213203435596)) ;
#72707=CARTESIAN_POINT('Ctrl Pts',(78.3808694312064,235.049867093014,16.0213203435596)) ;
#72708=CARTESIAN_POINT('Ctrl Pts',(78.3902911630086,235.043648279145,16.0221950109068)) ;
#72709=CARTESIAN_POINT('Ctrl Pts',(78.4016554225963,235.035682357433,16.0244263118334)) ;
#72710=CARTESIAN_POINT('Ctrl Pts',(78.4038207602224,235.034142767326,16.0249068532759)) ;
#72711=CARTESIAN_POINT('Ctrl Pts',(78.4059643744737,235.032597310185,16.0254384350468)) ;
#72712=CARTESIAN_POINT('Origin',(73.7684286213811,233.65,16.0213203435596)) ;
#72713=CARTESIAN_POINT('',(73.9584121733008,233.5875,16.0254384350469)) ;
#72714=CARTESIAN_POINT('',(73.9584121733008,233.5875,16.0213203435596)) ;
#72715=CARTESIAN_POINT('Ctrl Pts',(73.9584121733008,233.5875,16.0254384350469)) ;
#72716=CARTESIAN_POINT('Ctrl Pts',(73.9521575063278,233.568487458438,16.0294645582753)) ;
#72717=CARTESIAN_POINT('Ctrl Pts',(73.9433240426927,233.551232680424,16.0362204083692)) ;
#72718=CARTESIAN_POINT('Ctrl Pts',(73.9191213406789,233.516341976154,16.056050217191)) ;
#72719=CARTESIAN_POINT('Ctrl Pts',(73.9027977149204,233.500317381536,16.070223718736)) ;
#72720=CARTESIAN_POINT('Ctrl Pts',(73.8642966685758,233.47255607295,16.1046945816758)) ;
#72721=CARTESIAN_POINT('Ctrl Pts',(73.8413737577571,233.462261648626,16.1258672215766)) ;
#72722=CARTESIAN_POINT('Ctrl Pts',(73.7937494062409,233.449993240996,16.1708720249644)) ;
#72723=CARTESIAN_POINT('Ctrl Pts',(73.7686195190054,233.44849787393,16.1951765216962)) ;
#72724=CARTESIAN_POINT('Ctrl Pts',(73.7435680991658,233.451549971806,16.2199877856659)) ;
#72725=CARTESIAN_POINT('Ctrl Pts',(73.7428958188225,233.45163534784,16.220654066485)) ;
#72726=CARTESIAN_POINT('Ctrl Pts',(73.7422239935301,233.451724137931,16.2213203435596)) ;
#72727=CARTESIAN_POINT('Origin',(74.5283628290597,239.4,16.2213203435596)) ;
#72728=CARTESIAN_POINT('',(73.9728250515664,233.626666666667,16.0213203435596)) ;
#72729=CARTESIAN_POINT('Ctrl Pts',(73.9584121733008,233.5875,16.0254384350468)) ;
#72730=CARTESIAN_POINT('Ctrl Pts',(73.9618612750826,233.597984361719,16.0232182514845)) ;
#72731=CARTESIAN_POINT('Ctrl Pts',(73.9656622873096,233.608558985895,16.0218983740811)) ;
#72732=CARTESIAN_POINT('Ctrl Pts',(73.9707959711885,233.621645086545,16.0213707571522)) ;
#72733=CARTESIAN_POINT('Ctrl Pts',(73.9718024438033,233.624160355296,16.0213203435596)) ;
#72734=CARTESIAN_POINT('Ctrl Pts',(73.9728250515665,233.626666666667,16.0213203435596)) ;
#72735=CARTESIAN_POINT('',(75.083900606553,233.626666666667,16.0213203435596)) ;
#72736=CARTESIAN_POINT('Origin',(74.5283628290597,239.4,16.0213203435596)) ;
#72737=CARTESIAN_POINT('Ctrl Pts',(75.0839006065529,233.626666666667,16.0213203435596)) ;
#72738=CARTESIAN_POINT('Ctrl Pts',(75.0881621728995,233.616221985357,16.0213203435596)) ;
#72739=CARTESIAN_POINT('Ctrl Pts',(75.0921291869651,233.605652904248,16.0221950109068)) ;
#72740=CARTESIAN_POINT('Ctrl Pts',(75.0966408147971,233.592528594019,16.0244263118334)) ;
#72741=CARTESIAN_POINT('Ctrl Pts',(75.0974876613757,233.590010285935,16.0249068532759)) ;
#72742=CARTESIAN_POINT('Ctrl Pts',(75.0983134848186,233.5875,16.0254384350468)) ;
#72743=CARTESIAN_POINT('Ctrl Pts',(79.5657826988647,236.44459798751,7.27867958886636)) ;
#72744=CARTESIAN_POINT('Ctrl Pts',(79.4870812400902,236.469851175839,7.10540671867988)) ;
#72745=CARTESIAN_POINT('Ctrl Pts',(79.3728626924325,236.484513827223,6.87572289449329)) ;
#72746=CARTESIAN_POINT('Ctrl Pts',(79.2109449345459,236.451622856973,6.61251963169561)) ;
#72747=CARTESIAN_POINT('Ctrl Pts',(79.1249080993041,236.417892181793,6.49309973646919)) ;
#72748=CARTESIAN_POINT('Ctrl Pts',(79.0530360354225,236.376359946734,6.41122239160556)) ;
#72749=CARTESIAN_POINT('Ctrl Pts',(78.9990126464368,236.336361861471,6.36192444560416)) ;
#72750=CARTESIAN_POINT('Ctrl Pts',(78.908445191216,236.253354919289,6.30168466926149)) ;
#72751=CARTESIAN_POINT('Ctrl Pts',(78.8233604283728,236.115133957597,6.33246528275406)) ;
#72752=CARTESIAN_POINT('Ctrl Pts',(78.7867646631746,235.969017367392,6.46981689000949)) ;
#72753=CARTESIAN_POINT('Ctrl Pts',(78.7776026491497,235.821285683305,6.66032500142642)) ;
#72754=CARTESIAN_POINT('Ctrl Pts',(78.8104263003458,235.66713514265,6.93427995946187)) ;
#72755=CARTESIAN_POINT('Ctrl Pts',(78.8635464513941,235.567087660364,7.16318512434001)) ;
#72756=CARTESIAN_POINT('Ctrl Pts',(78.8957655188746,235.522398454586,7.27867958884211)) ;
#72757=CARTESIAN_POINT('Ctrl Pts',(79.6090300580747,236.430721069295,7.24979207610077)) ;
#72758=CARTESIAN_POINT('Ctrl Pts',(79.5283104770667,236.463357568788,7.07844135600528)) ;
#72759=CARTESIAN_POINT('Ctrl Pts',(79.4082537819674,236.486436190288,6.85076495835015)) ;
#72760=CARTESIAN_POINT('Ctrl Pts',(79.2349602606826,236.459327520044,6.5894676145758)) ;
#72761=CARTESIAN_POINT('Ctrl Pts',(79.1422533331441,236.426642473391,6.47083496648431)) ;
#72762=CARTESIAN_POINT('Ctrl Pts',(79.0646411031859,236.384416214936,6.38946908750231)) ;
#72763=CARTESIAN_POINT('Ctrl Pts',(79.0063276682255,236.342908901173,6.34047050406937)) ;
#72764=CARTESIAN_POINT('Ctrl Pts',(78.9086887020337,236.255628981196,6.28058367983847)) ;
#72765=CARTESIAN_POINT('Ctrl Pts',(78.8185329489278,236.10759602833,6.31119007162906)) ;
#72766=CARTESIAN_POINT('Ctrl Pts',(78.7832287335185,235.951015918468,6.44770640459992)) ;
#72767=CARTESIAN_POINT('Ctrl Pts',(78.7789048125338,235.793643854386,6.63695562729077)) ;
#72768=CARTESIAN_POINT('Ctrl Pts',(78.8220685829243,235.631914269905,6.9088523574302)) ;
#72769=CARTESIAN_POINT('Ctrl Pts',(78.885012217346,235.530003744361,7.13557881442663)) ;
#72770=CARTESIAN_POINT('Ctrl Pts',(78.9223274213261,235.485555975355,7.24979207607679)) ;
#72771=CARTESIAN_POINT('Ctrl Pts',(79.6964402031828,236.444885555299,7.19960835919207)) ;
#72772=CARTESIAN_POINT('Ctrl Pts',(79.6047997839638,236.484752447894,7.03137454200852)) ;
#72773=CARTESIAN_POINT('Ctrl Pts',(79.4687331749363,236.514458639794,6.80703935301077)) ;
#72774=CARTESIAN_POINT('Ctrl Pts',(79.2726259399176,236.487237708637,6.5489632709138)) ;
#72775=CARTESIAN_POINT('Ctrl Pts',(79.1679664882912,236.45196330917,6.43167580665653)) ;
#72776=CARTESIAN_POINT('Ctrl Pts',(79.0805062198949,236.40552837394,6.35118826354325)) ;
#72777=CARTESIAN_POINT('Ctrl Pts',(79.0149206087179,236.359594169686,6.30270558867851)) ;
#72778=CARTESIAN_POINT('Ctrl Pts',(78.9053117717612,236.262581220077,6.24342932307369)) ;
#72779=CARTESIAN_POINT('Ctrl Pts',(78.804905418412,236.097034364148,6.27373292820263)) ;
#72780=CARTESIAN_POINT('Ctrl Pts',(78.7669902051957,235.921304016953,6.40881025513765)) ;
#72781=CARTESIAN_POINT('Ctrl Pts',(78.7645854417403,235.744458153853,6.5959089226156)) ;
#72782=CARTESIAN_POINT('Ctrl Pts',(78.8168705353506,235.562348030992,6.86433851840462)) ;
#72783=CARTESIAN_POINT('Ctrl Pts',(78.8917192824295,235.447928391624,7.0874726589527)) ;
#72784=CARTESIAN_POINT('Ctrl Pts',(78.9358674149294,235.398046920369,7.19960835916855)) ;
#72785=CARTESIAN_POINT('Ctrl Pts',(79.7586972267648,236.51785665956,7.17608503413728)) ;
#72786=CARTESIAN_POINT('Ctrl Pts',(79.6563496393816,236.553617084748,7.00515935572852)) ;
#72787=CARTESIAN_POINT('Ctrl Pts',(79.5069600229606,236.575917823757,6.7780819280561)) ;
#72788=CARTESIAN_POINT('Ctrl Pts',(79.293876985863,236.535044702284,6.51747821181318)) ;
#72789=CARTESIAN_POINT('Ctrl Pts',(79.1803906379132,236.491463330501,6.39916180179056)) ;
#72790=CARTESIAN_POINT('Ctrl Pts',(79.085448679511,236.43714071249,6.31801271393377)) ;
#72791=CARTESIAN_POINT('Ctrl Pts',(79.0140430708291,236.384580768783,6.26914475369938)) ;
#72792=CARTESIAN_POINT('Ctrl Pts',(78.8942721210401,236.275167644272,6.20941748487202)) ;
#72793=CARTESIAN_POINT('Ctrl Pts',(78.7819007264524,236.092393015084,6.23994240617312)) ;
#72794=CARTESIAN_POINT('Ctrl Pts',(78.7343668090907,235.899558197127,6.37609492300486)) ;
#72795=CARTESIAN_POINT('Ctrl Pts',(78.7236624584774,235.705144496605,6.56483998757442)) ;
#72796=CARTESIAN_POINT('Ctrl Pts',(78.7694459290053,235.503407144677,6.83601514313855)) ;
#72797=CARTESIAN_POINT('Ctrl Pts',(78.841955902057,235.373802485635,7.06215508260834)) ;
#72798=CARTESIAN_POINT('Ctrl Pts',(78.8857062490269,235.316287661092,7.17608503411338)) ;
#72799=CARTESIAN_POINT('Ctrl Pts',(79.7759762964836,236.554183244316,7.17267980086571)) ;
#72800=CARTESIAN_POINT('Ctrl Pts',(79.6707562833474,236.587329118438,6.99940693067923)) ;
#72801=CARTESIAN_POINT('Ctrl Pts',(79.5176881965809,236.60542008249,6.76972310649274)) ;
#72802=CARTESIAN_POINT('Ctrl Pts',(79.2994954482259,236.557609970426,6.50651984369493)) ;
#72803=CARTESIAN_POINT('Ctrl Pts',(79.1831610173716,236.509973847899,6.38709994846854)) ;
#72804=CARTESIAN_POINT('Ctrl Pts',(79.0856384050087,236.451933089803,6.3052226036049)) ;
#72805=CARTESIAN_POINT('Ctrl Pts',(79.0121100075054,236.396329745053,6.2559246576035)) ;
#72806=CARTESIAN_POINT('Ctrl Pts',(78.888433281189,236.281356845433,6.19568488126083)) ;
#72807=CARTESIAN_POINT('Ctrl Pts',(78.7707529424765,236.091386124969,6.22646549475341)) ;
#72808=CARTESIAN_POINT('Ctrl Pts',(78.7182343819777,235.892027091496,6.36381710200884)) ;
#72809=CARTESIAN_POINT('Ctrl Pts',(78.7027605981832,235.691258807103,6.55432521342576)) ;
#72810=CARTESIAN_POINT('Ctrl Pts',(78.7439683914917,235.482941632937,6.8282801714612)) ;
#72811=CARTESIAN_POINT('Ctrl Pts',(78.8138125729589,235.348503010481,7.05718533633938)) ;
#72812=CARTESIAN_POINT('Ctrl Pts',(78.8564971400703,235.288628757204,7.17267980084148)) ;
#72813=CARTESIAN_POINT('Ctrl Pts',(78.8564971400703,235.288628757204,7.17267980084147)) ;
#72814=CARTESIAN_POINT('Ctrl Pts',(78.8322127772666,235.322692780517,7.10697198962071)) ;
#72815=CARTESIAN_POINT('Ctrl Pts',(78.8104250280159,235.359166818334,7.04152358318827)) ;
#72816=CARTESIAN_POINT('Ctrl Pts',(78.7914378312746,235.398127786439,6.97670925058748)) ;
#72817=CARTESIAN_POINT('Ctrl Pts',(78.7807477174163,235.420063472405,6.94021768184272)) ;
#72818=CARTESIAN_POINT('Ctrl Pts',(78.7709442790968,235.442787344193,6.90392743085573)) ;
#72819=CARTESIAN_POINT('Ctrl Pts',(78.7620720790055,235.466312115078,6.86790769436091)) ;
#72820=CARTESIAN_POINT('Ctrl Pts',(78.7590090216288,235.474433857402,6.85547216332687)) ;
#72821=CARTESIAN_POINT('Ctrl Pts',(78.7560566159773,235.482652921741,6.84306653074808)) ;
#72822=CARTESIAN_POINT('Ctrl Pts',(78.7532162176156,235.490970752063,6.83069237910109)) ;
#72823=CARTESIAN_POINT('Ctrl Pts',(78.7423004157144,235.522936616169,6.78313785650423)) ;
#72824=CARTESIAN_POINT('Ctrl Pts',(78.7330381191646,235.556357792529,6.73604544693575)) ;
#72825=CARTESIAN_POINT('Ctrl Pts',(78.7259773485412,235.591486331508,6.68991145156326)) ;
#72826=CARTESIAN_POINT('Ctrl Pts',(78.7243443243909,235.599610905379,6.67924152152199)) ;
#72827=CARTESIAN_POINT('Ctrl Pts',(78.7228288537345,235.607826871102,6.66862285804887)) ;
#72828=CARTESIAN_POINT('Ctrl Pts',(78.7214373324945,235.61613749082,6.65806160112184)) ;
#72829=CARTESIAN_POINT('Ctrl Pts',(78.7159079051888,235.649161038197,6.61609479475419)) ;
#72830=CARTESIAN_POINT('Ctrl Pts',(78.7123392499051,235.683678268544,6.575033543448)) ;
#72831=CARTESIAN_POINT('Ctrl Pts',(78.7111442988235,235.719920776149,6.5352941167486)) ;
#72832=CARTESIAN_POINT('Ctrl Pts',(78.7108794472324,235.727953645404,6.52648618263948)) ;
#72833=CARTESIAN_POINT('Ctrl Pts',(78.7107310413867,235.736071386349,6.51774318351641)) ;
#72834=CARTESIAN_POINT('Ctrl Pts',(78.7107032926989,235.744276743245,6.50906965181891)) ;
#72835=CARTESIAN_POINT('Ctrl Pts',(78.7106956592731,235.746533966463,6.50668363773311)) ;
#72836=CARTESIAN_POINT('Ctrl Pts',(78.7106971696829,235.748797821899,6.50430289572339)) ;
#72837=CARTESIAN_POINT('Ctrl Pts',(78.7107079956681,235.751068374094,6.50192761694854)) ;
#72838=CARTESIAN_POINT('Ctrl Pts',(78.7108625712828,235.783487779315,6.46801290435377)) ;
#72839=CARTESIAN_POINT('Ctrl Pts',(78.7129270713278,235.817199587996,6.43529524449621)) ;
#72840=CARTESIAN_POINT('Ctrl Pts',(78.7173726789433,235.852373496539,6.40435232380597)) ;
#72841=CARTESIAN_POINT('Ctrl Pts',(78.7180907228513,235.85805470211,6.39935449727259)) ;
#72842=CARTESIAN_POINT('Ctrl Pts',(78.7188708235085,235.863774142674,6.39440297002402)) ;
#72843=CARTESIAN_POINT('Ctrl Pts',(78.7197148945106,235.869532647099,6.3895001762352)) ;
#72844=CARTESIAN_POINT('Ctrl Pts',(78.7209663891753,235.87807071741,6.38223085854324)) ;
#72845=CARTESIAN_POINT('Ctrl Pts',(78.7223583960393,235.886694399858,6.37506878931773)) ;
#72846=CARTESIAN_POINT('Ctrl Pts',(78.7238968574451,235.895406104459,6.3680220898963)) ;
#72847=CARTESIAN_POINT('Ctrl Pts',(78.7266890802744,235.911217369126,6.3552327180466)) ;
#72848=CARTESIAN_POINT('Ctrl Pts',(78.7299639023541,235.927318514931,6.34282338850292)) ;
#72849=CARTESIAN_POINT('Ctrl Pts',(78.7338302037624,235.943681583749,6.33097921492544)) ;
#72850=CARTESIAN_POINT('Ctrl Pts',(78.7394922114334,235.967644490772,6.31363400704614)) ;
#72851=CARTESIAN_POINT('Ctrl Pts',(78.7464132687362,235.992270001039,6.29738579228852)) ;
#72852=CARTESIAN_POINT('Ctrl Pts',(78.7549456537334,236.017420547968,6.28290022688547)) ;
#72853=CARTESIAN_POINT('Ctrl Pts',(78.7603135972084,236.033243405741,6.27378698406848)) ;
#72854=CARTESIAN_POINT('Ctrl Pts',(78.7663187342802,236.049273842205,6.26537134622199)) ;
#72855=CARTESIAN_POINT('Ctrl Pts',(78.7730394330041,236.065475973807,6.2578129580718)) ;
#72856=CARTESIAN_POINT('Ctrl Pts',(78.7807377033575,236.084034816347,6.24915515063138)) ;
#72857=CARTESIAN_POINT('Ctrl Pts',(78.7893743477905,236.102819061703,6.24162313405724)) ;
#72858=CARTESIAN_POINT('Ctrl Pts',(78.7988258701155,236.12158097562,6.23533844570994)) ;
#72859=CARTESIAN_POINT('Ctrl Pts',(78.8093087363274,236.142390177217,6.22836797631217)) ;
#72860=CARTESIAN_POINT('Ctrl Pts',(78.8208448817506,236.163215179485,6.22295430296987)) ;
#72861=CARTESIAN_POINT('Ctrl Pts',(78.833312267638,236.183805435466,6.21921733601531)) ;
#72862=CARTESIAN_POINT('Ctrl Pts',(78.835433049314,236.187307969035,6.21858165415606)) ;
#72863=CARTESIAN_POINT('Ctrl Pts',(78.8375808814211,236.190803721444,6.21799455781567)) ;
#72864=CARTESIAN_POINT('Ctrl Pts',(78.8397552889646,236.194291466072,6.21745672558774)) ;
#72865=CARTESIAN_POINT('Ctrl Pts',(78.8511839473342,236.21262300744,6.21462988624397)) ;
#72866=CARTESIAN_POINT('Ctrl Pts',(78.863348221106,236.230737357873,6.21316350919955)) ;
#72867=CARTESIAN_POINT('Ctrl Pts',(78.8761748005146,236.248408354793,6.21318609107912)) ;
#72868=CARTESIAN_POINT('Ctrl Pts',(78.8873264039381,236.263771761004,6.21320572407383)) ;
#72869=CARTESIAN_POINT('Ctrl Pts',(78.8990111727565,236.278780648428,6.21441157326701)) ;
#72870=CARTESIAN_POINT('Ctrl Pts',(78.9111460827114,236.293170722242,6.21693629918754)) ;
#72871=CARTESIAN_POINT('Ctrl Pts',(78.911966469022,236.294143569968,6.21710698447412)) ;
#72872=CARTESIAN_POINT('Ctrl Pts',(78.9127889012084,236.295113579268,6.2172836850705)) ;
#72873=CARTESIAN_POINT('Ctrl Pts',(78.9136133487335,236.296080664322,6.21746643634462)) ;
#72874=CARTESIAN_POINT('Ctrl Pts',(78.9220291325022,236.30595246143,6.21933192221197)) ;
#72875=CARTESIAN_POINT('Ctrl Pts',(78.9305921718208,236.315577536009,6.22169251234177)) ;
#72876=CARTESIAN_POINT('Ctrl Pts',(78.9393008450243,236.324904604269,6.22458831777945)) ;
#72877=CARTESIAN_POINT('Ctrl Pts',(78.9508383577829,236.337261385438,6.22842476810926)) ;
#72878=CARTESIAN_POINT('Ctrl Pts',(78.962631711809,236.349096349494,6.2332000270552)) ;
#72879=CARTESIAN_POINT('Ctrl Pts',(78.9745203159935,236.360382813319,6.23871136073391)) ;
#72880=CARTESIAN_POINT('Ctrl Pts',(78.9868854803053,236.3721217002,6.24444361873968)) ;
#72881=CARTESIAN_POINT('Ctrl Pts',(78.9994585165609,236.3833129496,6.25106940511979)) ;
#72882=CARTESIAN_POINT('Ctrl Pts',(79.0120245851066,236.393931577287,6.25830798208034)) ;
#72883=CARTESIAN_POINT('Ctrl Pts',(79.0300218321948,236.409139680403,6.26867514326938)) ;
#72884=CARTESIAN_POINT('Ctrl Pts',(79.0480035991304,236.423170593099,6.28029815534635)) ;
#72885=CARTESIAN_POINT('Ctrl Pts',(79.0659499208125,236.436074634652,6.29304730407198)) ;
#72886=CARTESIAN_POINT('Ctrl Pts',(79.072489055785,236.440776504534,6.29769273536301)) ;
#72887=CARTESIAN_POINT('Ctrl Pts',(79.0790236250942,236.4453292415,6.30248751787712)) ;
#72888=CARTESIAN_POINT('Ctrl Pts',(79.0855531046979,236.449736852335,6.30742486590055)) ;
#72889=CARTESIAN_POINT('Ctrl Pts',(79.1021814237119,236.460961507822,6.31999857820217)) ;
#72890=CARTESIAN_POINT('Ctrl Pts',(79.1187759968485,236.471243033782,6.33349711463422)) ;
#72891=CARTESIAN_POINT('Ctrl Pts',(79.1352093243399,236.480719199796,6.34759111950266)) ;
#72892=CARTESIAN_POINT('Ctrl Pts',(79.1429558612837,236.485186187395,6.3542349187854)) ;
#72893=CARTESIAN_POINT('Ctrl Pts',(79.1506774590654,236.489471680698,6.36102802685583)) ;
#72894=CARTESIAN_POINT('Ctrl Pts',(79.1583626862522,236.493587078316,6.36794168881472)) ;
#72895=CARTESIAN_POINT('Ctrl Pts',(79.1908862082282,236.511003248537,6.3971999828363)) ;
#72896=CARTESIAN_POINT('Ctrl Pts',(79.2227594884558,236.525367080393,6.42861634230867)) ;
#72897=CARTESIAN_POINT('Ctrl Pts',(79.2539716103905,236.537251601533,6.46147697523877)) ;
#72898=CARTESIAN_POINT('Ctrl Pts',(79.2687761578396,236.542888672844,6.47706344515064)) ;
#72899=CARTESIAN_POINT('Ctrl Pts',(79.283431735008,236.547969053286,6.49297500336267)) ;
#72900=CARTESIAN_POINT('Ctrl Pts',(79.2979360861574,236.552559031693,6.50913659697102)) ;
#72901=CARTESIAN_POINT('Ctrl Pts',(79.31936721735,236.559341026172,6.5330164127128)) ;
#72902=CARTESIAN_POINT('Ctrl Pts',(79.3404681642074,236.565051995616,6.55744194205068)) ;
#72903=CARTESIAN_POINT('Ctrl Pts',(79.3612470116278,236.569837451894,6.58226166137312)) ;
#72904=CARTESIAN_POINT('Ctrl Pts',(79.3841739753656,236.575117628428,6.60964724216949)) ;
#72905=CARTESIAN_POINT('Ctrl Pts',(79.4067236213163,236.579243111831,6.63755577298641)) ;
#72906=CARTESIAN_POINT('Ctrl Pts',(79.4289017391005,236.582396378662,6.66580373102021)) ;
#72907=CARTESIAN_POINT('Ctrl Pts',(79.46756525416,236.58789352593,6.71504890869803)) ;
#72908=CARTESIAN_POINT('Ctrl Pts',(79.5050989743834,236.590433394674,6.76532386095455)) ;
#72909=CARTESIAN_POINT('Ctrl Pts',(79.5415950952572,236.590390900578,6.81629650876979)) ;
#72910=CARTESIAN_POINT('Ctrl Pts',(79.5452891117263,236.590386599466,6.82145579134549)) ;
#72911=CARTESIAN_POINT('Ctrl Pts',(79.5489724693669,236.590355875279,6.82662222168512)) ;
#72912=CARTESIAN_POINT('Ctrl Pts',(79.5526452455199,236.590299138915,6.83179545544048)) ;
#72913=CARTESIAN_POINT('Ctrl Pts',(79.5905217161694,236.589714030228,6.88514578999395)) ;
#72914=CARTESIAN_POINT('Ctrl Pts',(79.6272756492694,236.586360149865,6.93921965527791)) ;
#72915=CARTESIAN_POINT('Ctrl Pts',(79.6630047438853,236.580717651161,6.99367465948525)) ;
#72916=CARTESIAN_POINT('Ctrl Pts',(79.6649692503233,236.580407407503,6.99666877975323)) ;
#72917=CARTESIAN_POINT('Ctrl Pts',(79.6669306534082,236.58009025687,6.99966405226983)) ;
#72918=CARTESIAN_POINT('Ctrl Pts',(79.6688889677733,236.579766283224,7.00266042012122)) ;
#72919=CARTESIAN_POINT('Ctrl Pts',(79.6985906537757,236.574852586182,7.04810622731801)) ;
#72920=CARTESIAN_POINT('Ctrl Pts',(79.727564960678,236.568303432379,7.09382942892827)) ;
#72921=CARTESIAN_POINT('Ctrl Pts',(79.7558180615633,236.560235350949,7.13971368291887)) ;
#72922=CARTESIAN_POINT('Ctrl Pts',(79.7625790427186,236.558304655033,7.15069380781977)) ;
#72923=CARTESIAN_POINT('Ctrl Pts',(79.7692985406671,236.556286837037,7.16168309137831)) ;
#72924=CARTESIAN_POINT('Ctrl Pts',(79.775976296469,236.554183244321,7.17267980084166)) ;
#72925=CARTESIAN_POINT('Ctrl Pts',(79.5657826988647,236.44459798751,7.27867958886636)) ;
#72926=CARTESIAN_POINT('Ctrl Pts',(79.4870812400902,236.469851175839,7.10540671867988)) ;
#72927=CARTESIAN_POINT('Ctrl Pts',(79.3728626924325,236.484513827223,6.87572289449329)) ;
#72928=CARTESIAN_POINT('Ctrl Pts',(79.2109449345459,236.451622856973,6.61251963169561)) ;
#72929=CARTESIAN_POINT('Ctrl Pts',(79.1249080993041,236.417892181793,6.49309973646919)) ;
#72930=CARTESIAN_POINT('Ctrl Pts',(79.0530360354225,236.376359946734,6.41122239160556)) ;
#72931=CARTESIAN_POINT('Ctrl Pts',(78.9990126464368,236.336361861471,6.36192444560416)) ;
#72932=CARTESIAN_POINT('Ctrl Pts',(78.908445191216,236.253354919289,6.30168466926149)) ;
#72933=CARTESIAN_POINT('Ctrl Pts',(78.8233604283728,236.115133957597,6.33246528275406)) ;
#72934=CARTESIAN_POINT('Ctrl Pts',(78.7867646631746,235.969017367392,6.46981689000949)) ;
#72935=CARTESIAN_POINT('Ctrl Pts',(78.7776026491497,235.821285683305,6.66032500142642)) ;
#72936=CARTESIAN_POINT('Ctrl Pts',(78.8104263003458,235.66713514265,6.93427995946187)) ;
#72937=CARTESIAN_POINT('Ctrl Pts',(78.8635464513941,235.567087660364,7.16318512434001)) ;
#72938=CARTESIAN_POINT('Ctrl Pts',(78.8957655188746,235.522398454586,7.27867958884211)) ;
#72939=CARTESIAN_POINT('Origin',(78.7335324267296,235.405435110699,16.0213203435596)) ;
#72940=CARTESIAN_POINT('',(78.8957655188746,235.522398454586,16.0254384350469)) ;
#72941=CARTESIAN_POINT('',(78.8957655188746,235.522398454586,16.0213203435596)) ;
#72942=CARTESIAN_POINT('Ctrl Pts',(78.8957655188746,235.522398454586,16.0254384350468)) ;
#72943=CARTESIAN_POINT('Ctrl Pts',(78.9074705870995,235.506163031172,16.0294645582753)) ;
#72944=CARTESIAN_POINT('Ctrl Pts',(78.9162378160954,235.488874504924,16.0362204083692)) ;
#72945=CARTESIAN_POINT('Ctrl Pts',(78.9302389974868,235.448785866273,16.056050217191)) ;
#72946=CARTESIAN_POINT('Ctrl Pts',(78.9336083803761,235.426160755234,16.070223718736)) ;
#72947=CARTESIAN_POINT('Ctrl Pts',(78.9334374035686,235.378695066669,16.1046945816759)) ;
#72948=CARTESIAN_POINT('Ctrl Pts',(78.9282920188754,235.354099131457,16.1258672215769)) ;
#72949=CARTESIAN_POINT('Ctrl Pts',(78.9102244776702,235.308359032661,16.1708720249647)) ;
#72950=CARTESIAN_POINT('Ctrl Pts',(78.8966632779222,235.287149572103,16.1951765216822)) ;
#72951=CARTESIAN_POINT('Ctrl Pts',(78.8794692237515,235.26867652585,16.2199877856675)) ;
#72952=CARTESIAN_POINT('Ctrl Pts',(78.8790049966168,235.2681828224,16.2206540664845)) ;
#72953=CARTESIAN_POINT('Ctrl Pts',(78.8785382749251,235.267691493827,16.2213203435596)) ;
#72954=CARTESIAN_POINT('Origin',(73.474255491572,233.696592446523,16.0213203435596)) ;
#72955=CARTESIAN_POINT('',(73.2742568343815,233.69585956045,16.0254384350468)) ;
#72956=CARTESIAN_POINT('',(73.2742568343815,233.69585956045,16.0213203435596)) ;
#72957=CARTESIAN_POINT('Ctrl Pts',(73.4379069626932,233.499923220541,16.2213203435596)) ;
#72958=CARTESIAN_POINT('Ctrl Pts',(73.4372405812046,233.500046381583,16.2206540664654)) ;
#72959=CARTESIAN_POINT('Ctrl Pts',(73.4365748219496,233.500172930202,16.2199877856881)) ;
#72960=CARTESIAN_POINT('Ctrl Pts',(73.4155453396356,233.50428110497,16.1989219658443)) ;
#72961=CARTESIAN_POINT('Ctrl Pts',(73.3956762915721,233.511452628349,16.1784289743521)) ;
#72962=CARTESIAN_POINT('Ctrl Pts',(73.3593789232627,233.531623989932,16.1396302535154)) ;
#72963=CARTESIAN_POINT('Ctrl Pts',(73.3426362659354,233.544456831755,16.1210537744657)) ;
#72964=CARTESIAN_POINT('Ctrl Pts',(73.3122963096875,233.57704221544,16.0855257632981)) ;
#72965=CARTESIAN_POINT('Ctrl Pts',(73.2987314270749,233.597369350878,16.0684876094865)) ;
#72966=CARTESIAN_POINT('Ctrl Pts',(73.2818489952434,233.638752838189,16.0440628922432)) ;
#72967=CARTESIAN_POINT('Ctrl Pts',(73.2768470238562,233.65827800357,16.0353723462229)) ;
#72968=CARTESIAN_POINT('Ctrl Pts',(73.2745340907024,233.684665512636,16.027919277051)) ;
#72969=CARTESIAN_POINT('Ctrl Pts',(73.2742773990004,233.690247642977,16.0265673132454)) ;
#72970=CARTESIAN_POINT('Ctrl Pts',(73.2742568343815,233.69585956045,16.0254384350468)) ;
#72971=CARTESIAN_POINT('Origin',(74.5283628290597,239.4,7.2786795888419)) ;
#72972=CARTESIAN_POINT('Origin',(74.5283628290597,239.4,7.17267980084126)) ;
#72973=CARTESIAN_POINT('Origin',(79.6268886667016,236.635034487937,16.0213203435596)) ;
#72974=CARTESIAN_POINT('',(79.5657826988536,236.444597987514,16.0254384350469)) ;
#72975=CARTESIAN_POINT('',(79.5657826988536,236.444597987514,16.0213203435596)) ;
#72976=CARTESIAN_POINT('Ctrl Pts',(79.8026999024824,236.53969084959,16.2213203435596)) ;
#72977=CARTESIAN_POINT('Ctrl Pts',(79.802376846175,236.539095142004,16.2206540664836)) ;
#72978=CARTESIAN_POINT('Ctrl Pts',(79.8020507603675,236.538501073009,16.2199877856673)) ;
#72979=CARTESIAN_POINT('Ctrl Pts',(79.7916451864779,236.519770342471,16.1989219660218)) ;
#72980=CARTESIAN_POINT('Ctrl Pts',(79.7786847889848,236.503089877563,16.1784289743296)) ;
#72981=CARTESIAN_POINT('Ctrl Pts',(79.7482841804216,236.474802322421,16.1396302534665)) ;
#72982=CARTESIAN_POINT('Ctrl Pts',(79.7309056569223,236.462844675276,16.1210537744064)) ;
#72983=CARTESIAN_POINT('Ctrl Pts',(79.6905395533259,236.444059099522,16.0855257632409)) ;
#72984=CARTESIAN_POINT('Ctrl Pts',(79.6670155194585,236.437439559828,16.0684876094397)) ;
#72985=CARTESIAN_POINT('Ctrl Pts',(79.6224405258492,236.434171613905,16.0440628922132)) ;
#72986=CARTESIAN_POINT('Ctrl Pts',(79.6023252959214,236.43544806435,16.0353723461999)) ;
#72987=CARTESIAN_POINT('Ctrl Pts',(79.5765145478479,236.441402522945,16.0279192770416)) ;
#72988=CARTESIAN_POINT('Ctrl Pts',(79.5711263043329,236.442883367765,16.0265673132415)) ;
#72989=CARTESIAN_POINT('Ctrl Pts',(79.5657826988536,236.444597987514,16.0254384350468)) ;
#72990=CARTESIAN_POINT('Origin',(74.5283628290597,239.4,16.2213203435596)) ;
#72991=CARTESIAN_POINT('',(78.8725506972158,235.557080307089,16.0213203435596)) ;
#72992=CARTESIAN_POINT('Ctrl Pts',(78.8957655188745,235.522398454586,16.0254384350468)) ;
#72993=CARTESIAN_POINT('Ctrl Pts',(78.8893108232296,235.531351389741,16.0232182514845)) ;
#72994=CARTESIAN_POINT('Ctrl Pts',(78.8829899514931,235.540642081367,16.0218983740811)) ;
#72995=CARTESIAN_POINT('Ctrl Pts',(78.8754205773507,235.552487135842,16.0213707571522)) ;
#72996=CARTESIAN_POINT('Ctrl Pts',(78.8739772719456,235.554779827169,16.0213203435596)) ;
#72997=CARTESIAN_POINT('Ctrl Pts',(78.8725506972157,235.557080307089,16.0213203435596)) ;
#72998=CARTESIAN_POINT('',(79.5256245226196,236.455959313107,16.0213203435596)) ;
#72999=CARTESIAN_POINT('Origin',(74.5283628290597,239.4,16.0213203435596)) ;
#73000=CARTESIAN_POINT('Ctrl Pts',(79.5256245226197,236.455959313107,16.0213203435596)) ;
#73001=CARTESIAN_POINT('Ctrl Pts',(79.5365793331501,236.453267763066,16.0213203435596)) ;
#73002=CARTESIAN_POINT('Ctrl Pts',(79.5474616517457,236.450264794855,16.0221950109068)) ;
#73003=CARTESIAN_POINT('Ctrl Pts',(79.560731310064,236.446200502444,16.0244263118334)) ;
#73004=CARTESIAN_POINT('Ctrl Pts',(79.5632664280307,236.445405391366,16.0249068532759)) ;
#73005=CARTESIAN_POINT('Ctrl Pts',(79.5657826988536,236.444597987514,16.0254384350468)) ;
#73006=CARTESIAN_POINT('Origin',(72.0287747312355,234.166257616082,16.0213203435596)) ;
#73007=CARTESIAN_POINT('',(72.1901462641291,234.048108437619,16.0254384350468)) ;
#73008=CARTESIAN_POINT('',(72.1901462641291,234.048108437619,16.0213203435596)) ;
#73009=CARTESIAN_POINT('Ctrl Pts',(72.1901462641291,234.048108437619,16.0254384350468)) ;
#73010=CARTESIAN_POINT('Ctrl Pts',(72.1783225238984,234.031959234464,16.0294645582753)) ;
#73011=CARTESIAN_POINT('Ctrl Pts',(72.1645893811064,234.018278655779,16.0362204083691)) ;
#73012=CARTESIAN_POINT('Ctrl Pts',(72.1307894230788,233.992574670357,16.056050217191)) ;
#73013=CARTESIAN_POINT('Ctrl Pts',(72.1103128603666,233.982378652993,16.0702237187361)) ;
#73014=CARTESIAN_POINT('Ctrl Pts',(72.0651174732175,233.967873557184,16.1046945816758)) ;
#73015=CARTESIAN_POINT('Ctrl Pts',(72.0401353374473,233.965166546852,16.1258672215766)) ;
#73016=CARTESIAN_POINT('Ctrl Pts',(71.9910507411521,233.968215331796,16.1708720249644)) ;
#73017=CARTESIAN_POINT('Ctrl Pts',(71.9666887043084,233.974558715426,16.1951765216982)) ;
#73018=CARTESIAN_POINT('Ctrl Pts',(71.9438065383368,233.985202747463,16.2199877856666)) ;
#73019=CARTESIAN_POINT('Ctrl Pts',(71.9431935443829,233.985491690948,16.2206540664842)) ;
#73020=CARTESIAN_POINT('Ctrl Pts',(71.942582038207,233.985783740775,16.2213203435596)) ;
#73021=CARTESIAN_POINT('Origin',(74.5283628290597,239.4,16.2213203435596)) ;
#73022=CARTESIAN_POINT('',(72.2159568915352,234.080904326852,16.0213203435596)) ;
#73023=CARTESIAN_POINT('Ctrl Pts',(72.1901462641291,234.048108437619,16.0254384350468)) ;
#73024=CARTESIAN_POINT('Ctrl Pts',(72.1966664008005,234.057013827085,16.0232182514845)) ;
#73025=CARTESIAN_POINT('Ctrl Pts',(72.2035491168268,234.065896314941,16.0218983740811)) ;
#73026=CARTESIAN_POINT('Ctrl Pts',(72.2124753678236,234.076755540675,16.0213707571522)) ;
#73027=CARTESIAN_POINT('Ctrl Pts',(72.2142098409518,234.078836686269,16.0213203435596)) ;
#73028=CARTESIAN_POINT('Ctrl Pts',(72.2159568915352,234.080904326852,16.0213203435596)) ;
#73029=CARTESIAN_POINT('',(73.2726525382014,233.737563098327,16.0213203435596)) ;
#73030=CARTESIAN_POINT('Origin',(74.5283628290597,239.4,16.0213203435596)) ;
#73031=CARTESIAN_POINT('Ctrl Pts',(73.2726525382014,233.737563098327,16.0213203435596)) ;
#73032=CARTESIAN_POINT('Ctrl Pts',(73.2734779446195,233.726312719683,16.0213203435596)) ;
#73033=CARTESIAN_POINT('Ctrl Pts',(73.2739847735191,233.71503505146,16.0221950109068)) ;
#73034=CARTESIAN_POINT('Ctrl Pts',(73.2742199516675,233.701158921022,16.0244263118334)) ;
#73035=CARTESIAN_POINT('Ctrl Pts',(73.2742471506295,233.698502177724,16.0249068532759)) ;
#73036=CARTESIAN_POINT('Ctrl Pts',(73.2742568343815,233.69585956045,16.0254384350468)) ;
#73037=CARTESIAN_POINT('Ctrl Pts',(80.2332466613993,238.145896286595,7.28036629650082)) ;
#73038=CARTESIAN_POINT('Ctrl Pts',(80.1779056493182,238.145761083795,7.16431451492221)) ;
#73039=CARTESIAN_POINT('Ctrl Pts',(80.0654939997404,238.13039472435,6.93452072658987)) ;
#73040=CARTESIAN_POINT('Ctrl Pts',(79.921484160325,238.065724505406,6.66105185594091)) ;
#73041=CARTESIAN_POINT('Ctrl Pts',(79.8070585153582,237.972192585025,6.46924290901652)) ;
#73042=CARTESIAN_POINT('Ctrl Pts',(79.7385408827141,237.888743471261,6.37322093548194)) ;
#73043=CARTESIAN_POINT('Ctrl Pts',(79.6911769183589,237.803443935991,6.32731325641336)) ;
#73044=CARTESIAN_POINT('Ctrl Pts',(79.6626235218602,237.731818472063,6.31494132977146)) ;
#73045=CARTESIAN_POINT('Ctrl Pts',(79.6436095797225,237.657062576281,6.32730080160491)) ;
#73046=CARTESIAN_POINT('Ctrl Pts',(79.6317837391258,237.560234835217,6.37317692639864)) ;
#73047=CARTESIAN_POINT('Ctrl Pts',(79.638186797208,237.452382843011,6.46930294056729)) ;
#73048=CARTESIAN_POINT('Ctrl Pts',(79.6757637756622,237.309451563678,6.66107036149359)) ;
#73049=CARTESIAN_POINT('Ctrl Pts',(79.7542618476727,237.17249003623,6.93454557156964)) ;
#73050=CARTESIAN_POINT('Ctrl Pts',(79.8361608473108,237.093983531712,7.16431122291373)) ;
#73051=CARTESIAN_POINT('Ctrl Pts',(79.8808544858649,237.061344621366,7.28036634298531)) ;
#73052=CARTESIAN_POINT('Ctrl Pts',(80.2787215482779,238.145985700087,7.25145031090427)) ;
#73053=CARTESIAN_POINT('Ctrl Pts',(80.2205756685247,238.150146686166,7.13668815450591)) ;
#73054=CARTESIAN_POINT('Ctrl Pts',(80.1008696697319,238.141739542913,6.90908133772489)) ;
#73055=CARTESIAN_POINT('Ctrl Pts',(79.9446522226815,238.080894675372,6.6376698933697)) ;
#73056=CARTESIAN_POINT('Ctrl Pts',(79.8195172933758,237.985666275976,6.44712617479323)) ;
#73057=CARTESIAN_POINT('Ctrl Pts',(79.7445014978107,237.898473504043,6.35169067773445)) ;
#73058=CARTESIAN_POINT('Ctrl Pts',(79.692949166172,237.808172185119,6.30605438286228)) ;
#73059=CARTESIAN_POINT('Ctrl Pts',(79.6622096829835,237.731957089376,6.29375467249613)) ;
#73060=CARTESIAN_POINT('Ctrl Pts',(79.6422616441879,237.652190302909,6.30604200388241)) ;
#73061=CARTESIAN_POINT('Ctrl Pts',(79.6308854350235,237.548863326753,6.35164689420351)) ;
#73062=CARTESIAN_POINT('Ctrl Pts',(79.6403413094888,237.434133119528,6.44718596070129)) ;
#73063=CARTESIAN_POINT('Ctrl Pts',(79.6855942151938,237.28356807379,6.63768828531303)) ;
#73064=CARTESIAN_POINT('Ctrl Pts',(79.7762110553406,237.142507839417,6.90910610037119)) ;
#73065=CARTESIAN_POINT('Ctrl Pts',(79.8681037039669,237.065354698581,7.13668489810488)) ;
#73066=CARTESIAN_POINT('Ctrl Pts',(79.9175918880526,237.034542816821,7.25145035687956)) ;
#73067=CARTESIAN_POINT('Ctrl Pts',(80.3576208772263,238.186433078335,7.2012216783622)) ;
#73068=CARTESIAN_POINT('Ctrl Pts',(80.2910222038791,238.19295252776,7.0885508192026)) ;
#73069=CARTESIAN_POINT('Ctrl Pts',(80.1541383715028,238.186858411812,6.86454783277039)) ;
#73070=CARTESIAN_POINT('Ctrl Pts',(79.9760850814639,238.121396473258,6.59660334624683)) ;
#73071=CARTESIAN_POINT('Ctrl Pts',(79.8340166470322,238.016395912876,6.40822171016601)) ;
#73072=CARTESIAN_POINT('Ctrl Pts',(79.7491197147048,237.919514622506,6.3137962441714)) ;
#73073=CARTESIAN_POINT('Ctrl Pts',(79.6910247264725,237.818879034461,6.26862916485266)) ;
#73074=CARTESIAN_POINT('Ctrl Pts',(79.6565506977968,237.733801201014,6.25645441418595)) ;
#73075=CARTESIAN_POINT('Ctrl Pts',(79.6344168175111,237.644678443685,6.26861687996125)) ;
#73076=CARTESIAN_POINT('Ctrl Pts',(79.6222554874394,237.529139719225,6.31375285214006)) ;
#73077=CARTESIAN_POINT('Ctrl Pts',(79.6340236296205,237.400781569794,6.40828085240387)) ;
#73078=CARTESIAN_POINT('Ctrl Pts',(79.6872152287998,237.232315543738,6.59662176807364)) ;
#73079=CARTESIAN_POINT('Ctrl Pts',(79.7927919971073,237.074708318493,6.86457238457136)) ;
#73080=CARTESIAN_POINT('Ctrl Pts',(79.8999352530856,236.989316632693,7.08854762092014)) ;
#73081=CARTESIAN_POINT('Ctrl Pts',(79.9576484170219,236.955444337705,7.20122172350898)) ;
#73082=CARTESIAN_POINT('Ctrl Pts',(80.3943740298942,238.275157533004,7.17771948055087)) ;
#73083=CARTESIAN_POINT('Ctrl Pts',(80.3217995712605,238.27685019025,7.06324269887043)) ;
#73084=CARTESIAN_POINT('Ctrl Pts',(80.1739876651028,238.259964231434,6.83622602504918)) ;
#73085=CARTESIAN_POINT('Ctrl Pts',(79.9838492644881,238.177623628403,6.56553634319181)) ;
#73086=CARTESIAN_POINT('Ctrl Pts',(79.8324519761851,238.055644168661,6.37550114619807)) ;
#73087=CARTESIAN_POINT('Ctrl Pts',(79.7417046853161,237.945935908136,6.2803204097403)) ;
#73088=CARTESIAN_POINT('Ctrl Pts',(79.6789846091568,237.833401386599,6.23480589058125)) ;
#73089=CARTESIAN_POINT('Ctrl Pts',(79.6412127236151,237.738789039827,6.22253899168853)) ;
#73090=CARTESIAN_POINT('Ctrl Pts',(79.6161413587739,237.64001091775,6.23479354036237)) ;
#73091=CARTESIAN_POINT('Ctrl Pts',(79.6007280971451,237.512129301313,6.28027674251987)) ;
#73092=CARTESIAN_POINT('Ctrl Pts',(79.6096888129855,237.369948564794,6.37556075156494)) ;
#73093=CARTESIAN_POINT('Ctrl Pts',(79.6604473857773,237.182263486407,6.56555470566056)) ;
#73094=CARTESIAN_POINT('Ctrl Pts',(79.7658801251764,237.003897576842,6.83625071485809)) ;
#73095=CARTESIAN_POINT('Ctrl Pts',(79.8755208020787,236.903351717062,7.06323945062391)) ;
#73096=CARTESIAN_POINT('Ctrl Pts',(79.935231416945,236.862061782038,7.1777195264114)) ;
#73097=CARTESIAN_POINT('Ctrl Pts',(80.3996002740789,238.315077942443,7.17433670364794)) ;
#73098=CARTESIAN_POINT('Ctrl Pts',(80.325736250402,238.314513145266,7.05828625130696)) ;
#73099=CARTESIAN_POINT('Ctrl Pts',(80.1755857959063,238.292645299654,6.82849471713331)) ;
#73100=CARTESIAN_POINT('Ctrl Pts',(79.9827966599848,238.202695250306,6.55502796713346)) ;
#73101=CARTESIAN_POINT('Ctrl Pts',(79.8290739463553,238.073144136735,6.36322032432285)) ;
#73102=CARTESIAN_POINT('Ctrl Pts',(79.7366319322547,237.957784921701,6.26719895529102)) ;
#73103=CARTESIAN_POINT('Ctrl Pts',(79.6723150856581,237.84008129077,6.22129155594843)) ;
#73104=CARTESIAN_POINT('Ctrl Pts',(79.6332390648588,237.741381732928,6.20891970374262)) ;
#73105=CARTESIAN_POINT('Ctrl Pts',(79.6068193628199,237.638527187785,6.22127910121813)) ;
#73106=CARTESIAN_POINT('Ctrl Pts',(79.5896603331735,237.505527120618,6.26715494644022)) ;
#73107=CARTESIAN_POINT('Ctrl Pts',(79.5966681821472,237.357772061383,6.36328035562036)) ;
#73108=CARTESIAN_POINT('Ctrl Pts',(79.6448593894507,237.162600361155,6.55504647256913)) ;
#73109=CARTESIAN_POINT('Ctrl Pts',(79.7479629649841,236.976517066737,6.82851956202821)) ;
#73110=CARTESIAN_POINT('Ctrl Pts',(79.8565679236955,236.870567902859,7.05828295933517)) ;
#73111=CARTESIAN_POINT('Ctrl Pts',(79.9159949092403,236.826693582052,7.17433675013192)) ;
#73112=CARTESIAN_POINT('Ctrl Pts',(79.9151467531554,236.82732064467,7.17267980084143)) ;
#73113=CARTESIAN_POINT('Ctrl Pts',(79.8560499536753,236.871073595961,7.05718689587997)) ;
#73114=CARTESIAN_POINT('Ctrl Pts',(79.7477661218197,236.976872333025,6.82799745299379)) ;
#73115=CARTESIAN_POINT('Ctrl Pts',(79.6448593894507,237.162600361155,6.55504647256913)) ;
#73116=CARTESIAN_POINT('Ctrl Pts',(79.5966681821471,237.357772061383,6.36328035562036)) ;
#73117=CARTESIAN_POINT('Ctrl Pts',(79.5896603331735,237.505527120618,6.26715494644023)) ;
#73118=CARTESIAN_POINT('Ctrl Pts',(79.6068193628199,237.638527187785,6.22127910121812)) ;
#73119=CARTESIAN_POINT('Ctrl Pts',(79.6332390648588,237.741381732928,6.20891970374263)) ;
#73120=CARTESIAN_POINT('Ctrl Pts',(79.672315085658,237.84008129077,6.22129155594842)) ;
#73121=CARTESIAN_POINT('Ctrl Pts',(79.7366319322548,237.9577849217,6.26719895529104)) ;
#73122=CARTESIAN_POINT('Ctrl Pts',(79.8290739463553,238.073144136735,6.36322032432284)) ;
#73123=CARTESIAN_POINT('Ctrl Pts',(79.9827966599849,238.202695250307,6.55502796713348)) ;
#73124=CARTESIAN_POINT('Ctrl Pts',(80.1752177269682,238.292473568924,6.82797262020198)) ;
#73125=CARTESIAN_POINT('Ctrl Pts',(80.325019908484,238.314408535778,7.05719005380891)) ;
#73126=CARTESIAN_POINT('Ctrl Pts',(80.398545552619,238.31506917167,7.17267980084126)) ;
#73127=CARTESIAN_POINT('Ctrl Pts',(80.232503268608,238.145894005322,7.27867958883789)) ;
#73128=CARTESIAN_POINT('Ctrl Pts',(80.2105890887182,238.145813701796,7.2327390460971)) ;
#73129=CARTESIAN_POINT('Ctrl Pts',(80.1885289438461,238.144536258816,7.1869379140836)) ;
#73130=CARTESIAN_POINT('Ctrl Pts',(80.1663213133667,238.141988707811,7.14139165811073)) ;
#73131=CARTESIAN_POINT('Ctrl Pts',(80.1449425970939,238.139536245799,7.09754544567358)) ;
#73132=CARTESIAN_POINT('Ctrl Pts',(80.1234263498375,238.135906341529,7.05393543754444)) ;
#73133=CARTESIAN_POINT('Ctrl Pts',(80.1017950450755,238.130992693427,7.01066464617939)) ;
#73134=CARTESIAN_POINT('Ctrl Pts',(80.0894090875243,238.128179167498,6.98588804620328)) ;
#73135=CARTESIAN_POINT('Ctrl Pts',(80.0769859110699,238.124944008106,6.96122266319468)) ;
#73136=CARTESIAN_POINT('Ctrl Pts',(80.0645351246606,238.121261622656,6.93668783599072)) ;
#73137=CARTESIAN_POINT('Ctrl Pts',(80.0470380349159,238.116086766502,6.9022090441019)) ;
#73138=CARTESIAN_POINT('Ctrl Pts',(80.0295043160675,238.110037081132,6.86798808269392)) ;
#73139=CARTESIAN_POINT('Ctrl Pts',(80.0119134699705,238.103002425664,6.83420441808968)) ;
#73140=CARTESIAN_POINT('Ctrl Pts',(79.9948101708734,238.096162742351,6.80135709982332)) ;
#73141=CARTESIAN_POINT('Ctrl Pts',(79.9776522080704,238.088391577647,6.76892317408853)) ;
#73142=CARTESIAN_POINT('Ctrl Pts',(79.9604560297924,238.079554466258,6.73706759473268)) ;
#73143=CARTESIAN_POINT('Ctrl Pts',(79.9440162918452,238.071106089352,6.70661330609378)) ;
#73144=CARTESIAN_POINT('Ctrl Pts',(79.9275411472763,238.061682998992,6.6766876013464)) ;
#73145=CARTESIAN_POINT('Ctrl Pts',(79.9110856389802,238.051143022085,6.64743460946756)) ;
#73146=CARTESIAN_POINT('Ctrl Pts',(79.9050048912538,238.04724822045,6.636624851382)) ;
#73147=CARTESIAN_POINT('Ctrl Pts',(79.8989272739401,238.043200693744,6.62590695216758)) ;
#73148=CARTESIAN_POINT('Ctrl Pts',(79.8928572709278,238.038992579685,6.61528818440181)) ;
#73149=CARTESIAN_POINT('Ctrl Pts',(79.8785195831937,238.029052778139,6.5902060590653)) ;
#73150=CARTESIAN_POINT('Ctrl Pts',(79.8642201091082,238.018219074385,6.56567701872138)) ;
#73151=CARTESIAN_POINT('Ctrl Pts',(79.8499884620884,238.006327778712,6.54202098106688)) ;
#73152=CARTESIAN_POINT('Ctrl Pts',(79.8369505446297,237.995433907381,6.52034917695921)) ;
#73153=CARTESIAN_POINT('Ctrl Pts',(79.8239694641037,237.983651754103,6.49941006528887)) ;
#73154=CARTESIAN_POINT('Ctrl Pts',(79.81111401836,237.970837186803,6.4794496247295)) ;
#73155=CARTESIAN_POINT('Ctrl Pts',(79.8099369955991,237.969663906803,6.47762208072021)) ;
#73156=CARTESIAN_POINT('Ctrl Pts',(79.8087610611517,237.968481962524,6.47580274083484)) ;
#73157=CARTESIAN_POINT('Ctrl Pts',(79.8075862896947,237.967291237912,6.47399179386844)) ;
#73158=CARTESIAN_POINT('Ctrl Pts',(79.7946368721481,237.954165969941,6.45402986145733)) ;
#73159=CARTESIAN_POINT('Ctrl Pts',(79.7818294946238,237.939978518983,6.43508770960375)) ;
#73160=CARTESIAN_POINT('Ctrl Pts',(79.7693189745583,237.924604658638,6.41771185041663)) ;
#73161=CARTESIAN_POINT('Ctrl Pts',(79.7573739014043,237.909925661641,6.40112134034855)) ;
#73162=CARTESIAN_POINT('Ctrl Pts',(79.7456993800576,237.894164456387,6.38595873692502)) ;
#73163=CARTESIAN_POINT('Ctrl Pts',(79.734477336668,237.877221681256,6.37269974779979)) ;
#73164=CARTESIAN_POINT('Ctrl Pts',(79.7320288211619,237.873524970578,6.36980679512248)) ;
#73165=CARTESIAN_POINT('Ctrl Pts',(79.7296020341664,237.869772065423,6.36700446593625)) ;
#73166=CARTESIAN_POINT('Ctrl Pts',(79.7271991867293,237.865962041082,6.36429770144624)) ;
#73167=CARTESIAN_POINT('Ctrl Pts',(79.7179557275126,237.851305345006,6.35388511062318)) ;
#73168=CARTESIAN_POINT('Ctrl Pts',(79.7090655087212,237.835794327468,6.34488673059512)) ;
#73169=CARTESIAN_POINT('Ctrl Pts',(79.7007366393481,237.819542094098,6.33775032301849)) ;
#73170=CARTESIAN_POINT('Ctrl Pts',(79.6978250063942,237.813860586064,6.3352555546962)) ;
#73171=CARTESIAN_POINT('Ctrl Pts',(79.6949817107896,237.808088873185,6.33298833509643)) ;
#73172=CARTESIAN_POINT('Ctrl Pts',(79.6922146951874,237.802232977728,6.33096779349927)) ;
#73173=CARTESIAN_POINT('Ctrl Pts',(79.685607945018,237.788250968276,6.32614338501776)) ;
#73174=CARTESIAN_POINT('Ctrl Pts',(79.6794383233117,237.773784668057,6.32272529272555)) ;
#73175=CARTESIAN_POINT('Ctrl Pts',(79.6738226135057,237.759004570215,6.3208188962173)) ;
#73176=CARTESIAN_POINT('Ctrl Pts',(79.6703584983877,237.749887297038,6.31964291362681)) ;
#73177=CARTESIAN_POINT('Ctrl Pts',(79.6671043092355,237.740651177896,6.31904215864043)) ;
#73178=CARTESIAN_POINT('Ctrl Pts',(79.6640785278978,237.731340576308,6.31904136669014)) ;
#73179=CARTESIAN_POINT('Ctrl Pts',(79.6592031178307,237.716338500596,6.31904009062887)) ;
#73180=CARTESIAN_POINT('Ctrl Pts',(79.6549226304001,237.701140110227,6.320596471147)) ;
#73181=CARTESIAN_POINT('Ctrl Pts',(79.6512755675814,237.685946894271,6.32360659801529)) ;
#73182=CARTESIAN_POINT('Ctrl Pts',(79.6489898975475,237.676425073519,6.32549309054995)) ;
#73183=CARTESIAN_POINT('Ctrl Pts',(79.6469519912017,237.666905579811,6.3279505740265)) ;
#73184=CARTESIAN_POINT('Ctrl Pts',(79.6451610148983,237.65743956484,6.33095347029228)) ;
#73185=CARTESIAN_POINT('Ctrl Pts',(79.6416859636402,237.63907255062,6.33678002334399)) ;
#73186=CARTESIAN_POINT('Ctrl Pts',(79.6391416762444,237.620904336649,6.34465995043934)) ;
#73187=CARTESIAN_POINT('Ctrl Pts',(79.6374400792673,237.603154347333,6.35413826247109)) ;
#73188=CARTESIAN_POINT('Ctrl Pts',(79.636865391497,237.597159566008,6.35733941414242)) ;
#73189=CARTESIAN_POINT('Ctrl Pts',(79.6363863970514,237.591212363634,6.36072288479166)) ;
#73190=CARTESIAN_POINT('Ctrl Pts',(79.6359984527991,237.585320745256,6.36427114664549)) ;
#73191=CARTESIAN_POINT('Ctrl Pts',(79.6346378491189,237.56465757626,6.37671566182321)) ;
#73192=CARTESIAN_POINT('Ctrl Pts',(79.6343934893251,237.544671891111,6.39118719995713)) ;
#73193=CARTESIAN_POINT('Ctrl Pts',(79.635052067383,237.525403008395,6.40720016389703)) ;
#73194=CARTESIAN_POINT('Ctrl Pts',(79.6357409542367,237.505247341453,6.42395006957119)) ;
#73195=CARTESIAN_POINT('Ctrl Pts',(79.6374174274326,237.485875364109,6.44238654343785)) ;
#73196=CARTESIAN_POINT('Ctrl Pts',(79.6398737272436,237.467288791444,6.46195381172284)) ;
#73197=CARTESIAN_POINT('Ctrl Pts',(79.640373191123,237.463509398697,6.46593261906739)) ;
#73198=CARTESIAN_POINT('Ctrl Pts',(79.6409050234786,237.459762360674,6.46995818152148)) ;
#73199=CARTESIAN_POINT('Ctrl Pts',(79.641467668486,237.456047520528,6.47402582640356)) ;
#73200=CARTESIAN_POINT('Ctrl Pts',(79.6441978400383,237.438021676959,6.49376361523447)) ;
#73201=CARTESIAN_POINT('Ctrl Pts',(79.6476484287426,237.420762531615,6.51449226275907)) ;
#73202=CARTESIAN_POINT('Ctrl Pts',(79.6516751685792,237.404194825731,6.53597044669148)) ;
#73203=CARTESIAN_POINT('Ctrl Pts',(79.6558787868921,237.386899367201,6.55839208080987)) ;
#73204=CARTESIAN_POINT('Ctrl Pts',(79.6607103239457,237.370356714021,6.58163054579619)) ;
#73205=CARTESIAN_POINT('Ctrl Pts',(79.6660597149526,237.3544664928,6.60541130107295)) ;
#73206=CARTESIAN_POINT('Ctrl Pts',(79.6668004767532,237.352266079918,6.60870436285804)) ;
#73207=CARTESIAN_POINT('Ctrl Pts',(79.6675512491336,237.35007816528,6.61200782337307)) ;
#73208=CARTESIAN_POINT('Ctrl Pts',(79.6683118158661,237.347902472685,6.61532095361514)) ;
#73209=CARTESIAN_POINT('Ctrl Pts',(79.6749594114975,237.328886226022,6.64427876780854)) ;
#73210=CARTESIAN_POINT('Ctrl Pts',(79.6823510456142,237.310804268716,6.67397528311282)) ;
#73211=CARTESIAN_POINT('Ctrl Pts',(79.6903365250355,237.293576196946,6.70426237962481)) ;
#73212=CARTESIAN_POINT('Ctrl Pts',(79.6985670842247,237.275819383993,6.73547900762635)) ;
#73213=CARTESIAN_POINT('Ctrl Pts',(79.707428720787,237.258968872542,6.76732302378836)) ;
#73214=CARTESIAN_POINT('Ctrl Pts',(79.7168128848841,237.242927836814,6.7996322476753)) ;
#73215=CARTESIAN_POINT('Ctrl Pts',(79.7265781104582,237.226235424926,6.83325344782879)) ;
#73216=CARTESIAN_POINT('Ctrl Pts',(79.7369093968226,237.210418788751,6.86737840405015)) ;
#73217=CARTESIAN_POINT('Ctrl Pts',(79.7477405814739,237.195371789186,6.90182436586147)) ;
#73218=CARTESIAN_POINT('Ctrl Pts',(79.7513857712113,237.190307784632,6.91341700974418)) ;
#73219=CARTESIAN_POINT('Ctrl Pts',(79.7550880189685,237.185331027006,6.92504601170794)) ;
#73220=CARTESIAN_POINT('Ctrl Pts',(79.7588460733137,237.180437766862,6.93670440563104)) ;
#73221=CARTESIAN_POINT('Ctrl Pts',(79.7725748310283,237.162561925596,6.97929433403692)) ;
#73222=CARTESIAN_POINT('Ctrl Pts',(79.7870252383589,237.145825256622,7.02227651420834)) ;
#73223=CARTESIAN_POINT('Ctrl Pts',(79.8020894436934,237.130149985728,7.06555117398127)) ;
#73224=CARTESIAN_POINT('Ctrl Pts',(79.8177535740407,237.113850454419,7.11054922707215)) ;
#73225=CARTESIAN_POINT('Ctrl Pts',(79.8340818004957,237.09869761457,7.15586351936518)) ;
#73226=CARTESIAN_POINT('Ctrl Pts',(79.8510076139652,237.084618645229,7.20138187753961)) ;
#73227=CARTESIAN_POINT('Ctrl Pts',(79.8605668598529,237.076667220618,7.22708942648398)) ;
#73228=CARTESIAN_POINT('Ctrl Pts',(79.8703176608738,237.069058674587,7.25286206607173)) ;
#73229=CARTESIAN_POINT('Ctrl Pts',(79.8802543914393,237.06178343507,7.27867958883835)) ;
#73230=CARTESIAN_POINT('Origin',(79.7621052129773,236.900411902176,16.0213203435596)) ;
#73231=CARTESIAN_POINT('',(79.8802543914407,237.061783435069,16.0254384350469)) ;
#73232=CARTESIAN_POINT('',(79.8802543914407,237.061783435069,16.0213203435596)) ;
#73233=CARTESIAN_POINT('Ctrl Pts',(79.8802543914407,237.061783435069,16.0254384350469)) ;
#73234=CARTESIAN_POINT('Ctrl Pts',(79.8964035945954,237.049959694839,16.0294645582753)) ;
#73235=CARTESIAN_POINT('Ctrl Pts',(79.9100841732802,237.036226552047,16.0362204083692)) ;
#73236=CARTESIAN_POINT('Ctrl Pts',(79.9357881587029,237.002426594019,16.056050217191)) ;
#73237=CARTESIAN_POINT('Ctrl Pts',(79.9459841760662,236.981950031307,16.070223718736)) ;
#73238=CARTESIAN_POINT('Ctrl Pts',(79.9604892718756,236.936754644158,16.1046945816758)) ;
#73239=CARTESIAN_POINT('Ctrl Pts',(79.9631962822073,236.911772508388,16.1258672215767)) ;
#73240=CARTESIAN_POINT('Ctrl Pts',(79.9601474972632,236.862687912092,16.1708720249643)) ;
#73241=CARTESIAN_POINT('Ctrl Pts',(79.9538041136321,236.838325875245,16.195176521693)) ;
#73242=CARTESIAN_POINT('Ctrl Pts',(79.9431600815964,236.815443709278,16.2199877856673)) ;
#73243=CARTESIAN_POINT('Ctrl Pts',(79.9428711381123,236.814830715324,16.2206540664837)) ;
#73244=CARTESIAN_POINT('Ctrl Pts',(79.9425790882848,236.814219209147,16.2213203435596)) ;
#73245=CARTESIAN_POINT('Origin',(71.7633973169967,234.301474162358,16.0213203435596)) ;
#73246=CARTESIAN_POINT('',(71.5729608165738,234.362580130206,16.0254384350468)) ;
#73247=CARTESIAN_POINT('',(71.5729608165738,234.362580130206,16.0213203435596)) ;
#73248=CARTESIAN_POINT('Ctrl Pts',(71.6680536786497,234.125662926577,16.2213203435596)) ;
#73249=CARTESIAN_POINT('Ctrl Pts',(71.6674579710607,234.125985982886,16.22065406648)) ;
#73250=CARTESIAN_POINT('Ctrl Pts',(71.6668639020618,234.126312068696,16.2199877856681)) ;
#73251=CARTESIAN_POINT('Ctrl Pts',(71.6481331715546,234.136717642569,16.19892196599)) ;
#73252=CARTESIAN_POINT('Ctrl Pts',(71.6314527066269,234.149678040072,16.1784289743351)) ;
#73253=CARTESIAN_POINT('Ctrl Pts',(71.6031651514905,234.180078648626,16.1396302534806)) ;
#73254=CARTESIAN_POINT('Ctrl Pts',(71.5912075043469,234.19745717212,16.1210537744242)) ;
#73255=CARTESIAN_POINT('Ctrl Pts',(71.5724219285888,234.23782327571,16.0855257632587)) ;
#73256=CARTESIAN_POINT('Ctrl Pts',(71.5658023888919,234.261347309579,16.0684876094541)) ;
#73257=CARTESIAN_POINT('Ctrl Pts',(71.5625344429639,234.305922303191,16.0440628922224)) ;
#73258=CARTESIAN_POINT('Ctrl Pts',(71.5638108934068,234.326037533119,16.035372346207)) ;
#73259=CARTESIAN_POINT('Ctrl Pts',(71.5697653520014,234.3518482812,16.0279192770445)) ;
#73260=CARTESIAN_POINT('Ctrl Pts',(71.5712461968226,234.357236524721,16.0265673132427)) ;
#73261=CARTESIAN_POINT('Ctrl Pts',(71.5729608165737,234.362580130206,16.0254384350468)) ;
#73262=CARTESIAN_POINT('Origin',(74.5283628290597,239.4,7.2786795888419)) ;
#73263=CARTESIAN_POINT('Origin',(74.5283628290597,239.4,7.17267980084126)) ;
#73264=CARTESIAN_POINT('Origin',(80.2317703825363,238.345892662512,16.0213203435596)) ;
#73265=CARTESIAN_POINT('',(80.2325032686099,238.145894005322,16.0254384350469)) ;
#73266=CARTESIAN_POINT('',(80.2325032686099,238.145894005322,16.0213203435596)) ;
#73267=CARTESIAN_POINT('Ctrl Pts',(80.4284396085182,238.309544133633,16.2213203435595)) ;
#73268=CARTESIAN_POINT('Ctrl Pts',(80.4283164474799,238.308877752164,16.2206540664845)) ;
#73269=CARTESIAN_POINT('Ctrl Pts',(80.428189898863,238.308211992918,16.2199877856662)) ;
#73270=CARTESIAN_POINT('Ctrl Pts',(80.4240817240622,238.287182510412,16.1989219660283)) ;
#73271=CARTESIAN_POINT('Ctrl Pts',(80.4169102007044,238.267313462493,16.1784289743315)) ;
#73272=CARTESIAN_POINT('Ctrl Pts',(80.3967388391005,238.231016094161,16.1396302534697)) ;
#73273=CARTESIAN_POINT('Ctrl Pts',(80.3839059972643,238.214273436827,16.1210537744103)) ;
#73274=CARTESIAN_POINT('Ctrl Pts',(80.3513206135603,238.183933480584,16.0855257632447)) ;
#73275=CARTESIAN_POINT('Ctrl Pts',(80.3309934781214,238.170368597982,16.0684876094427)) ;
#73276=CARTESIAN_POINT('Ctrl Pts',(80.2896099908123,238.153486166166,16.0440628922152)) ;
#73277=CARTESIAN_POINT('Ctrl Pts',(80.2700848254327,238.148484194786,16.0353723462014)) ;
#73278=CARTESIAN_POINT('Ctrl Pts',(80.2436973163872,238.146171261641,16.0279192770422)) ;
#73279=CARTESIAN_POINT('Ctrl Pts',(80.2381151860642,238.14591456994,16.0265673132417)) ;
#73280=CARTESIAN_POINT('Ctrl Pts',(80.2325032686099,238.145894005322,16.0254384350468)) ;
#73281=CARTESIAN_POINT('Origin',(74.5283628290597,239.4,16.2213203435596)) ;
#73282=CARTESIAN_POINT('',(79.8474585022077,237.087594062475,16.0213203435596)) ;
#73283=CARTESIAN_POINT('Ctrl Pts',(79.8802543914408,237.061783435069,16.0254384350469)) ;
#73284=CARTESIAN_POINT('Ctrl Pts',(79.8713490019745,237.068303571741,16.0232182514845)) ;
#73285=CARTESIAN_POINT('Ctrl Pts',(79.8624665141187,237.075186287767,16.0218983740811)) ;
#73286=CARTESIAN_POINT('Ctrl Pts',(79.8516072883844,237.084112538764,16.0213707571522)) ;
#73287=CARTESIAN_POINT('Ctrl Pts',(79.8495261427911,237.085847011892,16.0213203435596)) ;
#73288=CARTESIAN_POINT('Ctrl Pts',(79.8474585022078,237.087594062475,16.0213203435596)) ;
#73289=CARTESIAN_POINT('',(80.1907997307331,238.144289709142,16.0213203435596)) ;
#73290=CARTESIAN_POINT('Origin',(74.5283628290597,239.4,16.0213203435596)) ;
#73291=CARTESIAN_POINT('Ctrl Pts',(80.1907997307331,238.144289709141,16.0213203435596)) ;
#73292=CARTESIAN_POINT('Ctrl Pts',(80.2020501093769,238.14511511556,16.0213203435596)) ;
#73293=CARTESIAN_POINT('Ctrl Pts',(80.2133277776002,238.145621944459,16.0221950109068)) ;
#73294=CARTESIAN_POINT('Ctrl Pts',(80.227203908038,238.145857122608,16.0244263118334)) ;
#73295=CARTESIAN_POINT('Ctrl Pts',(80.2298606513355,238.145884321569,16.0249068532759)) ;
#73296=CARTESIAN_POINT('Ctrl Pts',(80.2325032686099,238.145894005322,16.0254384350468)) ;
#73297=CARTESIAN_POINT('Origin',(70.5337979397592,235.19483040233,16.0213203435596)) ;
#73298=CARTESIAN_POINT('',(70.6507612836456,235.032597310185,16.0254384350468)) ;
#73299=CARTESIAN_POINT('',(70.6507612836456,235.032597310185,16.0213203435596)) ;
#73300=CARTESIAN_POINT('Ctrl Pts',(70.6507612836456,235.032597310185,16.0254384350468)) ;
#73301=CARTESIAN_POINT('Ctrl Pts',(70.6345258602317,235.02089224196,16.0294645582753)) ;
#73302=CARTESIAN_POINT('Ctrl Pts',(70.6172373339836,235.012125012964,16.0362204083692)) ;
#73303=CARTESIAN_POINT('Ctrl Pts',(70.5771486953323,234.998123831573,16.0560502171909)) ;
#73304=CARTESIAN_POINT('Ctrl Pts',(70.5545235842934,234.994754448684,16.070223718736)) ;
#73305=CARTESIAN_POINT('Ctrl Pts',(70.5070578957287,234.994925425491,16.1046945816757)) ;
#73306=CARTESIAN_POINT('Ctrl Pts',(70.4824619605172,235.000070810184,16.1258672215763)) ;
#73307=CARTESIAN_POINT('Ctrl Pts',(70.436721861721,235.018138351389,16.1708720249638)) ;
#73308=CARTESIAN_POINT('Ctrl Pts',(70.4155124011642,235.031699551137,16.1951765216815)) ;
#73309=CARTESIAN_POINT('Ctrl Pts',(70.3970393549092,235.048893605308,16.2199877856679)) ;
#73310=CARTESIAN_POINT('Ctrl Pts',(70.3965456514613,235.049357832442,16.2206540664828)) ;
#73311=CARTESIAN_POINT('Ctrl Pts',(70.3960543228867,235.049824554134,16.2213203435596)) ;
#73312=CARTESIAN_POINT('Origin',(74.5283628290597,239.4,16.2213203435596)) ;
#73313=CARTESIAN_POINT('',(70.6854431361484,235.055812131844,16.0213203435596)) ;
#73314=CARTESIAN_POINT('Ctrl Pts',(70.6507612836457,235.032597310185,16.0254384350469)) ;
#73315=CARTESIAN_POINT('Ctrl Pts',(70.6597142188007,235.03905200583,16.0232182514845)) ;
#73316=CARTESIAN_POINT('Ctrl Pts',(70.6690049104272,235.045372877566,16.0218983740811)) ;
#73317=CARTESIAN_POINT('Ctrl Pts',(70.6808499649014,235.052942251709,16.0213707571522)) ;
#73318=CARTESIAN_POINT('Ctrl Pts',(70.6831426562284,235.054385557114,16.0213203435596)) ;
#73319=CARTESIAN_POINT('Ctrl Pts',(70.6854431361486,235.055812131844,16.0213203435596)) ;
#73320=CARTESIAN_POINT('',(71.5843221421672,234.40273830644,16.0213203435596)) ;
#73321=CARTESIAN_POINT('Origin',(74.5283628290597,239.4,16.0213203435596)) ;
#73322=CARTESIAN_POINT('Ctrl Pts',(71.5843221421672,234.40273830644,16.0213203435596)) ;
#73323=CARTESIAN_POINT('Ctrl Pts',(71.5816305921256,234.39178349591,16.0213203435596)) ;
#73324=CARTESIAN_POINT('Ctrl Pts',(71.5786276239152,234.380901177314,16.0221950109068)) ;
#73325=CARTESIAN_POINT('Ctrl Pts',(71.5745633315043,234.367631518996,16.0244263118334)) ;
#73326=CARTESIAN_POINT('Ctrl Pts',(71.5737682204258,234.365096401029,16.0249068532759)) ;
#73327=CARTESIAN_POINT('Ctrl Pts',(71.5729608165738,234.362580130206,16.0254384350468)) ;
#73328=CARTESIAN_POINT('Ctrl Pts',(80.3408628290597,239.969950655759,7.27867958884207)) ;
#73329=CARTESIAN_POINT('Ctrl Pts',(80.2885314039892,239.952734880846,7.16318954730702)) ;
#73330=CARTESIAN_POINT('Ctrl Pts',(80.1867665649176,239.903495511764,6.93433474994972)) ;
#73331=CARTESIAN_POINT('Ctrl Pts',(80.0699170197431,239.797829761707,6.66117794267636)) ;
#73332=CARTESIAN_POINT('Ctrl Pts',(79.9999528336347,239.689106134798,6.49328644843112)) ;
#73333=CARTESIAN_POINT('Ctrl Pts',(79.9663766082065,239.6132157885,6.41181121705511)) ;
#73334=CARTESIAN_POINT('Ctrl Pts',(79.9424927848733,239.538465694316,6.35347296267418)) ;
#73335=CARTESIAN_POINT('Ctrl Pts',(79.9216609370228,239.414589162551,6.30217046564654)) ;
#73336=CARTESIAN_POINT('Ctrl Pts',(79.9350370465868,239.282669940057,6.33519178586446)) ;
#73337=CARTESIAN_POINT('Ctrl Pts',(79.9662361722743,239.186893556273,6.41145261667877)) ;
#73338=CARTESIAN_POINT('Ctrl Pts',(79.9996838292369,239.11091773279,6.49259951597652)) ;
#73339=CARTESIAN_POINT('Ctrl Pts',(80.0697670156571,239.002192054553,6.66079439764563)) ;
#73340=CARTESIAN_POINT('Ctrl Pts',(80.1865578960656,238.896505082212,6.93380047883317)) ;
#73341=CARTESIAN_POINT('Ctrl Pts',(80.2885314039892,238.847265119153,7.163189547307)) ;
#73342=CARTESIAN_POINT('Ctrl Pts',(80.3408628290597,238.830049344241,7.27867958884205)) ;
#73343=CARTESIAN_POINT('Ctrl Pts',(80.3840073254959,239.984144153038,7.24979207607674)) ;
#73344=CARTESIAN_POINT('Ctrl Pts',(80.327695104819,239.970119016261,7.1355831883288)) ;
#73345=CARTESIAN_POINT('Ctrl Pts',(80.2168873775464,239.92515275458,6.90890516875886)) ;
#73346=CARTESIAN_POINT('Ctrl Pts',(80.0872644090126,239.819386167439,6.63780263189585)) ;
#73347=CARTESIAN_POINT('Ctrl Pts',(80.0088484791991,239.706352588273,6.47101811980176)) ;
#73348=CARTESIAN_POINT('Ctrl Pts',(79.9710587774453,239.626526469016,6.39005214895656)) ;
#73349=CARTESIAN_POINT('Ctrl Pts',(79.9441141909301,239.547412991843,6.33206751004184)) ;
#73350=CARTESIAN_POINT('Ctrl Pts',(79.9205448061692,239.415579861931,6.2810645188759)) ;
#73351=CARTESIAN_POINT('Ctrl Pts',(79.9356913897779,239.274844790961,6.31389543197584)) ;
#73352=CARTESIAN_POINT('Ctrl Pts',(79.9708973932049,239.173489891446,6.38969559217925)) ;
#73353=CARTESIAN_POINT('Ctrl Pts',(80.008539600943,239.093561108983,6.47033490089508)) ;
#73354=CARTESIAN_POINT('Ctrl Pts',(80.0870927203403,238.98056853352,6.63742123865058)) ;
#73355=CARTESIAN_POINT('Ctrl Pts',(80.2166470863611,238.874723810129,6.90837475287206)) ;
#73356=CARTESIAN_POINT('Ctrl Pts',(80.327695104819,238.829880983738,7.13558318832877)) ;
#73357=CARTESIAN_POINT('Ctrl Pts',(80.3840073254959,238.815855846962,7.24979207607673)) ;
#73358=CARTESIAN_POINT('Ctrl Pts',(80.4463978769533,240.046981897287,7.19960839071963)) ;
#73359=CARTESIAN_POINT('Ctrl Pts',(80.3813641849446,240.032577112202,7.08747698484387)) ;
#73360=CARTESIAN_POINT('Ctrl Pts',(80.2535732837017,239.984593320072,6.86438826993785)) ;
#73361=CARTESIAN_POINT('Ctrl Pts',(80.1046406899897,239.867698231238,6.59674657937938)) ;
#73362=CARTESIAN_POINT('Ctrl Pts',(80.0147751931735,239.741969801163,6.43185373754287)) ;
#73363=CARTESIAN_POINT('Ctrl Pts',(79.971516906311,239.652939705859,6.35176231641288)) ;
#73364=CARTESIAN_POINT('Ctrl Pts',(79.9406932623428,239.56466954151,6.2943871120956)) ;
#73365=CARTESIAN_POINT('Ctrl Pts',(79.9137527545012,239.417443548513,6.24390250673371)) ;
#73366=CARTESIAN_POINT('Ctrl Pts',(79.9310621458369,239.260304020071,6.27640300071354)) ;
#73367=CARTESIAN_POINT('Ctrl Pts',(79.9713339971205,239.14721859975,6.351408721716)) ;
#73368=CARTESIAN_POINT('Ctrl Pts',(80.0144245398524,239.058085730517,6.43117626971816)) ;
#73369=CARTESIAN_POINT('Ctrl Pts',(80.1044455623915,238.93234532304,6.59636871271608)) ;
#73370=CARTESIAN_POINT('Ctrl Pts',(80.2533028536955,238.815437211919,6.86386231950446)) ;
#73371=CARTESIAN_POINT('Ctrl Pts',(80.3813641849446,238.767422887798,7.08747698484384)) ;
#73372=CARTESIAN_POINT('Ctrl Pts',(80.4463978769533,238.753018102712,7.19960839071962)) ;
#73373=CARTESIAN_POINT('Ctrl Pts',(80.4538735935557,240.142610480885,7.17608503411334)) ;
#73374=CARTESIAN_POINT('Ctrl Pts',(80.3846751038144,240.121796616249,7.0621594456609)) ;
#73375=CARTESIAN_POINT('Ctrl Pts',(80.2498546406098,240.060206570595,6.83606809856264)) ;
#73376=CARTESIAN_POINT('Ctrl Pts',(80.0946540093807,239.923582092156,6.56568507344859)) ;
#73377=CARTESIAN_POINT('Ctrl Pts',(80.0016160154075,239.781211815477,6.39934495813426)) ;
#73378=CARTESIAN_POINT('Ctrl Pts',(79.956946110464,239.681398056183,6.31859474911535)) ;
#73379=CARTESIAN_POINT('Ctrl Pts',(79.925163217437,239.582888242748,6.26076462735161)) ;
#73380=CARTESIAN_POINT('Ctrl Pts',(79.8974336231358,239.419304875701,6.2098975150157)) ;
#73381=CARTESIAN_POINT('Ctrl Pts',(79.9152402321547,239.244981652347,6.24264091507684)) ;
#73382=CARTESIAN_POINT('Ctrl Pts',(79.9567588075993,239.118767221015,6.31823906006946)) ;
#73383=CARTESIAN_POINT('Ctrl Pts',(80.0012573105604,239.018841087611,6.39866345547881)) ;
#73384=CARTESIAN_POINT('Ctrl Pts',(80.0944541609073,238.876460220697,6.56530464002502)) ;
#73385=CARTESIAN_POINT('Ctrl Pts',(80.2495762313356,238.739817789344,6.83553876784972)) ;
#73386=CARTESIAN_POINT('Ctrl Pts',(80.3846751038144,238.67820338375,7.06215944566087)) ;
#73387=CARTESIAN_POINT('Ctrl Pts',(80.4538735935557,238.657389519115,7.17608503411333)) ;
#73388=CARTESIAN_POINT('Ctrl Pts',(80.4465004238194,240.182155687653,7.17267980084145)) ;
#73389=CARTESIAN_POINT('Ctrl Pts',(80.3767773507721,240.158806652482,7.0571897593064)) ;
#73390=CARTESIAN_POINT('Ctrl Pts',(80.2412731536591,240.091756439979,6.8283349619491)) ;
#73391=CARTESIAN_POINT('Ctrl Pts',(80.0859037680535,239.947102365642,6.55517815467574)) ;
#73392=CARTESIAN_POINT('Ctrl Pts',(79.9929779090082,239.797804263718,6.3872866604305)) ;
#73393=CARTESIAN_POINT('Ctrl Pts',(79.9484044791676,239.693464121303,6.30581142905449)) ;
#73394=CARTESIAN_POINT('Ctrl Pts',(79.9167075774066,239.590628083797,6.24747317467356)) ;
#73395=CARTESIAN_POINT('Ctrl Pts',(79.8890717515519,239.420095928579,6.19617067764592)) ;
#73396=CARTESIAN_POINT('Ctrl Pts',(79.9068146439663,239.238447540333,6.22919199786384)) ;
#73397=CARTESIAN_POINT('Ctrl Pts',(79.9482185006771,239.10668693158,6.30545282867815)) ;
#73398=CARTESIAN_POINT('Ctrl Pts',(79.992621665789,239.002228657834,6.3865997279759)) ;
#73399=CARTESIAN_POINT('Ctrl Pts',(80.0857051319182,238.852927765033,6.55479460964501)) ;
#73400=CARTESIAN_POINT('Ctrl Pts',(80.2409968407949,238.708244359177,6.82780069083255)) ;
#73401=CARTESIAN_POINT('Ctrl Pts',(80.3767773507721,238.641193347518,7.05718975930638)) ;
#73402=CARTESIAN_POINT('Ctrl Pts',(80.4465004238194,238.617844312347,7.17267980084143)) ;
#73403=CARTESIAN_POINT('Ctrl Pts',(80.4465004238194,238.617844312347,7.17267980084143)) ;
#73404=CARTESIAN_POINT('Ctrl Pts',(80.3767773507721,238.641193347518,7.05718975930637)) ;
#73405=CARTESIAN_POINT('Ctrl Pts',(80.2409968407949,238.708244359176,6.82780069083255)) ;
#73406=CARTESIAN_POINT('Ctrl Pts',(80.0857051319181,238.852927765034,6.55479460964501)) ;
#73407=CARTESIAN_POINT('Ctrl Pts',(79.9926216657891,239.002228657833,6.38659972797591)) ;
#73408=CARTESIAN_POINT('Ctrl Pts',(79.9482185006771,239.106686931581,6.30545282867815)) ;
#73409=CARTESIAN_POINT('Ctrl Pts',(79.9068146439663,239.238447540332,6.22919199786383)) ;
#73410=CARTESIAN_POINT('Ctrl Pts',(79.889071751552,239.420095928579,6.19617067764593)) ;
#73411=CARTESIAN_POINT('Ctrl Pts',(79.9167075774066,239.590628083797,6.24747317467357)) ;
#73412=CARTESIAN_POINT('Ctrl Pts',(79.9484044791676,239.693464121303,6.3058114290545)) ;
#73413=CARTESIAN_POINT('Ctrl Pts',(79.9929779090082,239.797804263719,6.3872866604305)) ;
#73414=CARTESIAN_POINT('Ctrl Pts',(80.0859037680535,239.947102365641,6.55517815467574)) ;
#73415=CARTESIAN_POINT('Ctrl Pts',(80.241273153659,240.091756439979,6.82833496194906)) ;
#73416=CARTESIAN_POINT('Ctrl Pts',(80.3767773507721,240.158806652482,7.05718975930632)) ;
#73417=CARTESIAN_POINT('Ctrl Pts',(80.4465004238193,240.182155687653,7.17267980084132)) ;
#73418=CARTESIAN_POINT('Ctrl Pts',(80.3408628290597,239.969950655759,7.27867958884207)) ;
#73419=CARTESIAN_POINT('Ctrl Pts',(80.2885314039892,239.952734880846,7.16318954730702)) ;
#73420=CARTESIAN_POINT('Ctrl Pts',(80.1867665649176,239.903495511764,6.93433474994972)) ;
#73421=CARTESIAN_POINT('Ctrl Pts',(80.0699170197431,239.797829761707,6.66117794267636)) ;
#73422=CARTESIAN_POINT('Ctrl Pts',(79.9999528336347,239.689106134798,6.49328644843112)) ;
#73423=CARTESIAN_POINT('Ctrl Pts',(79.9663766082065,239.6132157885,6.41181121705511)) ;
#73424=CARTESIAN_POINT('Ctrl Pts',(79.9424927848733,239.538465694316,6.35347296267418)) ;
#73425=CARTESIAN_POINT('Ctrl Pts',(79.9216609370228,239.414589162551,6.30217046564654)) ;
#73426=CARTESIAN_POINT('Ctrl Pts',(79.9350370465868,239.282669940057,6.33519178586446)) ;
#73427=CARTESIAN_POINT('Ctrl Pts',(79.9662361722743,239.186893556273,6.41145261667877)) ;
#73428=CARTESIAN_POINT('Ctrl Pts',(79.9996838292369,239.11091773279,6.49259951597652)) ;
#73429=CARTESIAN_POINT('Ctrl Pts',(80.0697670156571,239.002192054553,6.66079439764563)) ;
#73430=CARTESIAN_POINT('Ctrl Pts',(80.1865578960656,238.896505082212,6.93380047883317)) ;
#73431=CARTESIAN_POINT('Ctrl Pts',(80.2885314039892,238.847265119153,7.163189547307)) ;
#73432=CARTESIAN_POINT('Ctrl Pts',(80.3408628290597,238.830049344241,7.27867958884205)) ;
#73433=CARTESIAN_POINT('Origin',(80.2783628290597,238.640065792321,16.0213203435596)) ;
#73434=CARTESIAN_POINT('',(80.3408628290597,238.830049344241,16.0254384350468)) ;
#73435=CARTESIAN_POINT('',(80.3408628290597,238.830049344241,16.0213203435596)) ;
#73436=CARTESIAN_POINT('Ctrl Pts',(80.3408628290597,238.830049344241,16.0254384350468)) ;
#73437=CARTESIAN_POINT('Ctrl Pts',(80.3598753706213,238.823794677268,16.0294645582753)) ;
#73438=CARTESIAN_POINT('Ctrl Pts',(80.377130148635,238.814961213633,16.0362204083691)) ;
#73439=CARTESIAN_POINT('Ctrl Pts',(80.4120208529058,238.790758511619,16.0560502171909)) ;
#73440=CARTESIAN_POINT('Ctrl Pts',(80.4280454475239,238.774434885861,16.070223718736)) ;
#73441=CARTESIAN_POINT('Ctrl Pts',(80.4558067561093,238.735933839516,16.1046945816758)) ;
#73442=CARTESIAN_POINT('Ctrl Pts',(80.4661011804338,238.713010928697,16.1258672215766)) ;
#73443=CARTESIAN_POINT('Ctrl Pts',(80.4783695880631,238.665386577181,16.1708720249644)) ;
#73444=CARTESIAN_POINT('Ctrl Pts',(80.4798649551292,238.640256689945,16.1951765216955)) ;
#73445=CARTESIAN_POINT('Ctrl Pts',(80.4768128572537,238.615205270105,16.2199877856669)) ;
#73446=CARTESIAN_POINT('Ctrl Pts',(80.4767274812194,238.614532989764,16.220654066484)) ;
#73447=CARTESIAN_POINT('Ctrl Pts',(80.4766386911286,238.61386116447,16.2213203435596)) ;
#73448=CARTESIAN_POINT('Origin',(70.3231932313897,235.405435110699,16.0213203435596)) ;
#73449=CARTESIAN_POINT('',(70.1609601392447,235.522398454586,16.0254384350469)) ;
#73450=CARTESIAN_POINT('',(70.1609601392447,235.522398454586,16.0213203435596)) ;
#73451=CARTESIAN_POINT('Ctrl Pts',(70.1781873831944,235.267691493827,16.2213203435594)) ;
#73452=CARTESIAN_POINT('Ctrl Pts',(70.177720661491,235.268182822413,16.2206540664675)) ;
#73453=CARTESIAN_POINT('Ctrl Pts',(70.1772564343506,235.268676525868,16.2199877856904)) ;
#73454=CARTESIAN_POINT('Ctrl Pts',(70.1626579503238,235.284360928632,16.1989219658475)) ;
#73455=CARTESIAN_POINT('Ctrl Pts',(70.1507988684555,235.30184154635,16.1784289743615)) ;
#73456=CARTESIAN_POINT('Ctrl Pts',(70.1332901094989,235.339495578454,16.1396302535283)) ;
#73457=CARTESIAN_POINT('Ctrl Pts',(70.1272879703583,235.359718652633,16.1210537744804)) ;
#73458=CARTESIAN_POINT('Ctrl Pts',(70.1218956381112,235.403914160637,16.0855257633118)) ;
#73459=CARTESIAN_POINT('Ctrl Pts',(70.1228694079808,235.428332396604,16.0684876094977)) ;
#73460=CARTESIAN_POINT('Ctrl Pts',(70.1335358372496,235.471735585582,16.0440628922505)) ;
#73461=CARTESIAN_POINT('Ctrl Pts',(70.1409657616503,235.490471861208,16.0353723462285)) ;
#73462=CARTESIAN_POINT('Ctrl Pts',(70.1546047480969,235.513179312484,16.0279192770533)) ;
#73463=CARTESIAN_POINT('Ctrl Pts',(70.1576781740409,235.517846230396,16.0265673132464)) ;
#73464=CARTESIAN_POINT('Ctrl Pts',(70.160960139245,235.522398454586,16.0254384350468)) ;
#73465=CARTESIAN_POINT('Origin',(74.5283628290597,239.4,7.2786795888419)) ;
#73466=CARTESIAN_POINT('Origin',(74.5283628290597,239.4,7.17267980084126)) ;
#73467=CARTESIAN_POINT('Origin',(80.2783628290597,240.159934207678,16.0213203435596)) ;
#73468=CARTESIAN_POINT('',(80.3408628290597,239.969950655759,16.0254384350468)) ;
#73469=CARTESIAN_POINT('',(80.3408628290597,239.969950655759,16.0213203435596)) ;
#73470=CARTESIAN_POINT('Ctrl Pts',(80.4766386911288,240.186138835529,16.2213203435596)) ;
#73471=CARTESIAN_POINT('Ctrl Pts',(80.476727481219,240.18546701024,16.2206540664879)) ;
#73472=CARTESIAN_POINT('Ctrl Pts',(80.4768128572532,240.184794729899,16.2199877856617)) ;
#73473=CARTESIAN_POINT('Ctrl Pts',(80.4794042183208,240.163525007664,16.1989219660609)) ;
#73474=CARTESIAN_POINT('Ctrl Pts',(80.4787235677644,240.142412297601,16.1784289743283)) ;
#73475=CARTESIAN_POINT('Ctrl Pts',(80.4707559665322,240.101658155386,16.1396302534631)) ;
#73476=CARTESIAN_POINT('Ctrl Pts',(80.4637249743274,240.081769375812,16.1210537744024)) ;
#73477=CARTESIAN_POINT('Ctrl Pts',(80.4421099949043,240.042844925392,16.0855257632372)) ;
#73478=CARTESIAN_POINT('Ctrl Pts',(80.4269695195379,240.023662525103,16.0684876094366)) ;
#73479=CARTESIAN_POINT('Ctrl Pts',(80.3928284426024,239.994818177451,16.0440628922111)) ;
#73480=CARTESIAN_POINT('Ctrl Pts',(80.3758046009983,239.984027412056,16.0353723461983)) ;
#73481=CARTESIAN_POINT('Ctrl Pts',(80.3514233242228,239.973673493185,16.027919277041)) ;
#73482=CARTESIAN_POINT('Ctrl Pts',(80.3461937249045,239.971704391737,16.0265673132412)) ;
#73483=CARTESIAN_POINT('Ctrl Pts',(80.3408628290599,239.969950655758,16.0254384350468)) ;
#73484=CARTESIAN_POINT('Origin',(74.5283628290597,239.4,16.2213203435596)) ;
#73485=CARTESIAN_POINT('',(80.301696162393,238.844462222507,16.0213203435596)) ;
#73486=CARTESIAN_POINT('Ctrl Pts',(80.3408628290597,238.830049344241,16.0254384350468)) ;
#73487=CARTESIAN_POINT('Ctrl Pts',(80.3303784673406,238.833498446023,16.0232182514845)) ;
#73488=CARTESIAN_POINT('Ctrl Pts',(80.3198038431649,238.83729945825,16.0218983740811)) ;
#73489=CARTESIAN_POINT('Ctrl Pts',(80.3067177425144,238.842433142129,16.0213707571522)) ;
#73490=CARTESIAN_POINT('Ctrl Pts',(80.3042024737635,238.843439614744,16.0213203435596)) ;
#73491=CARTESIAN_POINT('Ctrl Pts',(80.3016961623929,238.844462222507,16.0213203435596)) ;
#73492=CARTESIAN_POINT('',(80.301696162393,239.955537777493,16.0213203435596)) ;
#73493=CARTESIAN_POINT('Origin',(74.5283628290597,239.4,16.0213203435596)) ;
#73494=CARTESIAN_POINT('Ctrl Pts',(80.3016961623929,239.955537777493,16.0213203435596)) ;
#73495=CARTESIAN_POINT('Ctrl Pts',(80.3121408437025,239.95979934384,16.0213203435596)) ;
#73496=CARTESIAN_POINT('Ctrl Pts',(80.3227099248118,239.963766357905,16.0221950109068)) ;
#73497=CARTESIAN_POINT('Ctrl Pts',(80.3358342350411,239.968277985737,16.0244263118334)) ;
#73498=CARTESIAN_POINT('Ctrl Pts',(80.3383525431248,239.969124832316,16.0249068532759)) ;
#73499=CARTESIAN_POINT('Ctrl Pts',(80.3408628290598,239.969950655759,16.0254384350468)) ;
#73500=CARTESIAN_POINT('Origin',(69.4298369914177,236.635034487937,16.0213203435596)) ;
#73501=CARTESIAN_POINT('',(69.4909429592657,236.444597987514,16.0254384350469)) ;
#73502=CARTESIAN_POINT('',(69.4909429592657,236.444597987514,16.0213203435596)) ;
#73503=CARTESIAN_POINT('Ctrl Pts',(69.4909429592658,236.444597987514,16.0254384350469)) ;
#73504=CARTESIAN_POINT('Ctrl Pts',(69.4718850890315,236.438482827851,16.0294645582753)) ;
#73505=CARTESIAN_POINT('Ctrl Pts',(69.4527335007328,236.435487146003,16.0362204083691)) ;
#73506=CARTESIAN_POINT('Ctrl Pts',(69.4102803367226,236.434559301829,16.056050217191)) ;
#73507=CARTESIAN_POINT('Ctrl Pts',(69.3877213808638,236.438346372087,16.0702237187361)) ;
#73508=CARTESIAN_POINT('Ctrl Pts',(69.3426316631928,236.45317668511,16.1046945816759)) ;
#73509=CARTESIAN_POINT('Ctrl Pts',(69.320829550048,236.465670798725,16.1258672215769)) ;
#73510=CARTESIAN_POINT('Ctrl Pts',(69.2829113083105,236.496988519374,16.1708720249652)) ;
#73511=CARTESIAN_POINT('Ctrl Pts',(69.2669305538229,236.516440070524,16.1951765216735)) ;
#73512=CARTESIAN_POINT('Ctrl Pts',(69.2546748977525,236.538501073008,16.2199877856701)) ;
#73513=CARTESIAN_POINT('Ctrl Pts',(69.2543488119446,236.539095142004,16.2206540664831)) ;
#73514=CARTESIAN_POINT('Ctrl Pts',(69.254025755637,236.53969084959,16.2213203435596)) ;
#73515=CARTESIAN_POINT('Origin',(74.5283628290597,239.4,16.2213203435596)) ;
#73516=CARTESIAN_POINT('',(69.5311011354997,236.455959313107,16.0213203435596)) ;
#73517=CARTESIAN_POINT('Ctrl Pts',(69.4909429592657,236.444597987514,16.0254384350469)) ;
#73518=CARTESIAN_POINT('Ctrl Pts',(69.5014523172327,236.447970158755,16.0232182514845)) ;
#73519=CARTESIAN_POINT('Ctrl Pts',(69.5122415468308,236.451110683407,16.0218983740811)) ;
#73520=CARTESIAN_POINT('Ctrl Pts',(69.5258459283211,236.454649262878,16.0213707571522)) ;
#73521=CARTESIAN_POINT('Ctrl Pts',(69.5284724132457,236.455313447305,16.0213203435596)) ;
#73522=CARTESIAN_POINT('Ctrl Pts',(69.5311011354996,236.455959313107,16.0213203435596)) ;
#73523=CARTESIAN_POINT('',(70.1841749609035,235.557080307089,16.0213203435596)) ;
#73524=CARTESIAN_POINT('Origin',(74.5283628290597,239.4,16.0213203435596)) ;
#73525=CARTESIAN_POINT('Ctrl Pts',(70.1841749609037,235.557080307089,16.0213203435596)) ;
#73526=CARTESIAN_POINT('Ctrl Pts',(70.1782299220736,235.547493397853,16.0213203435596)) ;
#73527=CARTESIAN_POINT('Ctrl Pts',(70.1720111082046,235.538071666051,16.0221950109068)) ;
#73528=CARTESIAN_POINT('Ctrl Pts',(70.1640451864931,235.526707406463,16.0244263118334)) ;
#73529=CARTESIAN_POINT('Ctrl Pts',(70.1625055963862,235.524542068837,16.0249068532759)) ;
#73530=CARTESIAN_POINT('Ctrl Pts',(70.1609601392448,235.522398454586,16.0254384350468)) ;
#73531=CARTESIAN_POINT('Ctrl Pts',(79.8802543914407,241.738216564931,7.27867958884204)) ;
#73532=CARTESIAN_POINT('Ctrl Pts',(79.835803113544,241.705671283424,7.16318668385245)) ;
#73533=CARTESIAN_POINT('Ctrl Pts',(79.7540359687551,241.627328321488,6.93379523402446)) ;
#73534=CARTESIAN_POINT('Ctrl Pts',(79.675621293688,241.490723852039,6.66079129118985)) ;
#73535=CARTESIAN_POINT('Ctrl Pts',(79.6425666774348,241.365662283546,6.49259690874814)) ;
#73536=CARTESIAN_POINT('Ctrl Pts',(79.6342342806502,241.283068999992,6.41145082407054)) ;
#73537=CARTESIAN_POINT('Ctrl Pts',(79.6341591116984,241.182339039687,6.33519087357569)) ;
#73538=CARTESIAN_POINT('Ctrl Pts',(79.6622035595951,241.052743230527,6.30217118028935)) ;
#73539=CARTESIAN_POINT('Ctrl Pts',(79.7202959489803,240.941367844591,6.35347468345946)) ;
#73540=CARTESIAN_POINT('Ctrl Pts',(79.7661098244323,240.877657242828,6.41181318029812)) ;
#73541=CARTESIAN_POINT('Ctrl Pts',(79.8214940286967,240.815857306447,6.49328852242612)) ;
#73542=CARTESIAN_POINT('Ctrl Pts',(79.9216310945127,240.734075598131,6.66117971759687)) ;
#73543=CARTESIAN_POINT('Ctrl Pts',(80.065413735872,240.669690330056,6.93433585613084)) ;
#73544=CARTESIAN_POINT('Ctrl Pts',(80.1774132992676,240.65430786939,7.16318984184328)) ;
#73545=CARTESIAN_POINT('Ctrl Pts',(80.23250326861,240.654105994678,7.27867958884203)) ;
#73546=CARTESIAN_POINT('Ctrl Pts',(79.9169012140497,241.765047765619,7.24979207607672)) ;
#73547=CARTESIAN_POINT('Ctrl Pts',(79.8676778948299,241.734306872547,7.13558035663909)) ;
#73548=CARTESIAN_POINT('Ctrl Pts',(79.7759215956017,241.657341581077,6.90836950611157)) ;
#73549=CARTESIAN_POINT('Ctrl Pts',(79.6854170373555,241.516642878156,6.63741808594036)) ;
#73550=CARTESIAN_POINT('Ctrl Pts',(79.6456256439924,241.384905848815,6.47033223326042)) ;
#73551=CARTESIAN_POINT('Ctrl Pts',(79.6345255741363,241.297256868669,6.38969373228111)) ;
#73552=CARTESIAN_POINT('Ctrl Pts',(79.6323635562481,241.18998321442,6.3138944436818)) ;
#73553=CARTESIAN_POINT('Ctrl Pts',(79.6614485258077,241.051455962317,6.28106514390401)) ;
#73554=CARTESIAN_POINT('Ctrl Pts',(79.7246032198788,240.933359420814,6.33206913634608)) ;
#73555=CARTESIAN_POINT('Ctrl Pts',(79.7746764094695,240.866444865567,6.39005401694239)) ;
#73556=CARTESIAN_POINT('Ctrl Pts',(79.8352840817867,240.802203860244,6.47102009681309)) ;
#73557=CARTESIAN_POINT('Ctrl Pts',(79.944791006663,240.718934914115,6.63780432564773)) ;
#73558=CARTESIAN_POINT('Ctrl Pts',(80.1007529981817,240.658400961759,6.90890620100791)) ;
#73559=CARTESIAN_POINT('Ctrl Pts',(80.2200321925607,240.649876834119,7.1355834795977)) ;
#73560=CARTESIAN_POINT('Ctrl Pts',(80.2779221549567,240.653939559214,7.2497920760767)) ;
#73561=CARTESIAN_POINT('Ctrl Pts',(79.9568202021994,241.844089757625,7.19960839981096)) ;
#73562=CARTESIAN_POINT('Ctrl Pts',(79.8994193858697,241.810292638923,7.08747421375449)) ;
#73563=CARTESIAN_POINT('Ctrl Pts',(79.7924622476912,241.72505347842,6.86385720549173)) ;
#73564=CARTESIAN_POINT('Ctrl Pts',(79.6870183903762,241.567867925046,6.59636568101839)) ;
#73565=CARTESIAN_POINT('Ctrl Pts',(79.6402596949716,241.420463149438,6.43117372668737)) ;
#73566=CARTESIAN_POINT('Ctrl Pts',(79.6268222315534,241.322376920331,6.35140697730098)) ;
#73567=CARTESIAN_POINT('Ctrl Pts',(79.6234672952181,241.202381421516,6.27640212195239)) ;
#73568=CARTESIAN_POINT('Ctrl Pts',(79.6555646533985,241.047584288124,6.24390323078809)) ;
#73569=CARTESIAN_POINT('Ctrl Pts',(79.7266821718544,240.915890106185,6.29438882568343)) ;
#73570=CARTESIAN_POINT('Ctrl Pts',(79.7832741387335,240.841465776635,6.35176426775246)) ;
#73571=CARTESIAN_POINT('Ctrl Pts',(79.8519269181584,240.770161214137,6.43185579663839)) ;
#73572=CARTESIAN_POINT('Ctrl Pts',(79.9762459680929,240.678356922049,6.59674833983391)) ;
#73573=CARTESIAN_POINT('Ctrl Pts',(80.1540113597504,240.613206175734,6.86438936993202)) ;
#73574=CARTESIAN_POINT('Ctrl Pts',(80.2903751411169,240.60706030193,7.08747727990587)) ;
#73575=CARTESIAN_POINT('Ctrl Pts',(80.3566770119809,240.613457036933,7.19960839981093)) ;
#73576=CARTESIAN_POINT('Ctrl Pts',(79.9343791952164,241.937348063495,7.17608503411331)) ;
#73577=CARTESIAN_POINT('Ctrl Pts',(79.8749978862602,241.896168371608,7.0621566209953)) ;
#73578=CARTESIAN_POINT('Ctrl Pts',(79.765550397568,241.795819886808,6.83553354957588)) ;
#73579=CARTESIAN_POINT('Ctrl Pts',(79.6602467046092,241.617930062692,6.56530151717807)) ;
#73580=CARTESIAN_POINT('Ctrl Pts',(79.6156098444531,241.453717854407,6.39866081947765)) ;
#73581=CARTESIAN_POINT('Ctrl Pts',(79.6041686543468,241.344931536776,6.31823722992109)) ;
#73582=CARTESIAN_POINT('Ctrl Pts',(79.6036851264843,241.212064334829,6.24263995519171)) ;
#73583=CARTESIAN_POINT('Ctrl Pts',(79.6406196804877,241.040770912242,6.20989816557033)) ;
#73584=CARTESIAN_POINT('Ctrl Pts',(79.7175423595761,240.893763866678,6.26076627615902)) ;
#73585=CARTESIAN_POINT('Ctrl Pts',(79.7782108398639,240.809897525748,6.31859663867191)) ;
#73586=CARTESIAN_POINT('Ctrl Pts',(79.8515384719066,240.728773354515,6.39934695661234)) ;
#73587=CARTESIAN_POINT('Ctrl Pts',(79.9840173160935,240.622122133448,6.56568678471671)) ;
#73588=CARTESIAN_POINT('Ctrl Pts',(80.1738406495645,240.540144605999,6.83606914895208)) ;
#73589=CARTESIAN_POINT('Ctrl Pts',(80.3210943845718,240.523230645993,7.06215973620728)) ;
#73590=CARTESIAN_POINT('Ctrl Pts',(80.393337712805,240.524818989667,7.17608503411328)) ;
#73591=CARTESIAN_POINT('Ctrl Pts',(79.9151467531554,241.97267935533,7.17267980084141)) ;
#73592=CARTESIAN_POINT('Ctrl Pts',(79.8560499536608,241.928926404028,7.05718689585183)) ;
#73593=CARTESIAN_POINT('Ctrl Pts',(79.7476341877425,241.823196674671,6.82779544602381)) ;
#73594=CARTESIAN_POINT('Ctrl Pts',(79.6446539418595,241.637607029148,6.55479150318921)) ;
#73595=CARTESIAN_POINT('Ctrl Pts',(79.6022633225759,241.466848501153,6.38659712074747)) ;
#73596=CARTESIAN_POINT('Ctrl Pts',(79.5923133136054,241.353781318703,6.30545103606987)) ;
#73597=CARTESIAN_POINT('Ctrl Pts',(79.5936527526702,241.215674828182,6.22919108557502)) ;
#73598=CARTESIAN_POINT('Ctrl Pts',(79.6329114963884,241.037434453048,6.19617139228868)) ;
#73599=CARTESIAN_POINT('Ctrl Pts',(79.711892278316,240.883789775029,6.2474748954588)) ;
#73600=CARTESIAN_POINT('Ctrl Pts',(79.7738158466498,240.795782399142,6.30581339229746)) ;
#73601=CARTESIAN_POINT('Ctrl Pts',(79.8484504478331,240.710323590906,6.38728873442546)) ;
#73602=CARTESIAN_POINT('Ctrl Pts',(79.9829634655173,240.597048995858,6.55517992959621)) ;
#73603=CARTESIAN_POINT('Ctrl Pts',(80.1754285723234,240.507487043079,6.82833606813018)) ;
#73604=CARTESIAN_POINT('Ctrl Pts',(80.3250199085055,240.485591464222,7.05719005384264)) ;
#73605=CARTESIAN_POINT('Ctrl Pts',(80.3985455526191,240.48493082833,7.17267980084139)) ;
#73606=CARTESIAN_POINT('Ctrl Pts',(80.3985455526191,240.48493082833,7.17267980084139)) ;
#73607=CARTESIAN_POINT('Ctrl Pts',(80.3618194988804,240.485260815909,7.11499268084841)) ;
#73608=CARTESIAN_POINT('Ctrl Pts',(80.324727685632,240.488159890155,7.05749448559109)) ;
#73609=CARTESIAN_POINT('Ctrl Pts',(80.2873368929612,240.493904456482,7.00044815896927)) ;
#73610=CARTESIAN_POINT('Ctrl Pts',(80.2618946329122,240.497813299807,6.96163145108278)) ;
#73611=CARTESIAN_POINT('Ctrl Pts',(80.2363140175748,240.503039163732,6.92302396449324)) ;
#73612=CARTESIAN_POINT('Ctrl Pts',(80.210616885397,240.509661862821,6.88470750123333)) ;
#73613=CARTESIAN_POINT('Ctrl Pts',(80.1985486563354,240.512772102869,6.86671281403429)) ;
#73614=CARTESIAN_POINT('Ctrl Pts',(80.1864548869752,240.516190215325,6.84878249237319)) ;
#73615=CARTESIAN_POINT('Ctrl Pts',(80.1743333850077,240.519925538921,6.83091833685153)) ;
#73616=CARTESIAN_POINT('Ctrl Pts',(80.098418576038,240.543319205645,6.71903831097155)) ;
#73617=CARTESIAN_POINT('Ctrl Pts',(80.0214440764623,240.579145495968,6.60979495876411)) ;
#73618=CARTESIAN_POINT('Ctrl Pts',(79.9445514182818,240.634230425691,6.50943178829059)) ;
#73619=CARTESIAN_POINT('Ctrl Pts',(79.9123655188488,240.65728799777,6.46742154975707)) ;
#73620=CARTESIAN_POINT('Ctrl Pts',(79.8801984195234,240.683717891127,6.42697356775467)) ;
#73621=CARTESIAN_POINT('Ctrl Pts',(79.8484771304882,240.714739226689,6.38961339026822)) ;
#73622=CARTESIAN_POINT('Ctrl Pts',(79.8422926650729,240.720787227346,6.382329552423)) ;
#73623=CARTESIAN_POINT('Ctrl Pts',(79.836125116678,240.727009754421,6.37516303641361)) ;
#73624=CARTESIAN_POINT('Ctrl Pts',(79.829977629233,240.733415831983,6.36812510586717)) ;
#73625=CARTESIAN_POINT('Ctrl Pts',(79.8111334235099,240.753052707135,6.3465513796467)) ;
#73626=CARTESIAN_POINT('Ctrl Pts',(79.7924812621589,240.774409041284,6.32618912069019)) ;
#73627=CARTESIAN_POINT('Ctrl Pts',(79.77429894775,240.797672530382,6.30766373908655)) ;
#73628=CARTESIAN_POINT('Ctrl Pts',(79.7561145116039,240.820938734152,6.28913619571245)) ;
#73629=CARTESIAN_POINT('Ctrl Pts',(79.7384101107657,240.846106021557,6.27245974990907)) ;
#73630=CARTESIAN_POINT('Ctrl Pts',(79.7214970190476,240.873450881185,6.25837194296375)) ;
#73631=CARTESIAN_POINT('Ctrl Pts',(79.7146821158104,240.884469125248,6.25269545029417)) ;
#73632=CARTESIAN_POINT('Ctrl Pts',(79.7079955681862,240.895840392378,6.24743874433886)) ;
#73633=CARTESIAN_POINT('Ctrl Pts',(79.7014921071138,240.907515086282,6.242672712917)) ;
#73634=CARTESIAN_POINT('Ctrl Pts',(79.6980536963052,240.91368755249,6.24015288943036)) ;
#73635=CARTESIAN_POINT('Ctrl Pts',(79.6946664466173,240.919944826602,6.23777018882985)) ;
#73636=CARTESIAN_POINT('Ctrl Pts',(79.6913383121865,240.926279538755,6.23553482538221)) ;
#73637=CARTESIAN_POINT('Ctrl Pts',(79.6879136502032,240.932797979742,6.23323462856712)) ;
#73638=CARTESIAN_POINT('Ctrl Pts',(79.6845476657179,240.939405752671,6.23108774124764)) ;
#73639=CARTESIAN_POINT('Ctrl Pts',(79.6812468904301,240.946100720566,6.22910489548604)) ;
#73640=CARTESIAN_POINT('Ctrl Pts',(79.6741449092849,240.960505680497,6.22483858469992)) ;
#73641=CARTESIAN_POINT('Ctrl Pts',(79.6673477720867,240.975308385753,6.22133351577758)) ;
#73642=CARTESIAN_POINT('Ctrl Pts',(79.6609436456837,240.990446791267,6.21871402346865)) ;
#73643=CARTESIAN_POINT('Ctrl Pts',(79.6582845127394,240.996732587376,6.21762635313585)) ;
#73644=CARTESIAN_POINT('Ctrl Pts',(79.6556928113517,241.003077185731,6.21669131846351)) ;
#73645=CARTESIAN_POINT('Ctrl Pts',(79.6531763820724,241.00947253337,6.21591845252413)) ;
#73646=CARTESIAN_POINT('Ctrl Pts',(79.6460361761062,241.027618920294,6.21372549521083)) ;
#73647=CARTESIAN_POINT('Ctrl Pts',(79.6395050619444,241.046169497294,6.21284107003716)) ;
#73648=CARTESIAN_POINT('Ctrl Pts',(79.6336142875784,241.06488171304,6.21317793824772)) ;
#73649=CARTESIAN_POINT('Ctrl Pts',(79.6282273107571,241.081993601263,6.21348599642979)) ;
#73650=CARTESIAN_POINT('Ctrl Pts',(79.6233733021783,241.099244782297,6.21481328366312)) ;
#73651=CARTESIAN_POINT('Ctrl Pts',(79.6190569490978,241.116492607629,6.21708379967837)) ;
#73652=CARTESIAN_POINT('Ctrl Pts',(79.6139675194462,241.136829589344,6.2197609744407)) ;
#73653=CARTESIAN_POINT('Ctrl Pts',(79.6096229368009,241.157167371827,6.22374822935041)) ;
#73654=CARTESIAN_POINT('Ctrl Pts',(79.6060732379793,241.177297802026,6.22899963880159)) ;
#73655=CARTESIAN_POINT('Ctrl Pts',(79.6048283277671,241.184357718765,6.23084135371402)) ;
#73656=CARTESIAN_POINT('Ctrl Pts',(79.6036814140677,241.191391754094,6.23283871080453)) ;
#73657=CARTESIAN_POINT('Ctrl Pts',(79.6026353815707,241.19838966958,6.23499018345485)) ;
#73658=CARTESIAN_POINT('Ctrl Pts',(79.5995061822654,241.21932388753,6.24142629967671)) ;
#73659=CARTESIAN_POINT('Ctrl Pts',(79.5971497090951,241.240005510031,6.24908072642258)) ;
#73660=CARTESIAN_POINT('Ctrl Pts',(79.5956115194735,241.260170523062,6.2578736201391)) ;
#73661=CARTESIAN_POINT('Ctrl Pts',(79.5937525470279,241.284540862756,6.2685002339889)) ;
#73662=CARTESIAN_POINT('Ctrl Pts',(79.5930888324691,241.30815681995,6.28079050605985)) ;
#73663=CARTESIAN_POINT('Ctrl Pts',(79.5933396151476,241.331054331832,6.29423684717359)) ;
#73664=CARTESIAN_POINT('Ctrl Pts',(79.5934185816702,241.338264307019,6.29847083496588)) ;
#73665=CARTESIAN_POINT('Ctrl Pts',(79.5935882572895,241.345402702503,6.30281925516304)) ;
#73666=CARTESIAN_POINT('Ctrl Pts',(79.5938400134437,241.352469723438,6.30726579180144)) ;
#73667=CARTESIAN_POINT('Ctrl Pts',(79.5942671096927,241.364458698018,6.31480919873539)) ;
#73668=CARTESIAN_POINT('Ctrl Pts',(79.5949303982531,241.376242423441,6.32263506012216)) ;
#73669=CARTESIAN_POINT('Ctrl Pts',(79.5958260797627,241.387800240562,6.33072043841245)) ;
#73670=CARTESIAN_POINT('Ctrl Pts',(79.5971357071902,241.404699589427,6.34254253483526)) ;
#73671=CARTESIAN_POINT('Ctrl Pts',(79.5989049944979,241.42116304008,6.35489088672781)) ;
#73672=CARTESIAN_POINT('Ctrl Pts',(79.6010914589459,241.437173649127,6.36767695139974)) ;
#73673=CARTESIAN_POINT('Ctrl Pts',(79.6081006167596,241.488498922498,6.40866528998672)) ;
#73674=CARTESIAN_POINT('Ctrl Pts',(79.6193970894368,241.535171381628,6.45415280681338)) ;
#73675=CARTESIAN_POINT('Ctrl Pts',(79.6333149493275,241.578268103782,6.50170615868925)) ;
#73676=CARTESIAN_POINT('Ctrl Pts',(79.634023379827,241.580461762336,6.50412666335619)) ;
#73677=CARTESIAN_POINT('Ctrl Pts',(79.6347387172234,241.58264617242,6.50655270031136)) ;
#73678=CARTESIAN_POINT('Ctrl Pts',(79.6354607419339,241.584821474574,6.5089839474707)) ;
#73679=CARTESIAN_POINT('Ctrl Pts',(79.6519191897111,241.634407169332,6.56440387122385)) ;
#73680=CARTESIAN_POINT('Ctrl Pts',(79.6718547135415,241.679255609474,6.6225313924061)) ;
#73681=CARTESIAN_POINT('Ctrl Pts',(79.6944378635415,241.720169665047,6.68231682911335)) ;
#73682=CARTESIAN_POINT('Ctrl Pts',(79.7127617888956,241.753367252641,6.73082661979756)) ;
#73683=CARTESIAN_POINT('Ctrl Pts',(79.7328279991205,241.783976003764,6.78042755176838)) ;
#73684=CARTESIAN_POINT('Ctrl Pts',(79.7541835606384,241.812447485982,6.83056033541379)) ;
#73685=CARTESIAN_POINT('Ctrl Pts',(79.7594619350772,241.819484675983,6.84295146844575)) ;
#73686=CARTESIAN_POINT('Ctrl Pts',(79.7648190500719,241.826391377569,6.85537511374401)) ;
#73687=CARTESIAN_POINT('Ctrl Pts',(79.7702523393973,241.833170083374,6.86782833897358)) ;
#73688=CARTESIAN_POINT('Ctrl Pts',(79.8060142023963,241.877787465916,6.94979535892975)) ;
#73689=CARTESIAN_POINT('Ctrl Pts',(79.8451700619027,241.916834644221,7.03316360005255)) ;
#73690=CARTESIAN_POINT('Ctrl Pts',(79.8870602112502,241.950886706729,7.11710633589805)) ;
#73691=CARTESIAN_POINT('Ctrl Pts',(79.8962920857629,241.958391200575,7.13560588330129)) ;
#73692=CARTESIAN_POINT('Ctrl Pts',(79.905656667599,241.965653268388,7.15413332186264)) ;
#73693=CARTESIAN_POINT('Ctrl Pts',(79.9151467531553,241.97267935533,7.17267980084126)) ;
#73694=CARTESIAN_POINT('Ctrl Pts',(79.8802543914407,241.738216564931,7.27867958884204)) ;
#73695=CARTESIAN_POINT('Ctrl Pts',(79.835803113544,241.705671283424,7.16318668385245)) ;
#73696=CARTESIAN_POINT('Ctrl Pts',(79.7540359687551,241.627328321488,6.93379523402446)) ;
#73697=CARTESIAN_POINT('Ctrl Pts',(79.675621293688,241.490723852039,6.66079129118985)) ;
#73698=CARTESIAN_POINT('Ctrl Pts',(79.6425666774348,241.365662283546,6.49259690874814)) ;
#73699=CARTESIAN_POINT('Ctrl Pts',(79.6342342806502,241.283068999992,6.41145082407054)) ;
#73700=CARTESIAN_POINT('Ctrl Pts',(79.6341591116984,241.182339039687,6.33519087357569)) ;
#73701=CARTESIAN_POINT('Ctrl Pts',(79.6622035595951,241.052743230527,6.30217118028935)) ;
#73702=CARTESIAN_POINT('Ctrl Pts',(79.7202959489803,240.941367844591,6.35347468345946)) ;
#73703=CARTESIAN_POINT('Ctrl Pts',(79.7661098244323,240.877657242828,6.41181318029812)) ;
#73704=CARTESIAN_POINT('Ctrl Pts',(79.8214940286967,240.815857306447,6.49328852242612)) ;
#73705=CARTESIAN_POINT('Ctrl Pts',(79.9216310945127,240.734075598131,6.66117971759687)) ;
#73706=CARTESIAN_POINT('Ctrl Pts',(80.065413735872,240.669690330056,6.93433585613084)) ;
#73707=CARTESIAN_POINT('Ctrl Pts',(80.1774132992676,240.65430786939,7.16318984184328)) ;
#73708=CARTESIAN_POINT('Ctrl Pts',(80.23250326861,240.654105994678,7.27867958884203)) ;
#73709=CARTESIAN_POINT('Origin',(80.2317703825363,240.454107337488,16.0213203435596)) ;
#73710=CARTESIAN_POINT('',(80.2325032686099,240.654105994678,16.0254384350469)) ;
#73711=CARTESIAN_POINT('',(80.2325032686099,240.654105994678,16.0213203435596)) ;
#73712=CARTESIAN_POINT('Ctrl Pts',(80.2325032686099,240.654105994678,16.0254384350469)) ;
#73713=CARTESIAN_POINT('Ctrl Pts',(80.2525180685422,240.654032651345,16.0294645582753)) ;
#73714=CARTESIAN_POINT('Ctrl Pts',(80.2716580279919,240.650963547834,16.0362204083692)) ;
#73715=CARTESIAN_POINT('Ctrl Pts',(80.3123201058787,240.638727230937,16.056050217191)) ;
#73716=CARTESIAN_POINT('Ctrl Pts',(80.3326046787805,240.628154412355,16.070223718736)) ;
#73717=CARTESIAN_POINT('Ctrl Pts',(80.3709047298332,240.600116457484,16.1046945816758)) ;
#73718=CARTESIAN_POINT('Ctrl Pts',(80.3877788781721,240.58149662584,16.1258672215767)) ;
#73719=CARTESIAN_POINT('Ctrl Pts',(80.414163561157,240.539994322448,16.1708720249643)) ;
#73720=CARTESIAN_POINT('Ctrl Pts',(80.4233513019733,240.516556473268,16.1951765216869)) ;
#73721=CARTESIAN_POINT('Ctrl Pts',(80.4281898988627,240.491788007084,16.2199877856666)) ;
#73722=CARTESIAN_POINT('Ctrl Pts',(80.4283164474799,240.491122247836,16.2206540664846)) ;
#73723=CARTESIAN_POINT('Ctrl Pts',(80.4284396085183,240.490455866367,16.2213203435596)) ;
#73724=CARTESIAN_POINT('Origin',(69.2946204451421,236.900411902176,16.0213203435596)) ;
#73725=CARTESIAN_POINT('',(69.1764712666787,237.061783435069,16.0254384350468)) ;
#73726=CARTESIAN_POINT('',(69.1764712666787,237.061783435069,16.0213203435596)) ;
#73727=CARTESIAN_POINT('Ctrl Pts',(69.1141465698345,236.814219209148,16.2213203435596)) ;
#73728=CARTESIAN_POINT('Ctrl Pts',(69.113854520009,236.81483071532,16.2206540664882)) ;
#73729=CARTESIAN_POINT('Ctrl Pts',(69.1135655765251,236.815443709273,16.2199877856604)) ;
#73730=CARTESIAN_POINT('Ctrl Pts',(69.1045283400562,236.834871642603,16.1989219660652)) ;
#73731=CARTESIAN_POINT('Ctrl Pts',(69.0986514909987,236.855161355671,16.1784289743247)) ;
#73732=CARTESIAN_POINT('Ctrl Pts',(69.0936354075348,236.896382972379,16.1396302534571)) ;
#73733=CARTESIAN_POINT('Ctrl Pts',(69.0941763076024,236.917471021874,16.1210537743952)) ;
#73734=CARTESIAN_POINT('Ctrl Pts',(69.102705057958,236.961169770065,16.0855257632304)) ;
#73735=CARTESIAN_POINT('Ctrl Pts',(69.1111768180338,236.984091981047,16.068487609431)) ;
#73736=CARTESIAN_POINT('Ctrl Pts',(69.1347335181114,237.022074758818,16.0440628922076)) ;
#73737=CARTESIAN_POINT('Ctrl Pts',(69.1475896237123,237.037598042927,16.0353723461956)) ;
#73738=CARTESIAN_POINT('Ctrl Pts',(69.1675780589742,237.054979433805,16.0279192770399)) ;
#73739=CARTESIAN_POINT('Ctrl Pts',(69.1719432176706,237.058468195629,16.0265673132408)) ;
#73740=CARTESIAN_POINT('Ctrl Pts',(69.1764712666784,237.061783435069,16.0254384350469)) ;
#73741=CARTESIAN_POINT('Origin',(74.5283628290597,239.4,7.2786795888419)) ;
#73742=CARTESIAN_POINT('Origin',(74.5283628290597,239.4,7.17267980084126)) ;
#73743=CARTESIAN_POINT('Origin',(79.7621052129773,241.899588097824,16.0213203435596)) ;
#73744=CARTESIAN_POINT('',(79.8802543914406,241.73821656493,16.0254384350469)) ;
#73745=CARTESIAN_POINT('',(79.8802543914406,241.73821656493,16.0213203435596)) ;
#73746=CARTESIAN_POINT('Ctrl Pts',(79.9425790882849,241.985780790852,16.2213203435596)) ;
#73747=CARTESIAN_POINT('Ctrl Pts',(79.9428711381098,241.985169284681,16.2206540664895)) ;
#73748=CARTESIAN_POINT('Ctrl Pts',(79.9431600815935,241.984556290729,16.2199877856614)) ;
#73749=CARTESIAN_POINT('Ctrl Pts',(79.952197318064,241.965128357396,16.1989219660712)) ;
#73750=CARTESIAN_POINT('Ctrl Pts',(79.9580741671204,241.944838644331,16.178428974326)) ;
#73751=CARTESIAN_POINT('Ctrl Pts',(79.9630902505847,241.903617027621,16.1396302534574)) ;
#73752=CARTESIAN_POINT('Ctrl Pts',(79.962549350517,241.882528978126,16.121053774395)) ;
#73753=CARTESIAN_POINT('Ctrl Pts',(79.9540206001612,241.838830229934,16.0855257632299)) ;
#73754=CARTESIAN_POINT('Ctrl Pts',(79.9455488400853,241.815908018952,16.0684876094306)) ;
#73755=CARTESIAN_POINT('Ctrl Pts',(79.9219921400076,241.777925241182,16.0440628922073)) ;
#73756=CARTESIAN_POINT('Ctrl Pts',(79.9091360344067,241.762401957072,16.0353723461954)) ;
#73757=CARTESIAN_POINT('Ctrl Pts',(79.8891475991448,241.745020566195,16.0279192770397)) ;
#73758=CARTESIAN_POINT('Ctrl Pts',(79.8847824404483,241.74153180437,16.0265673132406)) ;
#73759=CARTESIAN_POINT('Ctrl Pts',(79.8802543914405,241.73821656493,16.0254384350468)) ;
#73760=CARTESIAN_POINT('Origin',(74.5283628290597,239.4,16.2213203435596)) ;
#73761=CARTESIAN_POINT('',(80.1907997307331,240.655710290858,16.0213203435596)) ;
#73762=CARTESIAN_POINT('Ctrl Pts',(80.2325032686099,240.654105994679,16.0254384350468)) ;
#73763=CARTESIAN_POINT('Ctrl Pts',(80.2214662170119,240.654146439457,16.0232182514845)) ;
#73764=CARTESIAN_POINT('Ctrl Pts',(80.2102345744082,240.654493678325,16.0218983740811)) ;
#73765=CARTESIAN_POINT('Ctrl Pts',(80.1962025575493,240.655332274339,16.0213707571522)) ;
#73766=CARTESIAN_POINT('Ctrl Pts',(80.1934993776713,240.655512225888,16.0213203435596)) ;
#73767=CARTESIAN_POINT('Ctrl Pts',(80.1907997307331,240.655710290859,16.0213203435596)) ;
#73768=CARTESIAN_POINT('',(79.8474585022076,241.712405937524,16.0213203435596)) ;
#73769=CARTESIAN_POINT('Origin',(74.5283628290597,239.4,16.0213203435596)) ;
#73770=CARTESIAN_POINT('Ctrl Pts',(79.8474585022072,241.712405937525,16.0213203435596)) ;
#73771=CARTESIAN_POINT('Ctrl Pts',(79.8560750880036,241.719686511994,16.0213203435596)) ;
#73772=CARTESIAN_POINT('Ctrl Pts',(79.8649010067008,241.726725392249,16.0221950109068)) ;
#73773=CARTESIAN_POINT('Ctrl Pts',(79.8759887977938,241.735071840198,16.0244263118334)) ;
#73774=CARTESIAN_POINT('Ctrl Pts',(79.8781221611223,241.736655439149,16.0249068532758)) ;
#73775=CARTESIAN_POINT('Ctrl Pts',(79.8802543914402,241.738216564931,16.0254384350467)) ;
#73776=CARTESIAN_POINT('Origin',(68.824955275583,238.345892662512,16.0213203435596)) ;
#73777=CARTESIAN_POINT('',(68.8242223895095,238.145894005322,16.0254384350468)) ;
#73778=CARTESIAN_POINT('',(68.8242223895095,238.145894005322,16.0213203435596)) ;
#73779=CARTESIAN_POINT('Ctrl Pts',(68.8242223895095,238.145894005322,16.0254384350468)) ;
#73780=CARTESIAN_POINT('Ctrl Pts',(68.8042075895772,238.145967348655,16.0294645582753)) ;
#73781=CARTESIAN_POINT('Ctrl Pts',(68.7850676301275,238.149036452166,16.0362204083691)) ;
#73782=CARTESIAN_POINT('Ctrl Pts',(68.7444055522406,238.161272769063,16.056050217191)) ;
#73783=CARTESIAN_POINT('Ctrl Pts',(68.7241209793388,238.171845587645,16.0702237187361)) ;
#73784=CARTESIAN_POINT('Ctrl Pts',(68.6858209282861,238.199883542516,16.1046945816758)) ;
#73785=CARTESIAN_POINT('Ctrl Pts',(68.6689467799472,238.218503374159,16.1258672215767)) ;
#73786=CARTESIAN_POINT('Ctrl Pts',(68.6425620969623,238.260005677552,16.1708720249643)) ;
#73787=CARTESIAN_POINT('Ctrl Pts',(68.6333743561474,238.283443526724,16.1951765216964)) ;
#73788=CARTESIAN_POINT('Ctrl Pts',(68.6285357592563,238.308211992918,16.2199877856667)) ;
#73789=CARTESIAN_POINT('Ctrl Pts',(68.6284092106395,238.308877752164,16.2206540664842)) ;
#73790=CARTESIAN_POINT('Ctrl Pts',(68.6282860496011,238.309544133633,16.2213203435596)) ;
#73791=CARTESIAN_POINT('Origin',(74.5283628290597,239.4,16.2213203435596)) ;
#73792=CARTESIAN_POINT('',(68.8659259273863,238.144289709142,16.0213203435596)) ;
#73793=CARTESIAN_POINT('Ctrl Pts',(68.8242223895095,238.145894005322,16.0254384350468)) ;
#73794=CARTESIAN_POINT('Ctrl Pts',(68.8352594411076,238.145853560543,16.0232182514845)) ;
#73795=CARTESIAN_POINT('Ctrl Pts',(68.8464910837112,238.145506321675,16.0218983740811)) ;
#73796=CARTESIAN_POINT('Ctrl Pts',(68.8605231005701,238.144667725661,16.0213707571522)) ;
#73797=CARTESIAN_POINT('Ctrl Pts',(68.8632262804481,238.144487774112,16.0213203435596)) ;
#73798=CARTESIAN_POINT('Ctrl Pts',(68.8659259273863,238.144289709142,16.0213203435596)) ;
#73799=CARTESIAN_POINT('',(69.2092671559117,237.087594062475,16.0213203435596)) ;
#73800=CARTESIAN_POINT('Origin',(74.5283628290597,239.4,16.0213203435596)) ;
#73801=CARTESIAN_POINT('Ctrl Pts',(69.2092671559116,237.087594062475,16.0213203435596)) ;
#73802=CARTESIAN_POINT('Ctrl Pts',(69.2006505701154,237.080313488006,16.0213203435596)) ;
#73803=CARTESIAN_POINT('Ctrl Pts',(69.1918246514184,237.073274607751,16.0221950109068)) ;
#73804=CARTESIAN_POINT('Ctrl Pts',(69.1807368603254,237.064928159802,16.0244263118334)) ;
#73805=CARTESIAN_POINT('Ctrl Pts',(69.1786034969968,237.06334456085,16.0249068532759)) ;
#73806=CARTESIAN_POINT('Ctrl Pts',(69.1764712666787,237.061783435069,16.0254384350469)) ;
#73807=CARTESIAN_POINT('Ctrl Pts',(78.8957655188814,243.277601545423,7.27867958886638)) ;
#73808=CARTESIAN_POINT('Ctrl Pts',(78.8635406538411,243.232904298188,7.16316434207538)) ;
#73809=CARTESIAN_POINT('Ctrl Pts',(78.8166813609821,243.145809292233,6.96275402987872)) ;
#73810=CARTESIAN_POINT('Ctrl Pts',(78.7894462740705,243.032917191841,6.75724340359379)) ;
#73811=CARTESIAN_POINT('Ctrl Pts',(78.7835736824138,242.966127546698,6.65331354906745)) ;
#73812=CARTESIAN_POINT('Ctrl Pts',(78.7800312335663,242.880452545767,6.52713876856571)) ;
#73813=CARTESIAN_POINT('Ctrl Pts',(78.7936621040222,242.761889135694,6.38460879774661)) ;
#73814=CARTESIAN_POINT('Ctrl Pts',(78.882776252335,242.581776447516,6.30139782015858)) ;
#73815=CARTESIAN_POINT('Ctrl Pts',(78.9713921561075,242.483020602554,6.33510444744903)) ;
#73816=CARTESIAN_POINT('Ctrl Pts',(79.0528714154968,242.423850222314,6.41121110896327)) ;
#73817=CARTESIAN_POINT('Ctrl Pts',(79.1246096777318,242.38205224677,6.49241324931206)) ;
#73818=CARTESIAN_POINT('Ctrl Pts',(79.2452124162956,242.335284322678,6.66060069906232)) ;
#73819=CARTESIAN_POINT('Ctrl Pts',(79.4018524165444,242.318447164155,6.93370165979781)) ;
#73820=CARTESIAN_POINT('Ctrl Pts',(79.5133244990962,242.33856958246,7.16318512433992)) ;
#73821=CARTESIAN_POINT('Ctrl Pts',(79.5657826988536,242.355402012486,7.27867958884205)) ;
#73822=CARTESIAN_POINT('Ctrl Pts',(78.9223274213339,243.314444024655,7.2497920761008)) ;
#73823=CARTESIAN_POINT('Ctrl Pts',(78.8850055027858,243.269988257635,7.1355582627038)) ;
#73824=CARTESIAN_POINT('Ctrl Pts',(78.8295487878093,243.181250060656,6.93705316628695)) ;
#73825=CARTESIAN_POINT('Ctrl Pts',(78.79443887902,243.063184983711,6.7331427106619)) ;
#73826=CARTESIAN_POINT('Ctrl Pts',(78.7851346722495,242.992610689095,6.62995847244708)) ;
#73827=CARTESIAN_POINT('Ctrl Pts',(78.7776699511723,242.901880178901,6.50466949064327)) ;
#73828=CARTESIAN_POINT('Ctrl Pts',(78.7882507062251,242.774922910966,6.36302179397673)) ;
#73829=CARTESIAN_POINT('Ctrl Pts',(78.8812529483899,242.581900610752,6.28029626114192)) ;
#73830=CARTESIAN_POINT('Ctrl Pts',(78.9765146123003,242.477074597148,6.31380866775496)) ;
#73831=CARTESIAN_POINT('Ctrl Pts',(79.0645077757404,242.415741033935,6.38945550249625)) ;
#73832=CARTESIAN_POINT('Ctrl Pts',(79.1419656410233,242.373212149684,6.47014974693021)) ;
#73833=CARTESIAN_POINT('Ctrl Pts',(79.2719287950657,242.327970036664,6.6372286847837)) ;
#73834=CARTESIAN_POINT('Ctrl Pts',(79.4389924679933,242.318509674686,6.90827654234774)) ;
#73835=CARTESIAN_POINT('Ctrl Pts',(79.5552266855363,242.347525178783,7.13557881442655)) ;
#73836=CARTESIAN_POINT('Ctrl Pts',(79.6090300580634,242.3692789307,7.24979207607673)) ;
#73837=CARTESIAN_POINT('Ctrl Pts',(78.9358673079361,243.401953071295,7.19960840329867)) ;
#73838=CARTESIAN_POINT('Ctrl Pts',(78.8917112313382,243.352062624275,7.08745252517629)) ;
#73839=CARTESIAN_POINT('Ctrl Pts',(78.8257448247605,243.252491402447,6.89208991795338)) ;
#73840=CARTESIAN_POINT('Ctrl Pts',(78.7833339311877,243.11958953286,6.69086538804954)) ;
#73841=CARTESIAN_POINT('Ctrl Pts',(78.7714822977875,243.040196918718,6.58894321460344)) ;
#73842=CARTESIAN_POINT('Ctrl Pts',(78.7614184058194,242.938158012405,6.46515699374508)) ;
#73843=CARTESIAN_POINT('Ctrl Pts',(78.7715725864411,242.795537886239,6.32502691287734)) ;
#73844=CARTESIAN_POINT('Ctrl Pts',(78.8746244794737,242.579388215166,6.24314145731071)) ;
#73845=CARTESIAN_POINT('Ctrl Pts',(78.9813155195012,242.462582539517,6.27631699480972)) ;
#73846=CARTESIAN_POINT('Ctrl Pts',(79.080293196982,242.394732278809,6.35117086109098)) ;
#73847=CARTESIAN_POINT('Ctrl Pts',(79.1675719341539,242.347961153938,6.43099283075982)) ;
#73848=CARTESIAN_POINT('Ctrl Pts',(79.314304889617,242.299146827055,6.59617796284487)) ;
#73849=CARTESIAN_POINT('Ctrl Pts',(79.5034918835788,242.29208610874,6.86376506350529)) ;
#73850=CARTESIAN_POINT('Ctrl Pts',(79.6353575406729,242.328541198735,7.08747270305917)) ;
#73851=CARTESIAN_POINT('Ctrl Pts',(79.6964401621657,242.355114345509,7.19960840327504)) ;
#73852=CARTESIAN_POINT('Ctrl Pts',(78.885706249036,243.48371233892,7.17608503413733)) ;
#73853=CARTESIAN_POINT('Ctrl Pts',(78.8419480295462,243.426187165054,7.06213458186481)) ;
#73854=CARTESIAN_POINT('Ctrl Pts',(78.7779908352468,243.313384703808,6.86414331997508)) ;
#73855=CARTESIAN_POINT('Ctrl Pts',(78.7401538986497,243.165798805056,6.66077230046967)) ;
#73856=CARTESIAN_POINT('Ctrl Pts',(78.7315394990012,243.078165584419,6.55786216980516)) ;
#73857=CARTESIAN_POINT('Ctrl Pts',(78.7258439115146,242.965657464675,6.43290637600473)) ;
#73858=CARTESIAN_POINT('Ctrl Pts',(78.7429220836931,242.809363558599,6.29163643302005)) ;
#73859=CARTESIAN_POINT('Ctrl Pts',(78.8603129422467,242.571305830164,6.20913121818275)) ;
#73860=CARTESIAN_POINT('Ctrl Pts',(78.9775204042057,242.440886187788,6.24255434951516)) ;
#73861=CARTESIAN_POINT('Ctrl Pts',(79.0852206169547,242.363148138656,6.31799957071972)) ;
#73862=CARTESIAN_POINT('Ctrl Pts',(79.1799837053198,242.308472216173,6.3984787601664)) ;
#73863=CARTESIAN_POINT('Ctrl Pts',(79.3390667698205,242.248062299045,6.56511256803953)) ;
#73864=CARTESIAN_POINT('Ctrl Pts',(79.5449231900932,242.228718340238,6.83544080204649)) ;
#73865=CARTESIAN_POINT('Ctrl Pts',(79.6904777773622,242.258307346071,7.06215508260826)) ;
#73866=CARTESIAN_POINT('Ctrl Pts',(79.7586972267504,242.282143340434,7.17608503411332)) ;
#73867=CARTESIAN_POINT('Ctrl Pts',(78.8564971400792,243.511371242808,7.17267980086576)) ;
#73868=CARTESIAN_POINT('Ctrl Pts',(78.8138048922264,243.451486215648,7.05716455407476)) ;
#73869=CARTESIAN_POINT('Ctrl Pts',(78.7521698261773,243.33447060512,6.85675424187814)) ;
#73870=CARTESIAN_POINT('Ctrl Pts',(78.717654904468,243.181984925503,6.6512436155932)) ;
#73871=CARTESIAN_POINT('Ctrl Pts',(78.7111008184567,243.091493832933,6.54731376106682)) ;
#73872=CARTESIAN_POINT('Ctrl Pts',(78.7080889934782,242.975308192762,6.42113898056508)) ;
#73873=CARTESIAN_POINT('Ctrl Pts',(78.7290363766315,242.813992657412,6.27860900974601)) ;
#73874=CARTESIAN_POINT('Ctrl Pts',(78.8530816050133,242.567036921856,6.19539803215796)) ;
#73875=CARTESIAN_POINT('Ctrl Pts',(78.974544375891,242.430648427085,6.22910465944839)) ;
#73876=CARTESIAN_POINT('Ctrl Pts',(79.08541149884,242.348357089493,6.30521132096265)) ;
#73877=CARTESIAN_POINT('Ctrl Pts',(79.1827615086478,242.289958082444,6.38641346131143)) ;
#73878=CARTESIAN_POINT('Ctrl Pts',(79.345820343214,242.223883095797,6.5546009110617)) ;
#73879=CARTESIAN_POINT('Ctrl Pts',(79.556540488253,242.198132848066,6.82770187179718)) ;
#73880=CARTESIAN_POINT('Ctrl Pts',(79.7058422410964,242.22372348177,7.0571853363393)) ;
#73881=CARTESIAN_POINT('Ctrl Pts',(79.7759762964688,242.245816755679,7.17267980084142)) ;
#73882=CARTESIAN_POINT('Ctrl Pts',(79.7759762964688,242.245816755679,7.17267980084142)) ;
#73883=CARTESIAN_POINT('Ctrl Pts',(79.7232193461811,242.229197529155,7.08580138364638)) ;
#73884=CARTESIAN_POINT('Ctrl Pts',(79.6678914478665,242.217855098603,6.99933943687075)) ;
#73885=CARTESIAN_POINT('Ctrl Pts',(79.6099012824163,242.212757564659,6.91420575471137)) ;
#73886=CARTESIAN_POINT('Ctrl Pts',(79.5993389727162,242.2118291015,6.89869953378746)) ;
#73887=CARTESIAN_POINT('Ctrl Pts',(79.5886884059039,242.211107688293,6.8832373733379)) ;
#73888=CARTESIAN_POINT('Ctrl Pts',(79.5779491165789,242.210598998763,6.86782476897472)) ;
#73889=CARTESIAN_POINT('Ctrl Pts',(79.5692533403923,242.210187104627,6.85534493404905)) ;
#73890=CARTESIAN_POINT('Ctrl Pts',(79.5604985101053,242.209912688296,6.84289479517368)) ;
#73891=CARTESIAN_POINT('Ctrl Pts',(79.5516841294921,242.209779310136,6.8304773353399)) ;
#73892=CARTESIAN_POINT('Ctrl Pts',(79.5069926687389,242.209103044261,6.76751722014109)) ;
#73893=CARTESIAN_POINT('Ctrl Pts',(79.4607683535687,242.212055319315,6.70539635549695)) ;
#73894=CARTESIAN_POINT('Ctrl Pts',(79.4128176850172,242.2198822012,6.64522313485622)) ;
#73895=CARTESIAN_POINT('Ctrl Pts',(79.3755141178245,242.225971180209,6.59841094542943)) ;
#73896=CARTESIAN_POINT('Ctrl Pts',(79.3371660871178,242.235010068117,6.55277794871554)) ;
#73897=CARTESIAN_POINT('Ctrl Pts',(79.2976938567602,242.247566646749,6.50884764848157)) ;
#73898=CARTESIAN_POINT('Ctrl Pts',(79.29554782224,242.248249325456,6.50645923668091)) ;
#73899=CARTESIAN_POINT('Ctrl Pts',(79.2933984675045,242.248942396971,6.50407585761679)) ;
#73900=CARTESIAN_POINT('Ctrl Pts',(79.2912458053789,242.24964610781,6.50169781367092)) ;
#73901=CARTESIAN_POINT('Ctrl Pts',(79.2481610140484,242.263730637972,6.45410208280152)) ;
#73902=CARTESIAN_POINT('Ctrl Pts',(79.2037281831097,242.282048812277,6.40858833733514)) ;
#73903=CARTESIAN_POINT('Ctrl Pts',(79.1580399707387,242.306577949011,6.36756443793904)) ;
#73904=CARTESIAN_POINT('Ctrl Pts',(79.1438410202519,242.314201096862,6.35481505935611)) ;
#73905=CARTESIAN_POINT('Ctrl Pts',(79.1295207322322,242.322424215564,6.34249926125844)) ;
#73906=CARTESIAN_POINT('Ctrl Pts',(79.1151203415642,242.331272739319,6.33071074220801)) ;
#73907=CARTESIAN_POINT('Ctrl Pts',(79.1052060542713,242.337364713394,6.32259465929625)) ;
#73908=CARTESIAN_POINT('Ctrl Pts',(79.0952451490836,242.343777718423,6.3147383662346)) ;
#73909=CARTESIAN_POINT('Ctrl Pts',(79.0852580707614,242.350503720341,6.30716801584339)) ;
#73910=CARTESIAN_POINT('Ctrl Pts',(79.066498156481,242.363137967851,6.29294772840495)) ;
#73911=CARTESIAN_POINT('Ctrl Pts',(79.0476478742883,242.37687482735,6.2797379183036)) ;
#73912=CARTESIAN_POINT('Ctrl Pts',(79.0288431685158,242.391954252342,6.26803790430659)) ;
#73913=CARTESIAN_POINT('Ctrl Pts',(79.0231090081396,242.396552454639,6.26447019325204)) ;
#73914=CARTESIAN_POINT('Ctrl Pts',(79.0173788556137,242.40127569621,6.26104268604071)) ;
#73915=CARTESIAN_POINT('Ctrl Pts',(79.0116559086474,242.40613130245,6.25776900129401)) ;
#73916=CARTESIAN_POINT('Ctrl Pts',(78.9962659455198,242.419188841064,6.24896551458699)) ;
#73917=CARTESIAN_POINT('Ctrl Pts',(78.9809298436631,242.433202118851,6.24127537358637)) ;
#73918=CARTESIAN_POINT('Ctrl Pts',(78.9658408069922,242.447981105764,6.23479051959553)) ;
#73919=CARTESIAN_POINT('Ctrl Pts',(78.9519571307252,242.461579500037,6.22882369643702)) ;
#73920=CARTESIAN_POINT('Ctrl Pts',(78.938297864686,242.475964516107,6.22402506716956)) ;
#73921=CARTESIAN_POINT('Ctrl Pts',(78.924995550496,242.490971147193,6.22043027857374)) ;
#73922=CARTESIAN_POINT('Ctrl Pts',(78.9196512063887,242.497000218471,6.21898603458919)) ;
#73923=CARTESIAN_POINT('Ctrl Pts',(78.9143642429595,242.503130141156,6.2177362717046)) ;
#73924=CARTESIAN_POINT('Ctrl Pts',(78.9091423730922,242.50935227171,6.21668407135727)) ;
#73925=CARTESIAN_POINT('Ctrl Pts',(78.8967790392163,242.524083829448,6.21419287480723)) ;
#73926=CARTESIAN_POINT('Ctrl Pts',(78.8847765441358,242.539338038286,6.21280926967955)) ;
#73927=CARTESIAN_POINT('Ctrl Pts',(78.8733271793744,242.555016814374,6.21270853878516)) ;
#73928=CARTESIAN_POINT('Ctrl Pts',(78.8718843166039,242.556992672666,6.21269584455623)) ;
#73929=CARTESIAN_POINT('Ctrl Pts',(78.8704502764347,242.558975217609,6.21270352039433)) ;
#73930=CARTESIAN_POINT('Ctrl Pts',(78.8690254763894,242.560964204611,6.212731913334)) ;
#73931=CARTESIAN_POINT('Ctrl Pts',(78.8598605994944,242.573758154948,6.21291454794133)) ;
#73932=CARTESIAN_POINT('Ctrl Pts',(78.8510567308864,242.586800007912,6.2139087962786)) ;
#73933=CARTESIAN_POINT('Ctrl Pts',(78.8426724286616,242.599987892594,6.21570167975813)) ;
#73934=CARTESIAN_POINT('Ctrl Pts',(78.8402465142696,242.603803675755,6.21622043274669)) ;
#73935=CARTESIAN_POINT('Ctrl Pts',(78.8378555423078,242.607631831192,6.21680593800229)) ;
#73936=CARTESIAN_POINT('Ctrl Pts',(78.835498646092,242.611469363401,6.21745376350985)) ;
#73937=CARTESIAN_POINT('Ctrl Pts',(78.8257292807457,242.627375984117,6.22013900863075)) ;
#73938=CARTESIAN_POINT('Ctrl Pts',(78.8165816142084,242.643441255929,6.22393977750336)) ;
#73939=CARTESIAN_POINT('Ctrl Pts',(78.8080789759729,242.659535824001,6.22873230041116)) ;
#73940=CARTESIAN_POINT('Ctrl Pts',(78.8028449725826,242.66944322233,6.23168245311112)) ;
#73941=CARTESIAN_POINT('Ctrl Pts',(78.7978561370969,242.679361044475,6.23500875046676)) ;
#73942=CARTESIAN_POINT('Ctrl Pts',(78.7931247857659,242.689252533828,6.23868459605083)) ;
#73943=CARTESIAN_POINT('Ctrl Pts',(78.7857782191515,242.704611462041,6.24439223485403)) ;
#73944=CARTESIAN_POINT('Ctrl Pts',(78.7789906786787,242.719977150002,6.25093270073982)) ;
#73945=CARTESIAN_POINT('Ctrl Pts',(78.7727739048653,242.735180703857,6.25813416293056)) ;
#73946=CARTESIAN_POINT('Ctrl Pts',(78.7640306078395,242.756563046402,6.26826232986162)) ;
#73947=CARTESIAN_POINT('Ctrl Pts',(78.7564179084365,242.777622793233,6.27969809988633)) ;
#73948=CARTESIAN_POINT('Ctrl Pts',(78.7498196180722,242.798301334159,6.29219975216049)) ;
#73949=CARTESIAN_POINT('Ctrl Pts',(78.742764251576,242.820412316971,6.30556741768171)) ;
#73950=CARTESIAN_POINT('Ctrl Pts',(78.7368685023543,242.842087327435,6.32015310285032)) ;
#73951=CARTESIAN_POINT('Ctrl Pts',(78.731946840072,242.863288277844,6.33563841294475)) ;
#73952=CARTESIAN_POINT('Ctrl Pts',(78.7307013116998,242.868653616572,6.3395572907484)) ;
#73953=CARTESIAN_POINT('Ctrl Pts',(78.7295179741353,242.873988756594,6.34353370729427)) ;
#73954=CARTESIAN_POINT('Ctrl Pts',(78.7283934480067,242.879293401602,6.3475623765746)) ;
#73955=CARTESIAN_POINT('Ctrl Pts',(78.7223362189441,242.907866726037,6.36926269284759)) ;
#73956=CARTESIAN_POINT('Ctrl Pts',(78.718071336267,242.935547325288,6.39257820320909)) ;
#73957=CARTESIAN_POINT('Ctrl Pts',(78.7152239333612,242.962358867744,6.4169448327128)) ;
#73958=CARTESIAN_POINT('Ctrl Pts',(78.7120287473669,242.992445184214,6.44428761344905)) ;
#73959=CARTESIAN_POINT('Ctrl Pts',(78.710618917116,243.021437583673,6.47295541130282)) ;
#73960=CARTESIAN_POINT('Ctrl Pts',(78.7105120445948,243.049335951623,6.5021775037322)) ;
#73961=CARTESIAN_POINT('Ctrl Pts',(78.7105030190479,243.051692011209,6.5046453538628)) ;
#73962=CARTESIAN_POINT('Ctrl Pts',(78.7105033080588,243.054040248191,6.50711716242569)) ;
#73963=CARTESIAN_POINT('Ctrl Pts',(78.7105126321779,243.056380651557,6.50959246668126)) ;
#73964=CARTESIAN_POINT('Ctrl Pts',(78.7105597699396,243.068212479896,6.52210628180374)) ;
#73965=CARTESIAN_POINT('Ctrl Pts',(78.7108377274563,243.079844158621,6.53470937925584)) ;
#73966=CARTESIAN_POINT('Ctrl Pts',(78.7113824377319,243.091325519317,6.54751229341178)) ;
#73967=CARTESIAN_POINT('Ctrl Pts',(78.7118695050782,243.101591886844,6.55896036351707)) ;
#73968=CARTESIAN_POINT('Ctrl Pts',(78.7125699081622,243.111738076409,6.57056828687344)) ;
#73969=CARTESIAN_POINT('Ctrl Pts',(78.7134534138245,243.121756758647,6.58227904590185)) ;
#73970=CARTESIAN_POINT('Ctrl Pts',(78.7135566743772,243.122927701528,6.58364775184477)) ;
#73971=CARTESIAN_POINT('Ctrl Pts',(78.7136623208108,243.12409688938,6.58501770970791)) ;
#73972=CARTESIAN_POINT('Ctrl Pts',(78.7137702989929,243.125264309918,6.58638882085528)) ;
#73973=CARTESIAN_POINT('Ctrl Pts',(78.7184533488328,243.175895728805,6.64585436952773)) ;
#73974=CARTESIAN_POINT('Ctrl Pts',(78.7275259043401,243.223199800337,6.7074904562158)) ;
#73975=CARTESIAN_POINT('Ctrl Pts',(78.7400249137594,243.267677630087,6.77035648044285)) ;
#73976=CARTESIAN_POINT('Ctrl Pts',(78.7440175315536,243.281885393962,6.79043807239623)) ;
#73977=CARTESIAN_POINT('Ctrl Pts',(78.7483594753108,243.295805040432,6.81064506724375)) ;
#73978=CARTESIAN_POINT('Ctrl Pts',(78.7530185895239,243.309453604173,6.83094660614969)) ;
#73979=CARTESIAN_POINT('Ctrl Pts',(78.7660061234082,243.347499716791,6.8875382483337)) ;
#73980=CARTESIAN_POINT('Ctrl Pts',(78.7814591606107,243.383438265301,6.94486438343817)) ;
#73981=CARTESIAN_POINT('Ctrl Pts',(78.7990763319058,243.417432743563,7.00265863085758)) ;
#73982=CARTESIAN_POINT('Ctrl Pts',(78.8162440599792,243.450559966375,7.058978451292)) ;
#73983=CARTESIAN_POINT('Ctrl Pts',(78.8354493994883,243.481847275802,7.11572953305104)) ;
#73984=CARTESIAN_POINT('Ctrl Pts',(78.8564971400704,243.511371242796,7.17267980084187)) ;
#73985=CARTESIAN_POINT('Ctrl Pts',(78.8957655188814,243.277601545423,7.27867958886638)) ;
#73986=CARTESIAN_POINT('Ctrl Pts',(78.8635406538411,243.232904298188,7.16316434207538)) ;
#73987=CARTESIAN_POINT('Ctrl Pts',(78.8166813609821,243.145809292233,6.96275402987872)) ;
#73988=CARTESIAN_POINT('Ctrl Pts',(78.7894462740705,243.032917191841,6.75724340359379)) ;
#73989=CARTESIAN_POINT('Ctrl Pts',(78.7835736824138,242.966127546698,6.65331354906745)) ;
#73990=CARTESIAN_POINT('Ctrl Pts',(78.7800312335663,242.880452545767,6.52713876856571)) ;
#73991=CARTESIAN_POINT('Ctrl Pts',(78.7936621040222,242.761889135694,6.38460879774661)) ;
#73992=CARTESIAN_POINT('Ctrl Pts',(78.882776252335,242.581776447516,6.30139782015858)) ;
#73993=CARTESIAN_POINT('Ctrl Pts',(78.9713921561075,242.483020602554,6.33510444744903)) ;
#73994=CARTESIAN_POINT('Ctrl Pts',(79.0528714154968,242.423850222314,6.41121110896327)) ;
#73995=CARTESIAN_POINT('Ctrl Pts',(79.1246096777318,242.38205224677,6.49241324931206)) ;
#73996=CARTESIAN_POINT('Ctrl Pts',(79.2452124162956,242.335284322678,6.66060069906232)) ;
#73997=CARTESIAN_POINT('Ctrl Pts',(79.4018524165444,242.318447164155,6.93370165979781)) ;
#73998=CARTESIAN_POINT('Ctrl Pts',(79.5133244990962,242.33856958246,7.16318512433992)) ;
#73999=CARTESIAN_POINT('Ctrl Pts',(79.5657826988536,242.355402012486,7.27867958884205)) ;
#74000=CARTESIAN_POINT('Origin',(79.6268886667016,242.164965512063,16.0213203435596)) ;
#74001=CARTESIAN_POINT('',(79.5657826988536,242.355402012486,16.0254384350469)) ;
#74002=CARTESIAN_POINT('',(79.5657826988536,242.355402012486,16.0213203435596)) ;
#74003=CARTESIAN_POINT('Ctrl Pts',(79.5657826988536,242.355402012486,16.0254384350469)) ;
#74004=CARTESIAN_POINT('Ctrl Pts',(79.5848405690879,242.361517172149,16.0294645582753)) ;
#74005=CARTESIAN_POINT('Ctrl Pts',(79.6039921573866,242.364512853997,16.0362204083692)) ;
#74006=CARTESIAN_POINT('Ctrl Pts',(79.6464453213966,242.365440698171,16.056050217191)) ;
#74007=CARTESIAN_POINT('Ctrl Pts',(79.6690042772555,242.361653627913,16.0702237187361)) ;
#74008=CARTESIAN_POINT('Ctrl Pts',(79.7140939949265,242.34682331489,16.1046945816759)) ;
#74009=CARTESIAN_POINT('Ctrl Pts',(79.7358961080713,242.334329201275,16.1258672215769)) ;
#74010=CARTESIAN_POINT('Ctrl Pts',(79.7738143498085,242.303011480626,16.1708720249648)) ;
#74011=CARTESIAN_POINT('Ctrl Pts',(79.7897951042904,242.283559929487,16.195176521687)) ;
#74012=CARTESIAN_POINT('Ctrl Pts',(79.8020507603673,242.261498926991,16.2199877856679)) ;
#74013=CARTESIAN_POINT('Ctrl Pts',(79.8023768461752,242.260904857995,16.220654066484)) ;
#74014=CARTESIAN_POINT('Ctrl Pts',(79.8026999024823,242.26030915041,16.2213203435596)) ;
#74015=CARTESIAN_POINT('Origin',(68.7783628290597,238.640065792321,16.0213203435596)) ;
#74016=CARTESIAN_POINT('',(68.7158628290597,238.830049344241,16.0254384350468)) ;
#74017=CARTESIAN_POINT('',(68.7158628290597,238.830049344241,16.0213203435596)) ;
#74018=CARTESIAN_POINT('Ctrl Pts',(68.5800869669908,238.61386116447,16.2213203435596)) ;
#74019=CARTESIAN_POINT('Ctrl Pts',(68.5799981768998,238.614532989765,16.2206540664825)) ;
#74020=CARTESIAN_POINT('Ctrl Pts',(68.5799128008651,238.61520527011,16.2199877856702)) ;
#74021=CARTESIAN_POINT('Ctrl Pts',(68.5773214398071,238.636474992276,16.1989219659976)) ;
#74022=CARTESIAN_POINT('Ctrl Pts',(68.5780020903549,238.65758770239,16.178428974336)) ;
#74023=CARTESIAN_POINT('Ctrl Pts',(68.5859696915829,238.698341844598,16.1396302534779)) ;
#74024=CARTESIAN_POINT('Ctrl Pts',(68.5930006837847,238.718230624168,16.1210537744199)) ;
#74025=CARTESIAN_POINT('Ctrl Pts',(68.6146156632017,238.757155074589,16.0855257632539)) ;
#74026=CARTESIAN_POINT('Ctrl Pts',(68.629756138567,238.77633747488,16.0684876094502)) ;
#74027=CARTESIAN_POINT('Ctrl Pts',(68.6638972155015,238.805181822537,16.0440628922199)) ;
#74028=CARTESIAN_POINT('Ctrl Pts',(68.6809210571054,238.815972587934,16.0353723462051)) ;
#74029=CARTESIAN_POINT('Ctrl Pts',(68.7053023338861,238.82632650681,16.0279192770437)) ;
#74030=CARTESIAN_POINT('Ctrl Pts',(68.7105319332097,238.828295608261,16.0265673132423)) ;
#74031=CARTESIAN_POINT('Ctrl Pts',(68.7158628290598,238.830049344241,16.0254384350468)) ;
#74032=CARTESIAN_POINT('Origin',(74.5283628290597,239.4,7.2786795888419)) ;
#74033=CARTESIAN_POINT('Origin',(74.5283628290597,239.4,7.17267980084127)) ;
#74034=CARTESIAN_POINT('Origin',(78.7335324267296,243.3945648893,16.0213203435596)) ;
#74035=CARTESIAN_POINT('',(78.8957655188746,243.277601545414,16.0254384350469)) ;
#74036=CARTESIAN_POINT('',(78.8957655188746,243.277601545414,16.0213203435596)) ;
#74037=CARTESIAN_POINT('Ctrl Pts',(78.8785382749254,243.532308506173,16.2213203435596)) ;
#74038=CARTESIAN_POINT('Ctrl Pts',(78.8790049966057,243.531817177611,16.2206540665006)) ;
#74039=CARTESIAN_POINT('Ctrl Pts',(78.879469223731,243.531323474171,16.2199877856431)) ;
#74040=CARTESIAN_POINT('Ctrl Pts',(78.8940677080386,243.515639071118,16.1989219662062)) ;
#74041=CARTESIAN_POINT('Ctrl Pts',(78.9059267896971,243.498158453602,16.1784289743019)) ;
#74042=CARTESIAN_POINT('Ctrl Pts',(78.9234355486647,243.460504421427,16.1396302534118)) ;
#74043=CARTESIAN_POINT('Ctrl Pts',(78.9294376878011,243.440281347212,16.1210537743409)) ;
#74044=CARTESIAN_POINT('Ctrl Pts',(78.9348300200081,243.396085839179,16.0855257631784)) ;
#74045=CARTESIAN_POINT('Ctrl Pts',(78.9338562501174,243.371667603226,16.0684876093885)) ;
#74046=CARTESIAN_POINT('Ctrl Pts',(78.9231898208194,243.328264414275,16.0440628921802)) ;
#74047=CARTESIAN_POINT('Ctrl Pts',(78.9157598964075,243.309528138661,16.0353723461746)) ;
#74048=CARTESIAN_POINT('Ctrl Pts',(78.9021209099727,243.286820687439,16.0279192770313)) ;
#74049=CARTESIAN_POINT('Ctrl Pts',(78.8990474840521,243.282153769567,16.0265673132372)) ;
#74050=CARTESIAN_POINT('Ctrl Pts',(78.8957655188748,243.277601545414,16.0254384350468)) ;
#74051=CARTESIAN_POINT('Origin',(74.5283628290597,239.4,16.2213203435596)) ;
#74052=CARTESIAN_POINT('',(79.5256245226196,242.344040686892,16.0213203435596)) ;
#74053=CARTESIAN_POINT('Ctrl Pts',(79.5657826988536,242.355402012486,16.0254384350468)) ;
#74054=CARTESIAN_POINT('Ctrl Pts',(79.5552733408866,242.352029841245,16.0232182514845)) ;
#74055=CARTESIAN_POINT('Ctrl Pts',(79.5444841112885,242.348889316593,16.0218983740811)) ;
#74056=CARTESIAN_POINT('Ctrl Pts',(79.5308797297982,242.345350737123,16.0213707571522)) ;
#74057=CARTESIAN_POINT('Ctrl Pts',(79.5282532448735,242.344686552695,16.0213203435596)) ;
#74058=CARTESIAN_POINT('Ctrl Pts',(79.5256245226195,242.344040686893,16.0213203435596)) ;
#74059=CARTESIAN_POINT('',(78.8725506972158,243.242919692911,16.0213203435596)) ;
#74060=CARTESIAN_POINT('Origin',(74.5283628290597,239.4,16.0213203435596)) ;
#74061=CARTESIAN_POINT('Ctrl Pts',(78.8725506972156,243.242919692911,16.0213203435596)) ;
#74062=CARTESIAN_POINT('Ctrl Pts',(78.8784957360457,243.252506602147,16.0213203435596)) ;
#74063=CARTESIAN_POINT('Ctrl Pts',(78.8847145499147,243.261928333949,16.0221950109068)) ;
#74064=CARTESIAN_POINT('Ctrl Pts',(78.8926804716262,243.273292593537,16.0244263118334)) ;
#74065=CARTESIAN_POINT('Ctrl Pts',(78.8942200617331,243.275457931163,16.0249068532759)) ;
#74066=CARTESIAN_POINT('Ctrl Pts',(78.8957655188745,243.277601545414,16.0254384350468)) ;
#74067=CARTESIAN_POINT('Origin',(68.7783628290597,240.159934207678,16.0213203435596)) ;
#74068=CARTESIAN_POINT('',(68.7158628290597,239.969950655759,16.0254384350468)) ;
#74069=CARTESIAN_POINT('',(68.7158628290597,239.969950655759,16.0213203435596)) ;
#74070=CARTESIAN_POINT('Ctrl Pts',(68.7158628290597,239.969950655759,16.0254384350468)) ;
#74071=CARTESIAN_POINT('Ctrl Pts',(68.6968502874981,239.976205322732,16.0294645582753)) ;
#74072=CARTESIAN_POINT('Ctrl Pts',(68.6795955094843,239.985038786367,16.0362204083692)) ;
#74073=CARTESIAN_POINT('Ctrl Pts',(68.6447048052136,240.009241488381,16.056050217191)) ;
#74074=CARTESIAN_POINT('Ctrl Pts',(68.6286802105954,240.025565114139,16.070223718736)) ;
#74075=CARTESIAN_POINT('Ctrl Pts',(68.6009189020099,240.064066160484,16.1046945816759)) ;
#74076=CARTESIAN_POINT('Ctrl Pts',(68.5906244776854,240.086989071303,16.125867221577)) ;
#74077=CARTESIAN_POINT('Ctrl Pts',(68.5783560700561,240.134613422819,16.1708720249648)) ;
#74078=CARTESIAN_POINT('Ctrl Pts',(68.5768607029914,240.159743310064,16.1951765216854)) ;
#74079=CARTESIAN_POINT('Ctrl Pts',(68.5799128008655,240.184794729893,16.219987785668)) ;
#74080=CARTESIAN_POINT('Ctrl Pts',(68.5799981768999,240.185467010236,16.2206540664841)) ;
#74081=CARTESIAN_POINT('Ctrl Pts',(68.5800869669907,240.186138835529,16.2213203435596)) ;
#74082=CARTESIAN_POINT('Origin',(74.5283628290597,239.4,16.2213203435596)) ;
#74083=CARTESIAN_POINT('',(68.7550294957263,239.955537777493,16.0213203435596)) ;
#74084=CARTESIAN_POINT('Ctrl Pts',(68.7158628290597,239.969950655759,16.0254384350468)) ;
#74085=CARTESIAN_POINT('Ctrl Pts',(68.7263471907788,239.966501553977,16.0232182514845)) ;
#74086=CARTESIAN_POINT('Ctrl Pts',(68.7369218149545,239.96270054175,16.0218983740811)) ;
#74087=CARTESIAN_POINT('Ctrl Pts',(68.750007915605,239.957566857871,16.0213707571522)) ;
#74088=CARTESIAN_POINT('Ctrl Pts',(68.7525231843559,239.956560385256,16.0213203435596)) ;
#74089=CARTESIAN_POINT('Ctrl Pts',(68.7550294957264,239.955537777493,16.0213203435596)) ;
#74090=CARTESIAN_POINT('',(68.7550294957263,238.844462222507,16.0213203435596)) ;
#74091=CARTESIAN_POINT('Origin',(74.5283628290597,239.4,16.0213203435596)) ;
#74092=CARTESIAN_POINT('Ctrl Pts',(68.7550294957264,238.844462222507,16.0213203435596)) ;
#74093=CARTESIAN_POINT('Ctrl Pts',(68.7445848144169,238.84020065616,16.0213203435596)) ;
#74094=CARTESIAN_POINT('Ctrl Pts',(68.7340157333076,238.836233642095,16.0221950109068)) ;
#74095=CARTESIAN_POINT('Ctrl Pts',(68.7208914230783,238.831722014263,16.0244263118334)) ;
#74096=CARTESIAN_POINT('Ctrl Pts',(68.7183731149947,238.830875167684,16.0249068532759)) ;
#74097=CARTESIAN_POINT('Ctrl Pts',(68.7158628290597,238.830049344241,16.0254384350468)) ;
#74098=CARTESIAN_POINT('Ctrl Pts',(77.4837648415492,244.437419869805,7.27867958886636)) ;
#74099=CARTESIAN_POINT('Ctrl Pts',(77.4585116532207,244.35871841103,7.10540671867986)) ;
#74100=CARTESIAN_POINT('Ctrl Pts',(77.443848797508,244.244500039629,6.87572294129316)) ;
#74101=CARTESIAN_POINT('Ctrl Pts',(77.4767397974834,244.082582260847,6.61251968150632)) ;
#74102=CARTESIAN_POINT('Ctrl Pts',(77.5104704548032,243.996545441785,6.49309979197962)) ;
#74103=CARTESIAN_POINT('Ctrl Pts',(77.5520026928461,243.924673376047,6.41122244792242)) ;
#74104=CARTESIAN_POINT('Ctrl Pts',(77.5920007761937,243.870649989262,6.36192450350774)) ;
#74105=CARTESIAN_POINT('Ctrl Pts',(77.6750077189191,243.780082536022,6.30168473213267)) ;
#74106=CARTESIAN_POINT('Ctrl Pts',(77.8132286883953,243.69499776711,6.3324653452167)) ;
#74107=CARTESIAN_POINT('Ctrl Pts',(77.9593452832999,243.658401997693,6.46981695114858)) ;
#74108=CARTESIAN_POINT('Ctrl Pts',(78.1070770030435,243.649239949518,6.66032504736798)) ;
#74109=CARTESIAN_POINT('Ctrl Pts',(78.261227537895,243.682063603977,6.93428000315929)) ;
#74110=CARTESIAN_POINT('Ctrl Pts',(78.3612751686961,243.735183622334,7.16318512433995)) ;
#74111=CARTESIAN_POINT('Ctrl Pts',(78.4059643744738,243.767402689815,7.27867958884208)) ;
#74112=CARTESIAN_POINT('Ctrl Pts',(77.4976417597645,244.480667229015,7.24979207610077)) ;
#74113=CARTESIAN_POINT('Ctrl Pts',(77.4650052602715,244.399947648007,7.07844135600526)) ;
#74114=CARTESIAN_POINT('Ctrl Pts',(77.441926342153,244.27989101645,6.85076506164513)) ;
#74115=CARTESIAN_POINT('Ctrl Pts',(77.469035052647,244.106597484524,6.58946771467476)) ;
#74116=CARTESIAN_POINT('Ctrl Pts',(77.5017200730652,244.013890562126,6.47083507754566)) ;
#74117=CARTESIAN_POINT('Ctrl Pts',(77.5439463357434,243.936278331151,6.38946919876817)) ;
#74118=CARTESIAN_POINT('Ctrl Pts',(77.5854536468431,243.877964896304,6.34047061769564)) ;
#74119=CARTESIAN_POINT('Ctrl Pts',(77.6727335680326,243.780325930787,6.28058379867695)) ;
#74120=CARTESIAN_POINT('Ctrl Pts',(77.8207665331947,243.690170175011,6.31119018804536)) ;
#74121=CARTESIAN_POINT('Ctrl Pts',(77.9773466517903,243.654865956607,6.44770651855499)) ;
#74122=CARTESIAN_POINT('Ctrl Pts',(78.1347187687794,243.650542022732,6.63695571575657)) ;
#74123=CARTESIAN_POINT('Ctrl Pts',(78.296448346719,243.693705791539,6.90885244575103)) ;
#74124=CARTESIAN_POINT('Ctrl Pts',(78.3983590846983,243.756649388286,7.13557881442657)) ;
#74125=CARTESIAN_POINT('Ctrl Pts',(78.4428068537051,243.793964592266,7.24979207607676)) ;
#74126=CARTESIAN_POINT('Ctrl Pts',(77.4834771745742,244.568077333119,7.19960840329863)) ;
#74127=CARTESIAN_POINT('Ctrl Pts',(77.4436102819794,244.4764369139,7.03137458611506)) ;
#74128=CARTESIAN_POINT('Ctrl Pts',(77.4139039095814,244.340370527827,6.80703943420276)) ;
#74129=CARTESIAN_POINT('Ctrl Pts',(77.441124871434,244.144263265602,6.54896335582758)) ;
#74130=CARTESIAN_POINT('Ctrl Pts',(77.4763992563712,244.039603833945,6.4316758963033)) ;
#74131=CARTESIAN_POINT('Ctrl Pts',(77.5228341950722,243.952143562869,6.35118835405155)) ;
#74132=CARTESIAN_POINT('Ctrl Pts',(77.5687683992923,243.886557953544,6.30270568059201)) ;
#74133=CARTESIAN_POINT('Ctrl Pts',(77.6657813516918,243.776949117914,6.2434294197825)) ;
#74134=CARTESIAN_POINT('Ctrl Pts',(77.8313282196128,243.676542753242,6.27373302479717)) ;
#74135=CARTESIAN_POINT('Ctrl Pts',(78.007058574649,243.638627531938,6.40881035055017)) ;
#74136=CARTESIAN_POINT('Ctrl Pts',(78.1839044841603,243.636222713605,6.59590900476823)) ;
#74137=CARTESIAN_POINT('Ctrl Pts',(78.3660146003686,243.688507812405,6.86433859796256)) ;
#74138=CARTESIAN_POINT('Ctrl Pts',(78.480434429088,243.763356346367,7.0874727030592)) ;
#74139=CARTESIAN_POINT('Ctrl Pts',(78.530315900344,243.807504478867,7.19960840327508)) ;
#74140=CARTESIAN_POINT('Ctrl Pts',(77.4105061694992,244.630334397705,7.17608503413729)) ;
#74141=CARTESIAN_POINT('Ctrl Pts',(77.3747457443117,244.527986810322,7.0051593557285)) ;
#74142=CARTESIAN_POINT('Ctrl Pts',(77.352444704757,244.378597391926,6.77808201258452)) ;
#74143=CARTESIAN_POINT('Ctrl Pts',(77.3933178687395,244.165514331098,6.51747829524014)) ;
#74144=CARTESIAN_POINT('Ctrl Pts',(77.4368992140211,244.052028001316,6.39916189443959)) ;
#74145=CARTESIAN_POINT('Ctrl Pts',(77.4912218362456,243.957086040865,6.3180128069882)) ;
#74146=CARTESIAN_POINT('Ctrl Pts',(77.5437817769028,243.885680434673,6.26914484885761)) ;
#74147=CARTESIAN_POINT('Ctrl Pts',(77.6531949017869,243.765909487477,6.2094175851449)) ;
#74148=CARTESIAN_POINT('Ctrl Pts',(77.8359695421258,243.653538086233,6.23994250467339)) ;
#74149=CARTESIAN_POINT('Ctrl Pts',(78.0288043665172,243.606004164191,6.37609501939021)) ;
#74150=CARTESIAN_POINT('Ctrl Pts',(78.2232181197253,243.595299774762,6.56484006186565)) ;
#74151=CARTESIAN_POINT('Ctrl Pts',(78.424955462476,243.641083248432,6.8360152165287)) ;
#74152=CARTESIAN_POINT('Ctrl Pts',(78.5545603434248,243.713593072997,7.06215508260829)) ;
#74153=CARTESIAN_POINT('Ctrl Pts',(78.6120751679673,243.757343419967,7.17608503411335)) ;
#74154=CARTESIAN_POINT('Ctrl Pts',(77.3741795847432,244.647613467424,7.17267980086573)) ;
#74155=CARTESIAN_POINT('Ctrl Pts',(77.3410337106214,244.542393454288,6.99940693067922)) ;
#74156=CARTESIAN_POINT('Ctrl Pts',(77.3229424637377,244.389325610061,6.76972315329249)) ;
#74157=CARTESIAN_POINT('Ctrl Pts',(77.3707526168182,244.1711328328,6.5065198935057)) ;
#74158=CARTESIAN_POINT('Ctrl Pts',(77.4183887146006,244.054798424185,6.38710000397899)) ;
#74159=CARTESIAN_POINT('Ctrl Pts',(77.4764294768079,243.957275809245,6.30522265992179)) ;
#74160=CARTESIAN_POINT('Ctrl Pts',(77.5320328188919,243.883747414752,6.25592471550711)) ;
#74161=CARTESIAN_POINT('Ctrl Pts',(77.6470057191962,243.760070691083,6.19568494413203)) ;
#74162=CARTESIAN_POINT('Ctrl Pts',(77.836976450415,243.642390344,6.22646555721608)) ;
#74163=CARTESIAN_POINT('Ctrl Pts',(78.0363354903944,243.589871777701,6.36381716314794)) ;
#74164=CARTESIAN_POINT('Ctrl Pts',(78.237103824237,243.574397947023,6.55432525936736)) ;
#74165=CARTESIAN_POINT('Ctrl Pts',(78.4454209904142,243.615605744879,6.82828021515864)) ;
#74166=CARTESIAN_POINT('Ctrl Pts',(78.5798598185785,243.685449743899,7.05718533633932)) ;
#74167=CARTESIAN_POINT('Ctrl Pts',(78.6397340718556,243.728134311011,7.17267980084145)) ;
#74168=CARTESIAN_POINT('Ctrl Pts',(78.6397340718555,243.728134311011,7.17267980084155)) ;
#74169=CARTESIAN_POINT('Ctrl Pts',(78.6056702453262,243.703850088494,7.10697236920578)) ;
#74170=CARTESIAN_POINT('Ctrl Pts',(78.5691964024876,243.682062483905,7.04152434533095)) ;
#74171=CARTESIAN_POINT('Ctrl Pts',(78.5302356565323,243.66307540284,6.97671039020929)) ;
#74172=CARTESIAN_POINT('Ctrl Pts',(78.5082997438497,243.652385182667,6.9402184487615)) ;
#74173=CARTESIAN_POINT('Ctrl Pts',(78.4855756286922,243.642581657307,6.90392782990232)) ;
#74174=CARTESIAN_POINT('Ctrl Pts',(78.4620506024934,243.633709385751,6.86790773212447)) ;
#74175=CARTESIAN_POINT('Ctrl Pts',(78.4539288501039,243.63064633315,6.85547219591187)) ;
#74176=CARTESIAN_POINT('Ctrl Pts',(78.4457097777806,243.627693929755,6.84306655751141)) ;
#74177=CARTESIAN_POINT('Ctrl Pts',(78.4373919411165,243.624853531614,6.83069239945942)) ;
#74178=CARTESIAN_POINT('Ctrl Pts',(78.4054267240316,243.613937959829,6.78313885106156)) ;
#74179=CARTESIAN_POINT('Ctrl Pts',(78.3720062790205,243.60467579283,6.73604738536763)) ;
#74180=CARTESIAN_POINT('Ctrl Pts',(78.3368785400582,243.597615059998,6.68991428798604)) ;
#74181=CARTESIAN_POINT('Ctrl Pts',(78.3287444025781,243.595980085096,6.67923176279163)) ;
#74182=CARTESIAN_POINT('Ctrl Pts',(78.3205186574952,243.594462941081,6.66860062481077)) ;
#74183=CARTESIAN_POINT('Ctrl Pts',(78.3121980306879,243.593070046952,6.65802703595722)) ;
#74184=CARTESIAN_POINT('Ctrl Pts',(78.2791741928448,243.587541772351,6.61606138940173)) ;
#74185=CARTESIAN_POINT('Ctrl Pts',(78.2446566502133,243.583974335635,6.57500138393977)) ;
#74186=CARTESIAN_POINT('Ctrl Pts',(78.2084138054501,243.582780658522,6.53526328812201)) ;
#74187=CARTESIAN_POINT('Ctrl Pts',(78.2003901019826,243.582516393637,6.52646578066122)) ;
#74188=CARTESIAN_POINT('Ctrl Pts',(78.1922817207221,243.582368309447,6.5177330630473)) ;
#74189=CARTESIAN_POINT('Ctrl Pts',(78.1840859268662,243.582340602795,6.50906965208559)) ;
#74190=CARTESIAN_POINT('Ctrl Pts',(78.1818287265343,243.582332972117,6.5066836655122)) ;
#74191=CARTESIAN_POINT('Ctrl Pts',(78.1795648940714,243.582334485191,6.50430295098332)) ;
#74192=CARTESIAN_POINT('Ctrl Pts',(78.1772943649429,243.58234531375,6.50192769965503)) ;
#74193=CARTESIAN_POINT('Ctrl Pts',(78.1448749880298,243.58249992754,6.46801306402757)) ;
#74194=CARTESIAN_POINT('Ctrl Pts',(78.111163228768,243.584564437887,6.43529547007951)) ;
#74195=CARTESIAN_POINT('Ctrl Pts',(78.0759893913998,243.589010017353,6.4043525891647)) ;
#74196=CARTESIAN_POINT('Ctrl Pts',(78.0703029105687,243.589728724901,6.39935011822759)) ;
#74197=CARTESIAN_POINT('Ctrl Pts',(78.0645781241267,243.590509603748,6.3943940321019)) ;
#74198=CARTESIAN_POINT('Ctrl Pts',(78.0588142008808,243.591354572783,6.38948677170072)) ;
#74199=CARTESIAN_POINT('Ctrl Pts',(78.0502812827671,243.592605465844,6.38222205817499)) ;
#74200=CARTESIAN_POINT('Ctrl Pts',(78.0416628571285,243.593996700239,6.37506446485148)) ;
#74201=CARTESIAN_POINT('Ctrl Pts',(78.0329565182296,243.595534207291,6.36802209790309)) ;
#74202=CARTESIAN_POINT('Ctrl Pts',(78.0171453080364,243.598326408175,6.35523275609461)) ;
#74203=CARTESIAN_POINT('Ctrl Pts',(78.0010442203777,243.601601199969,6.34282344947888)) ;
#74204=CARTESIAN_POINT('Ctrl Pts',(77.9846812113037,243.605467462449,6.33097928884109)) ;
#74205=CARTESIAN_POINT('Ctrl Pts',(77.9607186006994,243.611129363747,6.31363425113956)) ;
#74206=CARTESIAN_POINT('Ctrl Pts',(77.936093389843,243.618050306344,6.29738619367076)) ;
#74207=CARTESIAN_POINT('Ctrl Pts',(77.9109431483584,243.626582550789,6.28290075179634)) ;
#74208=CARTESIAN_POINT('Ctrl Pts',(77.8951199349199,243.631950591689,6.27378727116955)) ;
#74209=CARTESIAN_POINT('Ctrl Pts',(77.8790891308354,243.637955860123,6.26537143050151)) ;
#74210=CARTESIAN_POINT('Ctrl Pts',(77.8628866246398,243.64467672787,6.25781288605435)) ;
#74211=CARTESIAN_POINT('Ctrl Pts',(77.844327856176,243.65237498312,6.24915513430744)) ;
#74212=CARTESIAN_POINT('Ctrl Pts',(77.8255436879687,243.661011610903,6.24162317342905)) ;
#74213=CARTESIAN_POINT('Ctrl Pts',(77.8067818557341,243.670463113482,6.23533853986355)) ;
#74214=CARTESIAN_POINT('Ctrl Pts',(77.7859713432594,243.680946663801,6.22836766177561)) ;
#74215=CARTESIAN_POINT('Ctrl Pts',(77.7651450311656,243.692483594737,6.22295373950091)) ;
#74216=CARTESIAN_POINT('Ctrl Pts',(77.7445535056794,243.704951875444,6.21921673644277)) ;
#74217=CARTESIAN_POINT('Ctrl Pts',(77.7410522809034,243.707071886094,6.21858132515651)) ;
#74218=CARTESIAN_POINT('Ctrl Pts',(77.7375578325966,243.709218926783,6.21799446327862)) ;
#74219=CARTESIAN_POINT('Ctrl Pts',(77.7340713860324,243.711392523157,6.21745682880153)) ;
#74220=CARTESIAN_POINT('Ctrl Pts',(77.7157398472004,243.722821169944,6.21462997713103)) ;
#74221=CARTESIAN_POINT('Ctrl Pts',(77.697625497054,243.73498543254,6.21316358595338)) ;
#74222=CARTESIAN_POINT('Ctrl Pts',(77.6799544975016,243.747812001882,6.21318615231491)) ;
#74223=CARTESIAN_POINT('Ctrl Pts',(77.6645936405816,243.758961744479,6.21320576855958)) ;
#74224=CARTESIAN_POINT('Ctrl Pts',(77.6495871697784,243.77064446397,6.2144111776784)) ;
#74225=CARTESIAN_POINT('Ctrl Pts',(77.6351992769763,243.782777207783,6.21693504199464)) ;
#74226=CARTESIAN_POINT('Ctrl Pts',(77.6342240251621,243.783599599261,6.21710611661182)) ;
#74227=CARTESIAN_POINT('Ctrl Pts',(77.63325162561,243.784424046822,6.21728323621031)) ;
#74228=CARTESIAN_POINT('Ctrl Pts',(77.6322821647892,243.785250519711,6.21746643644027)) ;
#74229=CARTESIAN_POINT('Ctrl Pts',(77.6224102773551,243.793666380515,6.21933193941812)) ;
#74230=CARTESIAN_POINT('Ctrl Pts',(77.6127851169546,243.802229499662,6.22169255583841)) ;
#74231=CARTESIAN_POINT('Ctrl Pts',(77.603457967227,243.810938254419,6.2245883950779)) ;
#74232=CARTESIAN_POINT('Ctrl Pts',(77.5911012765818,243.822475689924,6.22842482857422)) ;
#74233=CARTESIAN_POINT('Ctrl Pts',(77.5792663940833,243.834268961409,6.23320005369937)) ;
#74234=CARTESIAN_POINT('Ctrl Pts',(77.5679799955803,243.84615748058,6.23871133413667)) ;
#74235=CARTESIAN_POINT('Ctrl Pts',(77.5562410210379,243.858522720374,6.24444361274899)) ;
#74236=CARTESIAN_POINT('Ctrl Pts',(77.5450496960544,243.871095838374,6.25106944064198)) ;
#74237=CARTESIAN_POINT('Ctrl Pts',(77.5344310051272,243.883661988622,6.25830807140166)) ;
#74238=CARTESIAN_POINT('Ctrl Pts',(77.5192233858284,243.901658672991,6.26867491808675)) ;
#74239=CARTESIAN_POINT('Ctrl Pts',(77.5051928933561,243.919639878176,6.28029754581556)) ;
#74240=CARTESIAN_POINT('Ctrl Pts',(77.4922892068279,243.937585638839,6.29304624367543)) ;
#74241=CARTESIAN_POINT('Ctrl Pts',(77.4875869170504,243.94412533327,6.29769205334324)) ;
#74242=CARTESIAN_POINT('Ctrl Pts',(77.4830337863889,243.950660461088,6.30248724032742)) ;
#74243=CARTESIAN_POINT('Ctrl Pts',(77.4786258065215,243.957190498153,6.3074250167697)) ;
#74244=CARTESIAN_POINT('Ctrl Pts',(77.4674012196598,243.97381874294,6.31999869048131)) ;
#74245=CARTESIAN_POINT('Ctrl Pts',(77.4571197533067,243.990413240837,6.33349717741477)) ;
#74246=CARTESIAN_POINT('Ctrl Pts',(77.4476436294181,244.006846495269,6.34759111962041)) ;
#74247=CARTESIAN_POINT('Ctrl Pts',(77.4431766030217,244.014593099492,6.3542349766027)) ;
#74248=CARTESIAN_POINT('Ctrl Pts',(77.4388910741257,244.022314764158,6.36102814506278)) ;
#74249=CARTESIAN_POINT('Ctrl Pts',(77.4347756439215,244.030000057463,6.36794186933745)) ;
#74250=CARTESIAN_POINT('Ctrl Pts',(77.417359309355,244.062523908629,6.39720047149911)) ;
#74251=CARTESIAN_POINT('Ctrl Pts',(77.4029953763618,244.094397502566,6.42861718017856)) ;
#74252=CARTESIAN_POINT('Ctrl Pts',(77.3911107953339,244.125609926009,6.46147818340991)) ;
#74253=CARTESIAN_POINT('Ctrl Pts',(77.385473879065,244.140414134679,6.47706432172584)) ;
#74254=CARTESIAN_POINT('Ctrl Pts',(77.3803936266802,244.155069379978,6.49297553193036)) ;
#74255=CARTESIAN_POINT('Ctrl Pts',(77.3758037534668,244.169573406561,6.50913676629883)) ;
#74256=CARTESIAN_POINT('Ctrl Pts',(77.3690217789683,244.191004486209,6.53301652816881)) ;
#74257=CARTESIAN_POINT('Ctrl Pts',(77.3633108223515,244.212105384286,6.5574420009269)) ;
#74258=CARTESIAN_POINT('Ctrl Pts',(77.3585253774069,244.232884182501,6.58226166147533)) ;
#74259=CARTESIAN_POINT('Ctrl Pts',(77.3532451919441,244.255811185014,6.60964728858771)) ;
#74260=CARTESIAN_POINT('Ctrl Pts',(77.3491196999421,244.278360870846,6.63755586791247)) ;
#74261=CARTESIAN_POINT('Ctrl Pts',(77.3459664292511,244.300539026061,6.66580387508425)) ;
#74262=CARTESIAN_POINT('Ctrl Pts',(77.3404692948678,244.339202468415,6.71504896270834)) ;
#74263=CARTESIAN_POINT('Ctrl Pts',(77.33792943213,244.376736116788,6.76532381957312)) ;
#74264=CARTESIAN_POINT('Ctrl Pts',(77.3379719233937,244.4132321697,6.81629637010306)) ;
#74265=CARTESIAN_POINT('Ctrl Pts',(77.3379762242859,244.416926237014,6.82145572345211)) ;
#74266=CARTESIAN_POINT('Ctrl Pts',(77.3380069489883,244.420609645206,6.82662222476909)) ;
#74267=CARTESIAN_POINT('Ctrl Pts',(77.3380636865819,244.424282471624,6.83179552969322)) ;
#74268=CARTESIAN_POINT('Ctrl Pts',(77.3386487996133,244.46215892118,6.88514583833158)) ;
#74269=CARTESIAN_POINT('Ctrl Pts',(77.3420026814919,244.49891283477,6.93921967747165)) ;
#74270=CARTESIAN_POINT('Ctrl Pts',(77.3476451774573,244.53464191174,6.99367465481829)) ;
#74271=CARTESIAN_POINT('Ctrl Pts',(77.34795542128,244.536606419201,6.99666877664711)) ;
#74272=CARTESIAN_POINT('Ctrl Pts',(77.3482725720785,244.538567823308,6.99966405072471)) ;
#74273=CARTESIAN_POINT('Ctrl Pts',(77.3485965458904,244.540526138695,7.00266042013703)) ;
#74274=CARTESIAN_POINT('Ctrl Pts',(77.3535101894839,244.570227501896,7.0481057333876)) ;
#74275=CARTESIAN_POINT('Ctrl Pts',(77.3600592544265,244.59920150165,7.09382843494077)) ;
#74276=CARTESIAN_POINT('Ctrl Pts',(77.368127215059,244.62745431126,7.13971218679672)) ;
#74277=CARTESIAN_POINT('Ctrl Pts',(77.3700579907416,244.63421560327,7.1506928095768)) ;
#74278=CARTESIAN_POINT('Ctrl Pts',(77.3720758964805,244.640935408314,7.16168259192434)) ;
#74279=CARTESIAN_POINT('Ctrl Pts',(77.3741795847387,244.647613467409,7.17267980084153)) ;
#74280=CARTESIAN_POINT('Ctrl Pts',(77.4837648415492,244.437419869805,7.27867958886636)) ;
#74281=CARTESIAN_POINT('Ctrl Pts',(77.4585116532207,244.35871841103,7.10540671867986)) ;
#74282=CARTESIAN_POINT('Ctrl Pts',(77.443848797508,244.244500039629,6.87572294129316)) ;
#74283=CARTESIAN_POINT('Ctrl Pts',(77.4767397974834,244.082582260847,6.61251968150632)) ;
#74284=CARTESIAN_POINT('Ctrl Pts',(77.5104704548032,243.996545441785,6.49309979197962)) ;
#74285=CARTESIAN_POINT('Ctrl Pts',(77.5520026928461,243.924673376047,6.41122244792242)) ;
#74286=CARTESIAN_POINT('Ctrl Pts',(77.5920007761937,243.870649989262,6.36192450350774)) ;
#74287=CARTESIAN_POINT('Ctrl Pts',(77.6750077189191,243.780082536022,6.30168473213267)) ;
#74288=CARTESIAN_POINT('Ctrl Pts',(77.8132286883953,243.69499776711,6.3324653452167)) ;
#74289=CARTESIAN_POINT('Ctrl Pts',(77.9593452832999,243.658401997693,6.46981695114858)) ;
#74290=CARTESIAN_POINT('Ctrl Pts',(78.1070770030435,243.649239949518,6.66032504736798)) ;
#74291=CARTESIAN_POINT('Ctrl Pts',(78.261227537895,243.682063603977,6.93428000315929)) ;
#74292=CARTESIAN_POINT('Ctrl Pts',(78.3612751686961,243.735183622334,7.16318512433995)) ;
#74293=CARTESIAN_POINT('Ctrl Pts',(78.4059643744738,243.767402689815,7.27867958884208)) ;
#74294=CARTESIAN_POINT('Origin',(78.5229277183602,243.60516959767,16.0213203435596)) ;
#74295=CARTESIAN_POINT('',(78.4059643744738,243.767402689815,16.0254384350469)) ;
#74296=CARTESIAN_POINT('',(78.4059643744738,243.767402689815,16.0213203435596)) ;
#74297=CARTESIAN_POINT('Ctrl Pts',(78.4059643744738,243.767402689815,16.0254384350469)) ;
#74298=CARTESIAN_POINT('Ctrl Pts',(78.4221997978876,243.77910775804,16.0294645582753)) ;
#74299=CARTESIAN_POINT('Ctrl Pts',(78.4394883241358,243.787874987036,16.0362204083692)) ;
#74300=CARTESIAN_POINT('Ctrl Pts',(78.479576962787,243.801876168427,16.0560502171909)) ;
#74301=CARTESIAN_POINT('Ctrl Pts',(78.5022020738258,243.805245551316,16.0702237187359)) ;
#74302=CARTESIAN_POINT('Ctrl Pts',(78.5496677623908,243.805074574509,16.1046945816758)) ;
#74303=CARTESIAN_POINT('Ctrl Pts',(78.5742636976025,243.799929189816,16.1258672215766)) ;
#74304=CARTESIAN_POINT('Ctrl Pts',(78.6200037963982,243.781861648611,16.1708720249637)) ;
#74305=CARTESIAN_POINT('Ctrl Pts',(78.6412132569573,243.768300448861,16.1951765216776)) ;
#74306=CARTESIAN_POINT('Ctrl Pts',(78.65968630321,243.751106394692,16.2199877856684)) ;
#74307=CARTESIAN_POINT('Ctrl Pts',(78.6601800066578,243.750642167558,16.2206540664824)) ;
#74308=CARTESIAN_POINT('Ctrl Pts',(78.6606713352326,243.750175445865,16.2213203435596)) ;
#74309=CARTESIAN_POINT('Origin',(68.824955275583,240.454107337488,16.0213203435596)) ;
#74310=CARTESIAN_POINT('',(68.8242223895094,240.654105994678,16.0254384350469)) ;
#74311=CARTESIAN_POINT('',(68.8242223895094,240.654105994678,16.0213203435596)) ;
#74312=CARTESIAN_POINT('Ctrl Pts',(68.6282860496011,240.490455866367,16.2213203435596)) ;
#74313=CARTESIAN_POINT('Ctrl Pts',(68.6284092106404,240.491122247841,16.2206540664796)) ;
#74314=CARTESIAN_POINT('Ctrl Pts',(68.6285357592578,240.49178800709,16.2199877856732)) ;
#74315=CARTESIAN_POINT('Ctrl Pts',(68.6326439340485,240.512817489538,16.1989219659736)) ;
#74316=CARTESIAN_POINT('Ctrl Pts',(68.6398154574129,240.532686537501,16.1784289743378)) ;
#74317=CARTESIAN_POINT('Ctrl Pts',(68.6599868190111,240.568983905827,16.1396302534826)) ;
#74318=CARTESIAN_POINT('Ctrl Pts',(68.6728196608437,240.58572656316,16.1210537744257)) ;
#74319=CARTESIAN_POINT('Ctrl Pts',(68.7054050445426,240.616066519404,16.0855257632595)) ;
#74320=CARTESIAN_POINT('Ctrl Pts',(68.7257321799814,240.629631402009,16.0684876094548)) ;
#74321=CARTESIAN_POINT('Ctrl Pts',(68.7671156672911,240.646513833829,16.0440628922229)) ;
#74322=CARTESIAN_POINT('Ctrl Pts',(68.786640832671,240.651515805211,16.0353723462074)) ;
#74323=CARTESIAN_POINT('Ctrl Pts',(68.8130283417221,240.653828738359,16.0279192770447)) ;
#74324=CARTESIAN_POINT('Ctrl Pts',(68.8186104720501,240.65408543006,16.0265673132428)) ;
#74325=CARTESIAN_POINT('Ctrl Pts',(68.8242223895094,240.654105994679,16.0254384350468)) ;
#74326=CARTESIAN_POINT('Origin',(74.5283628290597,239.4,7.2786795888419)) ;
#74327=CARTESIAN_POINT('Origin',(74.5283628290597,239.4,7.17267980084127)) ;
#74328=CARTESIAN_POINT('Origin',(77.2933283411226,244.498525837642,16.0213203435596)) ;
#74329=CARTESIAN_POINT('',(77.4837648415456,244.437419869794,16.0254384350468)) ;
#74330=CARTESIAN_POINT('',(77.4837648415456,244.437419869794,16.0213203435596)) ;
#74331=CARTESIAN_POINT('Ctrl Pts',(77.3886719794696,244.674337073423,16.2213203435596)) ;
#74332=CARTESIAN_POINT('Ctrl Pts',(77.3892676870572,244.674014017114,16.2206540664816)) ;
#74333=CARTESIAN_POINT('Ctrl Pts',(77.389861756054,244.673687931306,16.2199877856697)) ;
#74334=CARTESIAN_POINT('Ctrl Pts',(77.4085924865708,244.663282357428,16.1989219659995)) ;
#74335=CARTESIAN_POINT('Ctrl Pts',(77.4252729514943,244.650321959927,16.1784289743326)) ;
#74336=CARTESIAN_POINT('Ctrl Pts',(77.4535605066343,244.619921351367,16.1396302534727)) ;
#74337=CARTESIAN_POINT('Ctrl Pts',(77.4655181537788,244.60254282787,16.121053774414)) ;
#74338=CARTESIAN_POINT('Ctrl Pts',(77.4843037295348,244.562176724276,16.0855257632485)) ;
#74339=CARTESIAN_POINT('Ctrl Pts',(77.4909232692299,244.538652690408,16.0684876094458)) ;
#74340=CARTESIAN_POINT('Ctrl Pts',(77.4941912151551,244.494077696798,16.0440628922171)) ;
#74341=CARTESIAN_POINT('Ctrl Pts',(77.4929147647111,244.47396246687,16.0353723462029)) ;
#74342=CARTESIAN_POINT('Ctrl Pts',(77.4869603061161,244.448151718793,16.0279192770428)) ;
#74343=CARTESIAN_POINT('Ctrl Pts',(77.4854794612957,244.442763475276,16.026567313242)) ;
#74344=CARTESIAN_POINT('Ctrl Pts',(77.4837648415456,244.437419869794,16.0254384350468)) ;
#74345=CARTESIAN_POINT('Origin',(74.5283628290597,239.4,16.2213203435596)) ;
#74346=CARTESIAN_POINT('',(78.3712825219709,243.744187868156,16.0213203435596)) ;
#74347=CARTESIAN_POINT('Ctrl Pts',(78.4059643744737,243.767402689815,16.0254384350468)) ;
#74348=CARTESIAN_POINT('Ctrl Pts',(78.3970114393187,243.76094799417,16.0232182514845)) ;
#74349=CARTESIAN_POINT('Ctrl Pts',(78.3877207476922,243.754627122434,16.0218983740811)) ;
#74350=CARTESIAN_POINT('Ctrl Pts',(78.3758756932179,243.747057748291,16.0213707571522)) ;
#74351=CARTESIAN_POINT('Ctrl Pts',(78.3735830018909,243.745614442886,16.0213203435596)) ;
#74352=CARTESIAN_POINT('Ctrl Pts',(78.3712825219707,243.744187868156,16.0213203435596)) ;
#74353=CARTESIAN_POINT('',(77.4724035159522,244.39726169356,16.0213203435596)) ;
#74354=CARTESIAN_POINT('Origin',(74.5283628290597,239.4,16.0213203435596)) ;
#74355=CARTESIAN_POINT('Ctrl Pts',(77.4724035159521,244.39726169356,16.0213203435596)) ;
#74356=CARTESIAN_POINT('Ctrl Pts',(77.4750950659937,244.40821650409,16.0213203435596)) ;
#74357=CARTESIAN_POINT('Ctrl Pts',(77.4780980342041,244.419098822686,16.0221950109068)) ;
#74358=CARTESIAN_POINT('Ctrl Pts',(77.482162326615,244.432368481004,16.0244263118334)) ;
#74359=CARTESIAN_POINT('Ctrl Pts',(77.4829574376935,244.434903598971,16.0249068532759)) ;
#74360=CARTESIAN_POINT('Ctrl Pts',(77.4837648415455,244.437419869794,16.0254384350468)) ;
#74361=CARTESIAN_POINT('Origin',(69.2946204451421,241.899588097824,16.0213203435596)) ;
#74362=CARTESIAN_POINT('',(69.1764712666787,241.738216564931,16.0254384350469)) ;
#74363=CARTESIAN_POINT('',(69.1764712666787,241.738216564931,16.0213203435596)) ;
#74364=CARTESIAN_POINT('Ctrl Pts',(69.1764712666787,241.738216564931,16.0254384350469)) ;
#74365=CARTESIAN_POINT('Ctrl Pts',(69.160322063524,241.750040305161,16.0294645582753)) ;
#74366=CARTESIAN_POINT('Ctrl Pts',(69.1466414848392,241.763773447953,16.0362204083692)) ;
#74367=CARTESIAN_POINT('Ctrl Pts',(69.1209374994165,241.797573405981,16.056050217191)) ;
#74368=CARTESIAN_POINT('Ctrl Pts',(69.1107414820532,241.818049968693,16.070223718736)) ;
#74369=CARTESIAN_POINT('Ctrl Pts',(69.0962363862438,241.863245355842,16.1046945816758)) ;
#74370=CARTESIAN_POINT('Ctrl Pts',(69.0935293759121,241.888227491612,16.1258672215767)) ;
#74371=CARTESIAN_POINT('Ctrl Pts',(69.0965781608562,241.937312087907,16.1708720249643)) ;
#74372=CARTESIAN_POINT('Ctrl Pts',(69.102921544489,241.961674124758,16.1951765216886)) ;
#74373=CARTESIAN_POINT('Ctrl Pts',(69.1135655765223,241.984556290721,16.2199877856668)) ;
#74374=CARTESIAN_POINT('Ctrl Pts',(69.1138545200074,241.985169284677,16.2206540664843)) ;
#74375=CARTESIAN_POINT('Ctrl Pts',(69.1141465698346,241.985780790853,16.2213203435596)) ;
#74376=CARTESIAN_POINT('Origin',(74.5283628290597,239.4,16.2213203435596)) ;
#74377=CARTESIAN_POINT('',(69.2092671559117,241.712405937524,16.0213203435596)) ;
#74378=CARTESIAN_POINT('Ctrl Pts',(69.1764712666787,241.738216564931,16.0254384350469)) ;
#74379=CARTESIAN_POINT('Ctrl Pts',(69.1853766561449,241.73169642826,16.0232182514845)) ;
#74380=CARTESIAN_POINT('Ctrl Pts',(69.1942591440007,241.724813712233,16.0218983740811)) ;
#74381=CARTESIAN_POINT('Ctrl Pts',(69.2051183697351,241.715887461236,16.0213707571522)) ;
#74382=CARTESIAN_POINT('Ctrl Pts',(69.2071995153286,241.714152988108,16.0213203435596)) ;
#74383=CARTESIAN_POINT('Ctrl Pts',(69.2092671559121,241.712405937524,16.0213203435596)) ;
#74384=CARTESIAN_POINT('',(68.8659259273863,240.655710290858,16.0213203435596)) ;
#74385=CARTESIAN_POINT('Origin',(74.5283628290597,239.4,16.0213203435596)) ;
#74386=CARTESIAN_POINT('Ctrl Pts',(68.8659259273863,240.655710290859,16.0213203435596)) ;
#74387=CARTESIAN_POINT('Ctrl Pts',(68.8546755487425,240.65488488444,16.0213203435596)) ;
#74388=CARTESIAN_POINT('Ctrl Pts',(68.8433978805191,240.654378055541,16.0221950109068)) ;
#74389=CARTESIAN_POINT('Ctrl Pts',(68.8295217500814,240.654142877393,16.0244263118334)) ;
#74390=CARTESIAN_POINT('Ctrl Pts',(68.8268650067839,240.654115678431,16.0249068532759)) ;
#74391=CARTESIAN_POINT('Ctrl Pts',(68.8242223895094,240.654105994679,16.0254384350468)) ;
#74392=CARTESIAN_POINT('Ctrl Pts',(75.7824688237379,245.10414043955,7.27867958884206)) ;
#74393=CARTESIAN_POINT('Ctrl Pts',(75.7826706984503,245.049050470116,7.16318984165068)) ;
#74394=CARTESIAN_POINT('Ctrl Pts',(75.7979890932181,244.936852228027,6.93380141407689)) ;
#74395=CARTESIAN_POINT('Ctrl Pts',(75.8624126704611,244.793118819323,6.66079598828704)) ;
#74396=CARTESIAN_POINT('Ctrl Pts',(75.9441595048601,244.69286791716,6.49260131446618)) ;
#74397=CARTESIAN_POINT('Ctrl Pts',(76.0060804700526,244.637579571816,6.41145429978875)) ;
#74398=CARTESIAN_POINT('Ctrl Pts',(76.087527546102,244.578310960323,6.33519313286103)) ;
#74399=CARTESIAN_POINT('Ctrl Pts',(76.2088559391776,244.524823920756,6.30217044135443)) ;
#74400=CARTESIAN_POINT('Ctrl Pts',(76.3331068362906,244.506355590964,6.35347138365035)) ;
#74401=CARTESIAN_POINT('Ctrl Pts',(76.4115789956862,244.505971060786,6.41180890998702)) ;
#74402=CARTESIAN_POINT('Ctrl Pts',(76.4941307169281,244.514452134586,6.49328329969644)) ;
#74403=CARTESIAN_POINT('Ctrl Pts',(76.6191536305483,244.547394262234,6.66117446013279)) ;
#74404=CARTESIAN_POINT('Ctrl Pts',(76.7557559389564,244.625871137754,6.93432872868204)) ;
#74405=CARTESIAN_POINT('Ctrl Pts',(76.8340341124954,244.7074402845,7.16318668389314)) ;
#74406=CARTESIAN_POINT('Ctrl Pts',(76.8665793939902,244.751891562381,7.27867958884203)) ;
#74407=CARTESIAN_POINT('Ctrl Pts',(75.782302388274,245.149559325897,7.24979207607673)) ;
#74408=CARTESIAN_POINT('Ctrl Pts',(75.7782396631717,245.091669363404,7.13558347940724)) ;
#74409=CARTESIAN_POINT('Ctrl Pts',(75.7865720408754,244.972199666082,6.90837563545836)) ;
#74410=CARTESIAN_POINT('Ctrl Pts',(75.8472015298446,244.816278812457,6.63742275202096)) ;
#74411=CARTESIAN_POINT('Ctrl Pts',(75.9303890431917,244.706654034264,6.47033661234462)) ;
#74412=CARTESIAN_POINT('Ctrl Pts',(75.9947732712511,244.646154912978,6.38969718854569)) ;
#74413=CARTESIAN_POINT('Ctrl Pts',(76.0802875845848,244.581351687701,6.31389669153484)) ;
#74414=CARTESIAN_POINT('Ctrl Pts',(76.2094531643599,244.523456540825,6.2810644103727)) ;
#74415=CARTESIAN_POINT('Ctrl Pts',(76.342117177089,244.505132950672,6.33206585723125)) ;
#74416=CARTESIAN_POINT('Ctrl Pts',(76.4256849987979,244.506310974435,6.39004977366433)) ;
#74417=CARTESIAN_POINT('Ctrl Pts',(76.5132819227883,244.517583033546,6.47101490855074)) ;
#74418=CARTESIAN_POINT('Ctrl Pts',(76.645015605031,244.55723133231,6.6377991047033)) ;
#74419=CARTESIAN_POINT('Ctrl Pts',(76.7856610937703,244.647825162852,6.90889913348456)) ;
#74420=CARTESIAN_POINT('Ctrl Pts',(76.8626697016172,244.739315065788,7.13558035667933)) ;
#74421=CARTESIAN_POINT('Ctrl Pts',(76.8934105946791,244.78853838499,7.24979207607671)) ;
#74422=CARTESIAN_POINT('Ctrl Pts',(75.7418198659931,245.228314182921,7.19960839981097)) ;
#74423=CARTESIAN_POINT('Ctrl Pts',(75.7354231309795,245.162012311947,7.08747727971887)) ;
#74424=CARTESIAN_POINT('Ctrl Pts',(75.741514293225,245.025381866761,6.86386325013094)) ;
#74425=CARTESIAN_POINT('Ctrl Pts',(75.8067006833652,244.847684053476,6.59637029411434)) ;
#74426=CARTESIAN_POINT('Ctrl Pts',(75.8984682441908,244.723213358552,6.43117805982654)) ;
#74427=CARTESIAN_POINT('Ctrl Pts',(75.9699223922858,244.65468834945,6.35141039969581)) ;
#74428=CARTESIAN_POINT('Ctrl Pts',(76.065027577409,244.581442276898,6.27640434964301)) ;
#74429=CARTESIAN_POINT('Ctrl Pts',(76.209126271206,244.51642084558,6.24390250637184)) ;
#74430=CARTESIAN_POINT('Ctrl Pts',(76.3574714895589,244.496546627825,6.29438558207702)) ;
#74431=CARTESIAN_POINT('Ctrl Pts',(76.4509465479782,244.498584229117,6.35176007082548)) ;
#74432=CARTESIAN_POINT('Ctrl Pts',(76.548986871076,244.512212968342,6.43185066721499)) ;
#74433=CARTESIAN_POINT('Ctrl Pts',(76.6963322794042,244.558827523821,6.59674318091439)) ;
#74434=CARTESIAN_POINT('Ctrl Pts',(76.853528602567,244.664346813509,6.86438240227357)) ;
#74435=CARTESIAN_POINT('Ctrl Pts',(76.9386554679947,244.77105655683,7.08747421379399)) ;
#74436=CARTESIAN_POINT('Ctrl Pts',(76.9724525866849,244.82845737314,7.19960839981094)) ;
#74437=CARTESIAN_POINT('Ctrl Pts',(75.6531818187263,245.264974883745,7.17608503411332)) ;
#74438=CARTESIAN_POINT('Ctrl Pts',(75.6515934750498,245.192731555392,7.06215973601728)) ;
#74439=CARTESIAN_POINT('Ctrl Pts',(75.6684443594419,245.045205445093,6.83553966272154)) ;
#74440=CARTESIAN_POINT('Ctrl Pts',(75.750463235268,244.855451291138,6.56530617079925)) ;
#74441=CARTESIAN_POINT('Ctrl Pts',(75.8570753675148,244.722818054325,6.39866518685632)) ;
#74442=CARTESIAN_POINT('Ctrl Pts',(75.9383593864038,244.649618706818,6.31824067693821)) ;
#74443=CARTESIAN_POINT('Ctrl Pts',(76.0455656774809,244.571129860748,6.24264219702634)) ;
#74444=CARTESIAN_POINT('Ctrl Pts',(76.2058533104506,244.500325505336,6.20989743397218)) ;
#74445=CARTESIAN_POINT('Ctrl Pts',(76.3699991515416,244.476147020544,6.26076300576044)) ;
#74446=CARTESIAN_POINT('Ctrl Pts',(76.4735091268837,244.475932678415,6.31859240668635)) ;
#74447=CARTESIAN_POINT('Ctrl Pts',(76.5822415391347,244.487571591132,6.39934178215723)) ;
#74448=CARTESIAN_POINT('Ctrl Pts',(76.7463946772425,244.532060709051,6.56568157766891)) ;
#74449=CARTESIAN_POINT('Ctrl Pts',(76.9242915764346,244.637444476803,6.83606210006298)) ;
#74450=CARTESIAN_POINT('Ctrl Pts',(77.0245312006819,244.746635057221,7.06215662103542)) ;
#74451=CARTESIAN_POINT('Ctrl Pts',(77.0657108925549,244.806016366157,7.17608503411329)) ;
#74452=CARTESIAN_POINT('Ctrl Pts',(75.6132936573898,245.270182723559,7.17267980084142)) ;
#74453=CARTESIAN_POINT('Ctrl Pts',(75.613954293283,245.196657079323,7.05719005365003)) ;
#74454=CARTESIAN_POINT('Ctrl Pts',(75.6357650439128,245.046802655971,6.82780162607624)) ;
#74455=CARTESIAN_POINT('Ctrl Pts',(75.725378892112,244.854402356644,6.55479620028639)) ;
#74456=CARTESIAN_POINT('Ctrl Pts',(75.8386073677345,244.71973854857,6.38660152646554)) ;
#74457=CARTESIAN_POINT('Ctrl Pts',(75.9242311476023,244.645229370074,6.3054545117881)) ;
#74458=CARTESIAN_POINT('Ctrl Pts',(76.0367475875534,244.565135771641,6.22919334486037)) ;
#74459=CARTESIAN_POINT('Ctrl Pts',(76.2040215237222,244.492128423453,6.19617065335378)) ;
#74460=CARTESIAN_POINT('Ctrl Pts',(76.3747470820875,244.465713468591,6.24747159564971)) ;
#74461=CARTESIAN_POINT('Ctrl Pts',(76.4823449745696,244.464080466568,6.30580912198637)) ;
#74462=CARTESIAN_POINT('Ctrl Pts',(76.5953524244594,244.474228894419,6.3872835116958)) ;
#74463=CARTESIAN_POINT('Ctrl Pts',(76.7660596886604,244.51647055355,6.55517467213211)) ;
#74464=CARTESIAN_POINT('Ctrl Pts',(76.9516452996115,244.61953353759,6.8283289406814)) ;
#74465=CARTESIAN_POINT('Ctrl Pts',(77.0572892331031,244.727687124622,7.0571868958925)) ;
#74466=CARTESIAN_POINT('Ctrl Pts',(77.1010421843896,244.786783924096,7.17267980084139)) ;
#74467=CARTESIAN_POINT('Ctrl Pts',(77.1010421843896,244.786783924096,7.17267980084139)) ;
#74468=CARTESIAN_POINT('Ctrl Pts',(77.0791876069748,244.75726510214,7.11499115223938)) ;
#74469=CARTESIAN_POINT('Ctrl Pts',(77.0550394100041,244.728960426818,7.05749126113466)) ;
#74470=CARTESIAN_POINT('Ctrl Pts',(77.0284135534917,244.702086718557,7.0004437744973)) ;
#74471=CARTESIAN_POINT('Ctrl Pts',(77.0103872443349,244.683892608141,6.96182133129954)) ;
#74472=CARTESIAN_POINT('Ctrl Pts',(76.9912256834656,244.66635418934,6.9234062563154)) ;
#74473=CARTESIAN_POINT('Ctrl Pts',(76.9708780595307,244.649535148678,6.88527933317742)) ;
#74474=CARTESIAN_POINT('Ctrl Pts',(76.9611711165242,244.641511535225,6.86709068023696)) ;
#74475=CARTESIAN_POINT('Ctrl Pts',(76.9511945473649,244.633651670802,6.84896784774311)) ;
#74476=CARTESIAN_POINT('Ctrl Pts',(76.9409391607941,244.62595933754,6.8309125757743)) ;
#74477=CARTESIAN_POINT('Ctrl Pts',(76.8773913582901,244.578293569745,6.7190325555223)) ;
#74478=CARTESIAN_POINT('Ctrl Pts',(76.8031623325145,244.537078339014,6.60978933753953)) ;
#74479=CARTESIAN_POINT('Ctrl Pts',(76.7134007239805,244.507249358531,6.50942641939294)) ;
#74480=CARTESIAN_POINT('Ctrl Pts',(76.6685028298768,244.492329189109,6.45922585208486)) ;
#74481=CARTESIAN_POINT('Ctrl Pts',(76.6197251017638,244.480261484262,6.41125670179517)) ;
#74482=CARTESIAN_POINT('Ctrl Pts',(76.565812191839,244.472857592713,6.36812019895627)) ;
#74483=CARTESIAN_POINT('Ctrl Pts',(76.5503252435035,244.470730761012,6.35572886649482)) ;
#74484=CARTESIAN_POINT('Ctrl Pts',(76.5344145188346,244.4689887049,6.34373617049952)) ;
#74485=CARTESIAN_POINT('Ctrl Pts',(76.5180884880173,244.467694881079,6.33226414275337)) ;
#74486=CARTESIAN_POINT('Ctrl Pts',(76.5059905865715,244.466736132854,6.32376315052751)) ;
#74487=CARTESIAN_POINT('Ctrl Pts',(76.493659107157,244.466023104738,6.31554422546924)) ;
#74488=CARTESIAN_POINT('Ctrl Pts',(76.4810997783083,244.465582306053,6.30765948836638)) ;
#74489=CARTESIAN_POINT('Ctrl Pts',(76.4515882934318,244.464546532256,6.28913220059743)) ;
#74490=CARTESIAN_POINT('Ctrl Pts',(76.420820949984,244.465016556187,6.27245603170864)) ;
#74491=CARTESIAN_POINT('Ctrl Pts',(76.3887570669136,244.467406750174,6.25836859846688)) ;
#74492=CARTESIAN_POINT('Ctrl Pts',(76.375058444912,244.468427910458,6.25235003787867)) ;
#74493=CARTESIAN_POINT('Ctrl Pts',(76.3611235725264,244.469799107948,6.24680344963583)) ;
#74494=CARTESIAN_POINT('Ctrl Pts',(76.3470386175973,244.471538328129,6.24181324805731)) ;
#74495=CARTESIAN_POINT('Ctrl Pts',(76.3395945070502,244.472457532157,6.23917585146004)) ;
#74496=CARTESIAN_POINT('Ctrl Pts',(76.3321107808768,244.473479158553,6.23669452539473)) ;
#74497=CARTESIAN_POINT('Ctrl Pts',(76.3245924379661,244.47460686297,6.23437907245424)) ;
#74498=CARTESIAN_POINT('Ctrl Pts',(76.3185272600237,244.475516601731,6.23251115630993)) ;
#74499=CARTESIAN_POINT('Ctrl Pts',(76.3124366187017,244.476495831121,6.23075031208375)) ;
#74500=CARTESIAN_POINT('Ctrl Pts',(76.3063237562274,244.477546881836,6.22910275882576)) ;
#74501=CARTESIAN_POINT('Ctrl Pts',(76.2904956240092,244.480268384201,6.22483672291973)) ;
#74502=CARTESIAN_POINT('Ctrl Pts',(76.27452491071,244.483470288184,6.22133192052908)) ;
#74503=CARTESIAN_POINT('Ctrl Pts',(76.2585136290706,244.487187448996,6.21871267557031)) ;
#74504=CARTESIAN_POINT('Ctrl Pts',(76.2518649603391,244.488730996316,6.21762503671356)) ;
#74505=CARTESIAN_POINT('Ctrl Pts',(76.2452083557863,244.49036366916,6.21669005024627)) ;
#74506=CARTESIAN_POINT('Ctrl Pts',(76.2385549428924,244.49208707673,6.21591725061576)) ;
#74507=CARTESIAN_POINT('Ctrl Pts',(76.2196778307588,244.496976741398,6.21372465780441)) ;
#74508=CARTESIAN_POINT('Ctrl Pts',(76.2008317612361,244.502596703282,6.21284053128981)) ;
#74509=CARTESIAN_POINT('Ctrl Pts',(76.1822313129452,244.508829679511,6.21317763161947)) ;
#74510=CARTESIAN_POINT('Ctrl Pts',(76.1652229263382,244.514529158779,6.21348587863817)) ;
#74511=CARTESIAN_POINT('Ctrl Pts',(76.1484150941123,244.520741581786,6.21481314442454)) ;
#74512=CARTESIAN_POINT('Ctrl Pts',(76.131925940963,244.527386914516,6.21708344522214)) ;
#74513=CARTESIAN_POINT('Ctrl Pts',(76.112482770511,244.535222752768,6.21976046841341)) ;
#74514=CARTESIAN_POINT('Ctrl Pts',(76.0934767109316,244.543661575844,6.22374740248841)) ;
#74515=CARTESIAN_POINT('Ctrl Pts',(76.0751055400727,244.552621536501,6.22899833985716)) ;
#74516=CARTESIAN_POINT('Ctrl Pts',(76.0686609549915,244.555764680137,6.23084036249629)) ;
#74517=CARTESIAN_POINT('Ctrl Pts',(76.0622949393628,244.55897191764,6.23283808866089)) ;
#74518=CARTESIAN_POINT('Ctrl Pts',(76.0560174782507,244.562239562755,6.23498999122571)) ;
#74519=CARTESIAN_POINT('Ctrl Pts',(76.0372400752442,244.572013878853,6.24142685176041)) ;
#74520=CARTESIAN_POINT('Ctrl Pts',(76.0191213517595,244.58226496701,6.24908226480483)) ;
#74521=CARTESIAN_POINT('Ctrl Pts',(76.0019017462595,244.592874457357,6.25787634700995)) ;
#74522=CARTESIAN_POINT('Ctrl Pts',(75.9810929668374,244.605695340181,6.26850342652273)) ;
#74523=CARTESIAN_POINT('Ctrl Pts',(75.9615970994002,244.619039772416,6.28079415544679)) ;
#74524=CARTESIAN_POINT('Ctrl Pts',(75.9432200150816,244.632701746941,6.2942409454276)) ;
#74525=CARTESIAN_POINT('Ctrl Pts',(75.9374338121325,244.637003351913,6.29847479746273)) ;
#74526=CARTESIAN_POINT('Ctrl Pts',(75.9317588233289,244.641336263499,6.30282306611641)) ;
#74527=CARTESIAN_POINT('Ctrl Pts',(75.9261898110665,244.645693623271,6.30726943863187)) ;
#74528=CARTESIAN_POINT('Ctrl Pts',(75.9167432121812,244.65308492141,6.31481172722269)) ;
#74529=CARTESIAN_POINT('Ctrl Pts',(75.9076013902148,244.66054663505,6.32263637113672)) ;
#74530=CARTESIAN_POINT('Ctrl Pts',(75.8987788178093,244.668063552107,6.33072043970214)) ;
#74531=CARTESIAN_POINT('Ctrl Pts',(75.8858753172798,244.679057459413,6.3425438374846)) ;
#74532=CARTESIAN_POINT('Ctrl Pts',(75.8735947782667,244.690167058658,6.3548936163373)) ;
#74533=CARTESIAN_POINT('Ctrl Pts',(75.8619259387552,244.701347996727,6.36768119039541)) ;
#74534=CARTESIAN_POINT('Ctrl Pts',(75.8245244921894,244.737185601429,6.40866845115694)) ;
#74535=CARTESIAN_POINT('Ctrl Pts',(75.7934068363604,244.77375673915,6.45415443988251)) ;
#74536=CARTESIAN_POINT('Ctrl Pts',(75.7667224839704,244.81034688431,6.50170616086635)) ;
#74537=CARTESIAN_POINT('Ctrl Pts',(75.7653632951594,244.812210632591,6.50412824577071)) ;
#74538=CARTESIAN_POINT('Ctrl Pts',(75.7640156635346,244.814074532772,6.50655587030767)) ;
#74539=CARTESIAN_POINT('Ctrl Pts',(75.7626793458367,244.815938489662,6.50898871181187)) ;
#74540=CARTESIAN_POINT('Ctrl Pts',(75.7322216671701,244.8584222494,6.5644386283242)) ;
#74541=CARTESIAN_POINT('Ctrl Pts',(75.7076465982727,244.900934559548,6.62259902957464)) ;
#74542=CARTESIAN_POINT('Ctrl Pts',(75.6878151675965,244.943275976356,6.68241852239716)) ;
#74543=CARTESIAN_POINT('Ctrl Pts',(75.6717433251411,244.977590423529,6.73089759988326)) ;
#74544=CARTESIAN_POINT('Ctrl Pts',(75.6587853917721,245.011792806485,6.7804659724872)) ;
#74545=CARTESIAN_POINT('Ctrl Pts',(75.6483110969455,245.045782320021,6.83056547755719)) ;
#74546=CARTESIAN_POINT('Ctrl Pts',(75.6457208412848,245.054187805192,6.84295490603485)) ;
#74547=CARTESIAN_POINT('Ctrl Pts',(75.6432823934182,245.062580296907,6.85537683699444)) ;
#74548=CARTESIAN_POINT('Ctrl Pts',(75.6409922292331,245.070959185311,6.8678283405692)) ;
#74549=CARTESIAN_POINT('Ctrl Pts',(75.6258122378237,245.126497323067,6.95036116442963)) ;
#74550=CARTESIAN_POINT('Ctrl Pts',(75.6172239927498,245.181498349157,7.03431234930241)) ;
#74551=CARTESIAN_POINT('Ctrl Pts',(75.6143557917654,245.23576402968,7.11884007619928)) ;
#74552=CARTESIAN_POINT('Ctrl Pts',(75.6137476157658,245.24727057496,7.13676341388841)) ;
#74553=CARTESIAN_POINT('Ctrl Pts',(75.6133964347853,245.258744086487,7.15471266410403)) ;
#74554=CARTESIAN_POINT('Ctrl Pts',(75.6132936573898,245.270182723559,7.17267980084131)) ;
#74555=CARTESIAN_POINT('Ctrl Pts',(75.7824688237379,245.10414043955,7.27867958884206)) ;
#74556=CARTESIAN_POINT('Ctrl Pts',(75.7826706984503,245.049050470116,7.16318984165068)) ;
#74557=CARTESIAN_POINT('Ctrl Pts',(75.7979890932181,244.936852228027,6.93380141407689)) ;
#74558=CARTESIAN_POINT('Ctrl Pts',(75.8624126704611,244.793118819323,6.66079598828704)) ;
#74559=CARTESIAN_POINT('Ctrl Pts',(75.9441595048601,244.69286791716,6.49260131446618)) ;
#74560=CARTESIAN_POINT('Ctrl Pts',(76.0060804700526,244.637579571816,6.41145429978875)) ;
#74561=CARTESIAN_POINT('Ctrl Pts',(76.087527546102,244.578310960323,6.33519313286103)) ;
#74562=CARTESIAN_POINT('Ctrl Pts',(76.2088559391776,244.524823920756,6.30217044135443)) ;
#74563=CARTESIAN_POINT('Ctrl Pts',(76.3331068362906,244.506355590964,6.35347138365035)) ;
#74564=CARTESIAN_POINT('Ctrl Pts',(76.4115789956862,244.505971060786,6.41180890998702)) ;
#74565=CARTESIAN_POINT('Ctrl Pts',(76.4941307169281,244.514452134586,6.49328329969644)) ;
#74566=CARTESIAN_POINT('Ctrl Pts',(76.6191536305483,244.547394262234,6.66117446013279)) ;
#74567=CARTESIAN_POINT('Ctrl Pts',(76.7557559389564,244.625871137754,6.93432872868204)) ;
#74568=CARTESIAN_POINT('Ctrl Pts',(76.8340341124954,244.7074402845,7.16318668389314)) ;
#74569=CARTESIAN_POINT('Ctrl Pts',(76.8665793939902,244.751891562381,7.27867958884203)) ;
#74570=CARTESIAN_POINT('Origin',(77.0279509268838,244.633742383918,16.0213203435596)) ;
#74571=CARTESIAN_POINT('',(76.8665793939902,244.751891562381,16.0254384350469)) ;
#74572=CARTESIAN_POINT('',(76.8665793939902,244.751891562381,16.0213203435596)) ;
#74573=CARTESIAN_POINT('Ctrl Pts',(76.8665793939902,244.751891562381,16.0254384350469)) ;
#74574=CARTESIAN_POINT('Ctrl Pts',(76.8784031342209,244.768040765536,16.0294645582753)) ;
#74575=CARTESIAN_POINT('Ctrl Pts',(76.892136277013,244.78172134422,16.0362204083692)) ;
#74576=CARTESIAN_POINT('Ctrl Pts',(76.9259362350405,244.807425329643,16.0560502171909)) ;
#74577=CARTESIAN_POINT('Ctrl Pts',(76.9464127977525,244.817621347006,16.070223718736)) ;
#74578=CARTESIAN_POINT('Ctrl Pts',(76.9916081849013,244.832126442816,16.1046945816754)) ;
#74579=CARTESIAN_POINT('Ctrl Pts',(77.0165903206712,244.834833453147,16.1258672215758)) ;
#74580=CARTESIAN_POINT('Ctrl Pts',(77.0656749169652,244.831784668204,16.1708720249623)) ;
#74581=CARTESIAN_POINT('Ctrl Pts',(77.0900369538065,244.825441284576,16.1951765216978)) ;
#74582=CARTESIAN_POINT('Ctrl Pts',(77.1129191197796,244.814797252538,16.2199877856629)) ;
#74583=CARTESIAN_POINT('Ctrl Pts',(77.1135321137367,244.814508309052,16.2206540664846)) ;
#74584=CARTESIAN_POINT('Ctrl Pts',(77.1141436199122,244.814216259225,16.2213203435596)) ;
#74585=CARTESIAN_POINT('Origin',(69.4298369914177,242.164965512063,16.0213203435596)) ;
#74586=CARTESIAN_POINT('',(69.4909429592658,242.355402012486,16.0254384350469)) ;
#74587=CARTESIAN_POINT('',(69.4909429592658,242.355402012486,16.0213203435596)) ;
#74588=CARTESIAN_POINT('Ctrl Pts',(69.254025755637,242.26030915041,16.2213203435596)) ;
#74589=CARTESIAN_POINT('Ctrl Pts',(69.2543488119456,242.260904857998,16.220654066481)) ;
#74590=CARTESIAN_POINT('Ctrl Pts',(69.2546748977555,242.261498926998,16.2199877856714)) ;
#74591=CARTESIAN_POINT('Ctrl Pts',(69.2650804716231,242.280229657494,16.1989219659808)) ;
#74592=CARTESIAN_POINT('Ctrl Pts',(69.2780408691307,242.296910122432,16.1784289743361)) ;
#74593=CARTESIAN_POINT('Ctrl Pts',(69.3084414776869,242.32519767757,16.1396302534792)) ;
#74594=CARTESIAN_POINT('Ctrl Pts',(69.3258200011823,242.337155324715,16.1210537744217)) ;
#74595=CARTESIAN_POINT('Ctrl Pts',(69.3661861047741,242.355940900472,16.0855257632557)) ;
#74596=CARTESIAN_POINT('Ctrl Pts',(69.3897101386423,242.362560440169,16.0684876094517)) ;
#74597=CARTESIAN_POINT('Ctrl Pts',(69.4342851322535,242.365828386096,16.0440628922209)) ;
#74598=CARTESIAN_POINT('Ctrl Pts',(69.4544003621822,242.364551935653,16.0353723462058)) ;
#74599=CARTESIAN_POINT('Ctrl Pts',(69.4802111102619,242.358597477058,16.027919277044)) ;
#74600=CARTESIAN_POINT('Ctrl Pts',(69.4855993537817,242.357116632237,16.0265673132425)) ;
#74601=CARTESIAN_POINT('Ctrl Pts',(69.4909429592658,242.355402012486,16.0254384350468)) ;
#74602=CARTESIAN_POINT('Origin',(74.5283628290597,239.4,7.2786795888419)) ;
#74603=CARTESIAN_POINT('Origin',(74.5283628290597,239.4,7.17267980084128)) ;
#74604=CARTESIAN_POINT('Origin',(75.5824701665474,245.103407553477,16.0213203435596)) ;
#74605=CARTESIAN_POINT('',(75.7824688237379,245.10414043955,16.0254384350469)) ;
#74606=CARTESIAN_POINT('',(75.7824688237379,245.10414043955,16.0213203435596)) ;
#74607=CARTESIAN_POINT('Ctrl Pts',(75.6188186954262,245.300076779459,16.2213203435596)) ;
#74608=CARTESIAN_POINT('Ctrl Pts',(75.6194850769117,245.299953618417,16.2206540664686)) ;
#74609=CARTESIAN_POINT('Ctrl Pts',(75.6201508361727,245.299827069798,16.2199877856852)) ;
#74610=CARTESIAN_POINT('Ctrl Pts',(75.6411803184818,245.295718895031,16.1989219658462)) ;
#74611=CARTESIAN_POINT('Ctrl Pts',(75.6610493665444,245.288547371652,16.1784289743552)) ;
#74612=CARTESIAN_POINT('Ctrl Pts',(75.6973467348523,245.268376010071,16.1396302535203)) ;
#74613=CARTESIAN_POINT('Ctrl Pts',(75.7140893921785,245.25554316825,16.1210537744717)) ;
#74614=CARTESIAN_POINT('Ctrl Pts',(75.744429348427,245.222957784567,16.085525763304)) ;
#74615=CARTESIAN_POINT('Ctrl Pts',(75.7579942310408,245.202630649128,16.0684876094913)) ;
#74616=CARTESIAN_POINT('Ctrl Pts',(75.7748766628741,245.161247161817,16.0440628922463)) ;
#74617=CARTESIAN_POINT('Ctrl Pts',(75.779878634262,245.141721996436,16.0353723462253)) ;
#74618=CARTESIAN_POINT('Ctrl Pts',(75.7821915674168,245.115334487368,16.027919277052)) ;
#74619=CARTESIAN_POINT('Ctrl Pts',(75.782448259119,245.109752357025,16.0265673132458)) ;
#74620=CARTESIAN_POINT('Ctrl Pts',(75.7824688237379,245.10414043955,16.0254384350468)) ;
#74621=CARTESIAN_POINT('Origin',(74.5283628290597,239.4,16.2213203435596)) ;
#74622=CARTESIAN_POINT('',(76.8407687665841,244.719095673148,16.0213203435596)) ;
#74623=CARTESIAN_POINT('Ctrl Pts',(76.8665793939903,244.751891562381,16.0254384350468)) ;
#74624=CARTESIAN_POINT('Ctrl Pts',(76.8600592573189,244.742986172915,16.0232182514845)) ;
#74625=CARTESIAN_POINT('Ctrl Pts',(76.8531765412925,244.734103685059,16.0218983740811)) ;
#74626=CARTESIAN_POINT('Ctrl Pts',(76.8442502902958,244.723244459325,16.0213707571522)) ;
#74627=CARTESIAN_POINT('Ctrl Pts',(76.8425158171676,244.721163313731,16.0213203435596)) ;
#74628=CARTESIAN_POINT('Ctrl Pts',(76.8407687665841,244.719095673148,16.0213203435596)) ;
#74629=CARTESIAN_POINT('',(75.7840731199179,245.062436901673,16.0213203435596)) ;
#74630=CARTESIAN_POINT('Origin',(74.5283628290597,239.4,16.0213203435596)) ;
#74631=CARTESIAN_POINT('Ctrl Pts',(75.784073119918,245.062436901673,16.0213203435596)) ;
#74632=CARTESIAN_POINT('Ctrl Pts',(75.7832477134999,245.073687280317,16.0213203435596)) ;
#74633=CARTESIAN_POINT('Ctrl Pts',(75.7827408846003,245.084964948541,16.0221950109068)) ;
#74634=CARTESIAN_POINT('Ctrl Pts',(75.7825057064519,245.098841078978,16.0244263118334)) ;
#74635=CARTESIAN_POINT('Ctrl Pts',(75.7824785074899,245.101497822276,16.0249068532759)) ;
#74636=CARTESIAN_POINT('Ctrl Pts',(75.7824688237379,245.10414043955,16.0254384350468)) ;
#74637=CARTESIAN_POINT('Origin',(70.3231932313898,243.3945648893,16.0213203435596)) ;
#74638=CARTESIAN_POINT('',(70.1609601392448,243.277601545414,16.0254384350468)) ;
#74639=CARTESIAN_POINT('',(70.1609601392448,243.277601545414,16.0213203435596)) ;
#74640=CARTESIAN_POINT('Ctrl Pts',(70.1609601392448,243.277601545414,16.0254384350468)) ;
#74641=CARTESIAN_POINT('Ctrl Pts',(70.1492550710199,243.293836968828,16.0294645582753)) ;
#74642=CARTESIAN_POINT('Ctrl Pts',(70.140487842024,243.311125495076,16.0362204083692)) ;
#74643=CARTESIAN_POINT('Ctrl Pts',(70.1264866606326,243.351214133727,16.0560502171909)) ;
#74644=CARTESIAN_POINT('Ctrl Pts',(70.1231172777434,243.373839244766,16.070223718736)) ;
#74645=CARTESIAN_POINT('Ctrl Pts',(70.1232882545508,243.421304933331,16.1046945816756)) ;
#74646=CARTESIAN_POINT('Ctrl Pts',(70.1284336392439,243.445900868542,16.1258672215763)) ;
#74647=CARTESIAN_POINT('Ctrl Pts',(70.1465011804487,243.491640967338,16.1708720249636)) ;
#74648=CARTESIAN_POINT('Ctrl Pts',(70.1600623801825,243.512850427881,16.1951765217044)) ;
#74649=CARTESIAN_POINT('Ctrl Pts',(70.1772564343691,243.531323474151,16.2199877856641)) ;
#74650=CARTESIAN_POINT('Ctrl Pts',(70.1777206615032,243.5318171776,16.2206540664853)) ;
#74651=CARTESIAN_POINT('Ctrl Pts',(70.1781873831942,243.532308506173,16.2213203435596)) ;
#74652=CARTESIAN_POINT('Origin',(74.5283628290597,239.4,16.2213203435596)) ;
#74653=CARTESIAN_POINT('',(70.1841749609036,243.242919692911,16.0213203435596)) ;
#74654=CARTESIAN_POINT('Ctrl Pts',(70.1609601392449,243.277601545414,16.0254384350468)) ;
#74655=CARTESIAN_POINT('Ctrl Pts',(70.1674148348898,243.268648610259,16.0232182514845)) ;
#74656=CARTESIAN_POINT('Ctrl Pts',(70.1737357066263,243.259357918633,16.0218983740811)) ;
#74657=CARTESIAN_POINT('Ctrl Pts',(70.1813050807688,243.247512864158,16.0213707571522)) ;
#74658=CARTESIAN_POINT('Ctrl Pts',(70.1827483861738,243.245220172831,16.0213203435596)) ;
#74659=CARTESIAN_POINT('Ctrl Pts',(70.1841749609038,243.242919692911,16.0213203435596)) ;
#74660=CARTESIAN_POINT('',(69.5311011354998,242.344040686892,16.0213203435596)) ;
#74661=CARTESIAN_POINT('Origin',(74.5283628290597,239.4,16.0213203435596)) ;
#74662=CARTESIAN_POINT('Ctrl Pts',(69.5311011355,242.344040686893,16.0213203435596)) ;
#74663=CARTESIAN_POINT('Ctrl Pts',(69.5201463249695,242.346732236934,16.0213203435596)) ;
#74664=CARTESIAN_POINT('Ctrl Pts',(69.5092640063738,242.349735205145,16.0221950109068)) ;
#74665=CARTESIAN_POINT('Ctrl Pts',(69.4959943480554,242.353799497556,16.0244263118334)) ;
#74666=CARTESIAN_POINT('Ctrl Pts',(69.4934592300887,242.354594608634,16.0249068532759)) ;
#74667=CARTESIAN_POINT('Ctrl Pts',(69.4909429592658,242.355402012486,16.0254384350468)) ;
#74668=CARTESIAN_POINT('Ctrl Pts',(73.9584121733008,245.2125,7.27867958884205)) ;
#74669=CARTESIAN_POINT('Ctrl Pts',(73.9756279482132,245.160168574929,7.163189547307)) ;
#74670=CARTESIAN_POINT('Ctrl Pts',(74.0248679112718,245.058195067006,6.93380047883313)) ;
#74671=CARTESIAN_POINT('Ctrl Pts',(74.1305548836119,244.941404186597,6.6607943976457)) ;
#74672=CARTESIAN_POINT('Ctrl Pts',(74.2392805618495,244.871321000177,6.49259951597657)) ;
#74673=CARTESIAN_POINT('Ctrl Pts',(74.3152563853318,244.837873343214,6.41145261667884)) ;
#74674=CARTESIAN_POINT('Ctrl Pts',(74.4110327691165,244.806674217527,6.33519178586455)) ;
#74675=CARTESIAN_POINT('Ctrl Pts',(74.5429519916097,244.793298107963,6.30217046564658)) ;
#74676=CARTESIAN_POINT('Ctrl Pts',(74.6668285233745,244.814129955813,6.35347296267426)) ;
#74677=CARTESIAN_POINT('Ctrl Pts',(74.7415786175593,244.838013779146,6.41181121705515)) ;
#74678=CARTESIAN_POINT('Ctrl Pts',(74.8174689638568,244.871590004575,6.49328644843118)) ;
#74679=CARTESIAN_POINT('Ctrl Pts',(74.9261925907657,244.941554190683,6.66117794267636)) ;
#74680=CARTESIAN_POINT('Ctrl Pts',(75.0318583408227,245.058403735858,6.93433474994977)) ;
#74681=CARTESIAN_POINT('Ctrl Pts',(75.0810977099062,245.160168574929,7.16318954730704)) ;
#74682=CARTESIAN_POINT('Ctrl Pts',(75.0983134848186,245.2125,7.27867958884208)) ;
#74683=CARTESIAN_POINT('Ctrl Pts',(73.9442186760216,245.255644496436,7.24979207607672)) ;
#74684=CARTESIAN_POINT('Ctrl Pts',(73.9582438127982,245.199332275759,7.13558318832877)) ;
#74685=CARTESIAN_POINT('Ctrl Pts',(74.0030866391885,245.088284257301,6.90837475287202)) ;
#74686=CARTESIAN_POINT('Ctrl Pts',(74.1089313625797,244.958729891281,6.63742123865064)) ;
#74687=CARTESIAN_POINT('Ctrl Pts',(74.2219239380421,244.880176771883,6.47033490089512)) ;
#74688=CARTESIAN_POINT('Ctrl Pts',(74.301852720505,244.842534564145,6.38969559217932)) ;
#74689=CARTESIAN_POINT('Ctrl Pts',(74.4032076200201,244.807328560718,6.31389543197594)) ;
#74690=CARTESIAN_POINT('Ctrl Pts',(74.5439426909897,244.792181977109,6.28106451887594)) ;
#74691=CARTESIAN_POINT('Ctrl Pts',(74.6757758209022,244.81575136187,6.33206751004191)) ;
#74692=CARTESIAN_POINT('Ctrl Pts',(74.754889298075,244.842695948385,6.3900521489566)) ;
#74693=CARTESIAN_POINT('Ctrl Pts',(74.834715417332,244.880485650139,6.47101811980182)) ;
#74694=CARTESIAN_POINT('Ctrl Pts',(74.9477489964978,244.958901579953,6.63780263189585)) ;
#74695=CARTESIAN_POINT('Ctrl Pts',(75.0535155836388,245.088524548487,6.90890516875891)) ;
#74696=CARTESIAN_POINT('Ctrl Pts',(75.0984818453212,245.199332275759,7.13558318832881)) ;
#74697=CARTESIAN_POINT('Ctrl Pts',(75.1125069820978,245.255644496436,7.24979207607676)) ;
#74698=CARTESIAN_POINT('Ctrl Pts',(73.8813809317722,245.318035047894,7.19960839071961)) ;
#74699=CARTESIAN_POINT('Ctrl Pts',(73.8957857168573,245.253001355885,7.08747698484384)) ;
#74700=CARTESIAN_POINT('Ctrl Pts',(73.9438000409784,245.124940024636,6.86386231950441)) ;
#74701=CARTESIAN_POINT('Ctrl Pts',(74.0607081520988,244.976082733332,6.59636871271614)) ;
#74702=CARTESIAN_POINT('Ctrl Pts',(74.1864485595767,244.886061710793,6.4311762697182)) ;
#74703=CARTESIAN_POINT('Ctrl Pts',(74.2755814288091,244.842971168061,6.35140872171606)) ;
#74704=CARTESIAN_POINT('Ctrl Pts',(74.3886668491307,244.802699316777,6.27640300071364)) ;
#74705=CARTESIAN_POINT('Ctrl Pts',(74.5458063775715,244.785389925441,6.24390250673374)) ;
#74706=CARTESIAN_POINT('Ctrl Pts',(74.6930323705689,244.812330433283,6.29438711209566)) ;
#74707=CARTESIAN_POINT('Ctrl Pts',(74.7813025349178,244.843154077251,6.35176231641292)) ;
#74708=CARTESIAN_POINT('Ctrl Pts',(74.8703326302217,244.886412364113,6.43185373754292)) ;
#74709=CARTESIAN_POINT('Ctrl Pts',(74.9960610602972,244.97627786093,6.59674657937938)) ;
#74710=CARTESIAN_POINT('Ctrl Pts',(75.1129561491309,245.125210454642,6.86438826993789)) ;
#74711=CARTESIAN_POINT('Ctrl Pts',(75.1609399412621,245.253001355885,7.08747698484388)) ;
#74712=CARTESIAN_POINT('Ctrl Pts',(75.1753447263472,245.318035047894,7.19960839071964)) ;
#74713=CARTESIAN_POINT('Ctrl Pts',(73.7857523481751,245.325510764496,7.17608503411331)) ;
#74714=CARTESIAN_POINT('Ctrl Pts',(73.8065662128101,245.256312274755,7.06215944566086)) ;
#74715=CARTESIAN_POINT('Ctrl Pts',(73.8681806184035,245.121213402276,6.83553876784966)) ;
#74716=CARTESIAN_POINT('Ctrl Pts',(74.0048230497562,244.966091331847,6.56530464002508)) ;
#74717=CARTESIAN_POINT('Ctrl Pts',(74.1472039166702,244.872894481501,6.39866345547885)) ;
#74718=CARTESIAN_POINT('Ctrl Pts',(74.2471300500745,244.82839597854,6.31823906006952)) ;
#74719=CARTESIAN_POINT('Ctrl Pts',(74.373344481406,244.786877403095,6.24264091507692)) ;
#74720=CARTESIAN_POINT('Ctrl Pts',(74.5476677047595,244.769070794076,6.20989751501573)) ;
#74721=CARTESIAN_POINT('Ctrl Pts',(74.7112510718069,244.796800388377,6.26076462735167)) ;
#74722=CARTESIAN_POINT('Ctrl Pts',(74.8097608852416,244.828583281404,6.31859474911539)) ;
#74723=CARTESIAN_POINT('Ctrl Pts',(74.9095746445357,244.873253186347,6.39934495813431)) ;
#74724=CARTESIAN_POINT('Ctrl Pts',(75.0519449212146,244.966291180321,6.56568507344858)) ;
#74725=CARTESIAN_POINT('Ctrl Pts',(75.1885693996538,245.12149181155,6.83606809856267)) ;
#74726=CARTESIAN_POINT('Ctrl Pts',(75.2501594453092,245.256312274755,7.0621594456609)) ;
#74727=CARTESIAN_POINT('Ctrl Pts',(75.2709733099443,245.325510764496,7.17608503411335)) ;
#74728=CARTESIAN_POINT('Ctrl Pts',(73.7462071414064,245.31813759476,7.17267980084142)) ;
#74729=CARTESIAN_POINT('Ctrl Pts',(73.7695561765774,245.248414521712,7.05718975930637)) ;
#74730=CARTESIAN_POINT('Ctrl Pts',(73.8366071882365,245.112634011735,6.82780069083249)) ;
#74731=CARTESIAN_POINT('Ctrl Pts',(73.9812905940924,244.957342302858,6.55479460964506)) ;
#74732=CARTESIAN_POINT('Ctrl Pts',(74.1305914868933,244.864258836729,6.38659972797594)) ;
#74733=CARTESIAN_POINT('Ctrl Pts',(74.2350497606397,244.819855671617,6.30545282867821)) ;
#74734=CARTESIAN_POINT('Ctrl Pts',(74.3668103693923,244.778451814907,6.22919199786392)) ;
#74735=CARTESIAN_POINT('Ctrl Pts',(74.5484587576374,244.760708922492,6.19617067764595)) ;
#74736=CARTESIAN_POINT('Ctrl Pts',(74.7189909128558,244.788344748346,6.24747317467362)) ;
#74737=CARTESIAN_POINT('Ctrl Pts',(74.821826950362,244.820041650107,6.30581142905452)) ;
#74738=CARTESIAN_POINT('Ctrl Pts',(74.926167092777,244.864615079948,6.38728666043055)) ;
#74739=CARTESIAN_POINT('Ctrl Pts',(75.0754651947014,244.957540938993,6.55517815467573)) ;
#74740=CARTESIAN_POINT('Ctrl Pts',(75.220119269038,245.112910324599,6.82833496194914)) ;
#74741=CARTESIAN_POINT('Ctrl Pts',(75.287169481542,245.248414521712,7.05718975930641)) ;
#74742=CARTESIAN_POINT('Ctrl Pts',(75.310518516713,245.31813759476,7.17267980084145)) ;
#74743=CARTESIAN_POINT('Ctrl Pts',(75.3105185167129,245.31813759476,7.17267980084142)) ;
#74744=CARTESIAN_POINT('Ctrl Pts',(75.287169481542,245.248414521712,7.05718975930639)) ;
#74745=CARTESIAN_POINT('Ctrl Pts',(75.220119269038,245.1129103246,6.82833496194911)) ;
#74746=CARTESIAN_POINT('Ctrl Pts',(75.0754651947014,244.957540938994,6.55517815467573)) ;
#74747=CARTESIAN_POINT('Ctrl Pts',(74.926167092777,244.864615079948,6.38728666043055)) ;
#74748=CARTESIAN_POINT('Ctrl Pts',(74.8218269503619,244.820041650108,6.30581142905452)) ;
#74749=CARTESIAN_POINT('Ctrl Pts',(74.7189909128558,244.788344748345,6.24747317467363)) ;
#74750=CARTESIAN_POINT('Ctrl Pts',(74.5484587576374,244.760708922493,6.19617067764596)) ;
#74751=CARTESIAN_POINT('Ctrl Pts',(74.3668103693923,244.778451814907,6.22919199786392)) ;
#74752=CARTESIAN_POINT('Ctrl Pts',(74.2350497606398,244.819855671617,6.3054528286782)) ;
#74753=CARTESIAN_POINT('Ctrl Pts',(74.1305914868933,244.864258836729,6.38659972797596)) ;
#74754=CARTESIAN_POINT('Ctrl Pts',(73.9812905940924,244.957342302859,6.55479460964504)) ;
#74755=CARTESIAN_POINT('Ctrl Pts',(73.8366071882364,245.112634011734,6.82780069083246)) ;
#74756=CARTESIAN_POINT('Ctrl Pts',(73.7695561765774,245.248414521712,7.05718975930628)) ;
#74757=CARTESIAN_POINT('Ctrl Pts',(73.7462071414064,245.31813759476,7.17267980084129)) ;
#74758=CARTESIAN_POINT('Ctrl Pts',(73.9584121733008,245.2125,7.27867958884205)) ;
#74759=CARTESIAN_POINT('Ctrl Pts',(73.9756279482132,245.160168574929,7.163189547307)) ;
#74760=CARTESIAN_POINT('Ctrl Pts',(74.0248679112718,245.058195067006,6.93380047883313)) ;
#74761=CARTESIAN_POINT('Ctrl Pts',(74.1305548836119,244.941404186597,6.6607943976457)) ;
#74762=CARTESIAN_POINT('Ctrl Pts',(74.2392805618495,244.871321000177,6.49259951597657)) ;
#74763=CARTESIAN_POINT('Ctrl Pts',(74.3152563853318,244.837873343214,6.41145261667884)) ;
#74764=CARTESIAN_POINT('Ctrl Pts',(74.4110327691165,244.806674217527,6.33519178586455)) ;
#74765=CARTESIAN_POINT('Ctrl Pts',(74.5429519916097,244.793298107963,6.30217046564658)) ;
#74766=CARTESIAN_POINT('Ctrl Pts',(74.6668285233745,244.814129955813,6.35347296267426)) ;
#74767=CARTESIAN_POINT('Ctrl Pts',(74.7415786175593,244.838013779146,6.41181121705515)) ;
#74768=CARTESIAN_POINT('Ctrl Pts',(74.8174689638568,244.871590004575,6.49328644843118)) ;
#74769=CARTESIAN_POINT('Ctrl Pts',(74.9261925907657,244.941554190683,6.66117794267636)) ;
#74770=CARTESIAN_POINT('Ctrl Pts',(75.0318583408227,245.058403735858,6.93433474994977)) ;
#74771=CARTESIAN_POINT('Ctrl Pts',(75.0810977099062,245.160168574929,7.16318954730704)) ;
#74772=CARTESIAN_POINT('Ctrl Pts',(75.0983134848186,245.2125,7.27867958884208)) ;
#74773=CARTESIAN_POINT('Origin',(75.2882970367382,245.15,16.0213203435596)) ;
#74774=CARTESIAN_POINT('',(75.0983134848186,245.2125,16.0254384350469)) ;
#74775=CARTESIAN_POINT('',(75.0983134848186,245.2125,16.0213203435596)) ;
#74776=CARTESIAN_POINT('Ctrl Pts',(75.0983134848186,245.2125,16.0254384350469)) ;
#74777=CARTESIAN_POINT('Ctrl Pts',(75.1045681517916,245.231512541561,16.0294645582753)) ;
#74778=CARTESIAN_POINT('Ctrl Pts',(75.1134016154265,245.248767319575,16.0362204083691)) ;
#74779=CARTESIAN_POINT('Ctrl Pts',(75.1376043174404,245.283658023846,16.056050217191)) ;
#74780=CARTESIAN_POINT('Ctrl Pts',(75.153927943199,245.299682618464,16.0702237187361)) ;
#74781=CARTESIAN_POINT('Ctrl Pts',(75.1924289895435,245.32744392705,16.1046945816758)) ;
#74782=CARTESIAN_POINT('Ctrl Pts',(75.2153519003623,245.337738351374,16.1258672215766)) ;
#74783=CARTESIAN_POINT('Ctrl Pts',(75.2629762518785,245.350006759003,16.1708720249644)) ;
#74784=CARTESIAN_POINT('Ctrl Pts',(75.288106139114,245.351502126069,16.1951765216962)) ;
#74785=CARTESIAN_POINT('Ctrl Pts',(75.3131575589535,245.348450028194,16.2199877856658)) ;
#74786=CARTESIAN_POINT('Ctrl Pts',(75.3138298392969,245.34836465216,16.2206540664851)) ;
#74787=CARTESIAN_POINT('Ctrl Pts',(75.3145016645892,245.348275862069,16.2213203435596)) ;
#74788=CARTESIAN_POINT('Origin',(70.5337979397592,243.60516959767,16.0213203435596)) ;
#74789=CARTESIAN_POINT('',(70.6507612836456,243.767402689815,16.0254384350468)) ;
#74790=CARTESIAN_POINT('',(70.6507612836456,243.767402689815,16.0213203435596)) ;
#74791=CARTESIAN_POINT('Ctrl Pts',(70.3960543228868,243.750175445865,16.2213203435596)) ;
#74792=CARTESIAN_POINT('Ctrl Pts',(70.3965456514624,243.750642167559,16.2206540664813)) ;
#74793=CARTESIAN_POINT('Ctrl Pts',(70.3970393549119,243.751106394694,16.219987785665)) ;
#74794=CARTESIAN_POINT('Ctrl Pts',(70.4127237578114,243.765704878851,16.1989219660085)) ;
#74795=CARTESIAN_POINT('Ctrl Pts',(70.4302043754361,243.777563960622,16.1784289743291)) ;
#74796=CARTESIAN_POINT('Ctrl Pts',(70.4678584075735,243.795072719583,16.1396302534698)) ;
#74797=CARTESIAN_POINT('Ctrl Pts',(70.4880814817692,243.801074858721,16.1210537744116)) ;
#74798=CARTESIAN_POINT('Ctrl Pts',(70.5322769897868,243.806467190948,16.0855257632468)) ;
#74799=CARTESIAN_POINT('Ctrl Pts',(70.5566952257469,243.805493421069,16.0684876094444)) ;
#74800=CARTESIAN_POINT('Ctrl Pts',(70.6000984147111,243.794826991786,16.0440628922162)) ;
#74801=CARTESIAN_POINT('Ctrl Pts',(70.6188346903313,243.787397067379,16.0353723462022)) ;
#74802=CARTESIAN_POINT('Ctrl Pts',(70.6415421415812,243.773758080939,16.0279192770425)) ;
#74803=CARTESIAN_POINT('Ctrl Pts',(70.6462090594739,243.770684655006,16.0265673132419)) ;
#74804=CARTESIAN_POINT('Ctrl Pts',(70.6507612836456,243.767402689815,16.0254384350468)) ;
#74805=CARTESIAN_POINT('Origin',(74.5283628290597,239.4,7.2786795888419)) ;
#74806=CARTESIAN_POINT('Origin',(74.5283628290597,239.4,7.17267980084126)) ;
#74807=CARTESIAN_POINT('Origin',(73.7684286213812,245.15,16.0213203435596)) ;
#74808=CARTESIAN_POINT('',(73.9584121733008,245.2125,16.0254384350469)) ;
#74809=CARTESIAN_POINT('',(73.9584121733008,245.2125,16.0213203435596)) ;
#74810=CARTESIAN_POINT('Ctrl Pts',(73.7422239935302,245.348275862069,16.2213203435596)) ;
#74811=CARTESIAN_POINT('Ctrl Pts',(73.7428958188243,245.34836465216,16.2206540664833)) ;
#74812=CARTESIAN_POINT('Ctrl Pts',(73.7435680991642,245.348450028194,16.2199877856676)) ;
#74813=CARTESIAN_POINT('Ctrl Pts',(73.764837821366,245.351041389257,16.1989219660258)) ;
#74814=CARTESIAN_POINT('Ctrl Pts',(73.7859505314575,245.350360738705,16.178428974329)) ;
#74815=CARTESIAN_POINT('Ctrl Pts',(73.8267046736716,245.342393137473,16.1396302534651)) ;
#74816=CARTESIAN_POINT('Ctrl Pts',(73.8465934532444,245.335362145269,16.1210537744048)) ;
#74817=CARTESIAN_POINT('Ctrl Pts',(73.8855179036651,245.313747165846,16.0855257632396)) ;
#74818=CARTESIAN_POINT('Ctrl Pts',(73.9047003039537,245.29860669048,16.0684876094385)) ;
#74819=CARTESIAN_POINT('Ctrl Pts',(73.9335446516065,245.264465613545,16.0440628922123)) ;
#74820=CARTESIAN_POINT('Ctrl Pts',(73.944335417002,245.247441771941,16.0353723461993)) ;
#74821=CARTESIAN_POINT('Ctrl Pts',(73.9546893358739,245.223060495165,16.0279192770413)) ;
#74822=CARTESIAN_POINT('Ctrl Pts',(73.9566584373223,245.217830895845,16.0265673132414)) ;
#74823=CARTESIAN_POINT('Ctrl Pts',(73.9584121733008,245.2125,16.0254384350468)) ;
#74824=CARTESIAN_POINT('Origin',(74.5283628290597,239.4,16.2213203435596)) ;
#74825=CARTESIAN_POINT('',(75.083900606553,245.173333333333,16.0213203435596)) ;
#74826=CARTESIAN_POINT('Ctrl Pts',(75.0983134848186,245.2125,16.0254384350468)) ;
#74827=CARTESIAN_POINT('Ctrl Pts',(75.0948643830368,245.202015638281,16.0232182514845)) ;
#74828=CARTESIAN_POINT('Ctrl Pts',(75.0910633708098,245.191441014105,16.0218983740811)) ;
#74829=CARTESIAN_POINT('Ctrl Pts',(75.0859296869309,245.178354913455,16.0213707571522)) ;
#74830=CARTESIAN_POINT('Ctrl Pts',(75.0849232143161,245.175839644704,16.0213203435596)) ;
#74831=CARTESIAN_POINT('Ctrl Pts',(75.0839006065529,245.173333333333,16.0213203435596)) ;
#74832=CARTESIAN_POINT('',(73.9728250515664,245.173333333333,16.0213203435596)) ;
#74833=CARTESIAN_POINT('Origin',(74.5283628290597,239.4,16.0213203435596)) ;
#74834=CARTESIAN_POINT('Ctrl Pts',(73.9728250515665,245.173333333333,16.0213203435596)) ;
#74835=CARTESIAN_POINT('Ctrl Pts',(73.9685634852199,245.183778014643,16.0213203435596)) ;
#74836=CARTESIAN_POINT('Ctrl Pts',(73.9645964711543,245.194347095752,16.0221950109068)) ;
#74837=CARTESIAN_POINT('Ctrl Pts',(73.9600848433223,245.207471405981,16.0244263118334)) ;
#74838=CARTESIAN_POINT('Ctrl Pts',(73.9592379967437,245.209989714065,16.0249068532759)) ;
#74839=CARTESIAN_POINT('Ctrl Pts',(73.9584121733008,245.2125,16.0254384350468)) ;
#74840=CARTESIAN_POINT('Origin',(71.7633973169968,244.498525837642,16.0213203435596)) ;
#74841=CARTESIAN_POINT('',(71.5729608165738,244.437419869794,16.0254384350468)) ;
#74842=CARTESIAN_POINT('',(71.5729608165738,244.437419869794,16.0213203435596)) ;
#74843=CARTESIAN_POINT('Ctrl Pts',(71.5729608165738,244.437419869794,16.0254384350468)) ;
#74844=CARTESIAN_POINT('Ctrl Pts',(71.5668456569106,244.456477740028,16.0294645582753)) ;
#74845=CARTESIAN_POINT('Ctrl Pts',(71.5638499750624,244.475629328327,16.0362204083692)) ;
#74846=CARTESIAN_POINT('Ctrl Pts',(71.562922130889,244.518082492337,16.056050217191)) ;
#74847=CARTESIAN_POINT('Ctrl Pts',(71.5667092011469,244.540641448196,16.0702237187361)) ;
#74848=CARTESIAN_POINT('Ctrl Pts',(71.58153951417,244.585731165867,16.1046945816758)) ;
#74849=CARTESIAN_POINT('Ctrl Pts',(71.5940336277842,244.607533279011,16.1258672215766)) ;
#74850=CARTESIAN_POINT('Ctrl Pts',(71.6253513484332,244.645451520748,16.1708720249643)) ;
#74851=CARTESIAN_POINT('Ctrl Pts',(71.6448028995719,244.66143227523,16.1951765216869)) ;
#74852=CARTESIAN_POINT('Ctrl Pts',(71.6668639020685,244.673687931308,16.2199877856679)) ;
#74853=CARTESIAN_POINT('Ctrl Pts',(71.6674579710636,244.674014017115,16.2206540664832)) ;
#74854=CARTESIAN_POINT('Ctrl Pts',(71.6680536786498,244.674337073423,16.2213203435596)) ;
#74855=CARTESIAN_POINT('Origin',(74.5283628290597,239.4,16.2213203435596)) ;
#74856=CARTESIAN_POINT('',(71.5843221421672,244.39726169356,16.0213203435596)) ;
#74857=CARTESIAN_POINT('Ctrl Pts',(71.5729608165739,244.437419869794,16.0254384350468)) ;
#74858=CARTESIAN_POINT('Ctrl Pts',(71.5763329878152,244.426910511827,16.0232182514845)) ;
#74859=CARTESIAN_POINT('Ctrl Pts',(71.5794735124668,244.416121282229,16.0218983740811)) ;
#74860=CARTESIAN_POINT('Ctrl Pts',(71.5830120919375,244.402516900739,16.0213707571522)) ;
#74861=CARTESIAN_POINT('Ctrl Pts',(71.583676276365,244.399890415814,16.0213203435596)) ;
#74862=CARTESIAN_POINT('Ctrl Pts',(71.5843221421673,244.39726169356,16.0213203435596)) ;
#74863=CARTESIAN_POINT('',(70.6854431361484,243.744187868156,16.0213203435596)) ;
#74864=CARTESIAN_POINT('Origin',(74.5283628290597,239.4,16.0213203435596)) ;
#74865=CARTESIAN_POINT('Ctrl Pts',(70.6854431361486,243.744187868156,16.0213203435596)) ;
#74866=CARTESIAN_POINT('Ctrl Pts',(70.675856226913,243.750132906986,16.0213203435596)) ;
#74867=CARTESIAN_POINT('Ctrl Pts',(70.6664344951108,243.756351720855,16.0221950109068)) ;
#74868=CARTESIAN_POINT('Ctrl Pts',(70.6550702355232,243.764317642567,16.0244263118334)) ;
#74869=CARTESIAN_POINT('Ctrl Pts',(70.652904897897,243.765857232674,16.0249068532759)) ;
#74870=CARTESIAN_POINT('Ctrl Pts',(70.6507612836457,243.767402689815,16.0254384350468)) ;
#74871=CARTESIAN_POINT('Ctrl Pts',(72.1901462641291,244.751891562381,7.27867958884205)) ;
#74872=CARTESIAN_POINT('Ctrl Pts',(72.2226915456361,244.707440284483,7.16318668384993)) ;
#74873=CARTESIAN_POINT('Ctrl Pts',(72.3010345108137,244.62567313033,6.93379520902284)) ;
#74874=CARTESIAN_POINT('Ctrl Pts',(72.4376389789193,244.547258447274,6.66079124794237)) ;
#74875=CARTESIAN_POINT('Ctrl Pts',(72.5627005459071,244.514203826472,6.49259685569267)) ;
#74876=CARTESIAN_POINT('Ctrl Pts',(72.6452938287017,244.505871428575,6.411450768915)) ;
#74877=CARTESIAN_POINT('Ctrl Pts',(72.7460237857294,244.505796254997,6.33519080978562)) ;
#74878=CARTESIAN_POINT('Ctrl Pts',(72.8756195873876,244.533840692988,6.30217109838147)) ;
#74879=CARTESIAN_POINT('Ctrl Pts',(72.986994973301,244.591933082758,6.35347460249892)) ;
#74880=CARTESIAN_POINT('Ctrl Pts',(73.0507055731919,244.637746956413,6.41181309644325)) ;
#74881=CARTESIAN_POINT('Ctrl Pts',(73.1125055094761,244.693131160356,6.49328843787088)) ;
#74882=CARTESIAN_POINT('Ctrl Pts',(73.1942872183044,244.793268231079,6.66117964447055)) ;
#74883=CARTESIAN_POINT('Ctrl Pts',(73.2586724865194,244.937050873409,6.93433578523243)) ;
#74884=CARTESIAN_POINT('Ctrl Pts',(73.2740549596695,245.049050470208,7.1631898418427)) ;
#74885=CARTESIAN_POINT('Ctrl Pts',(73.2742568343815,245.10414043955,7.27867958884209)) ;
#74886=CARTESIAN_POINT('Ctrl Pts',(72.1633150634402,244.78853838499,7.24979207607672)) ;
#74887=CARTESIAN_POINT('Ctrl Pts',(72.1940559565136,244.739315065769,7.13558035663659)) ;
#74888=CARTESIAN_POINT('Ctrl Pts',(72.2710212515803,244.647558801653,6.90836946535324)) ;
#74889=CARTESIAN_POINT('Ctrl Pts',(72.4117199496733,244.557054257005,6.63741801934678)) ;
#74890=CARTESIAN_POINT('Ctrl Pts',(72.5434569761114,244.517262868332,6.47033215351056)) ;
#74891=CARTESIAN_POINT('Ctrl Pts',(72.631105954999,244.506162798098,6.38969365013118)) ;
#74892=CARTESIAN_POINT('Ctrl Pts',(72.738379604366,244.50400077796,6.31389435183346)) ;
#74893=CARTESIAN_POINT('Ctrl Pts',(72.8769068455281,244.533085740452,6.28106503242219)) ;
#74894=CARTESIAN_POINT('Ctrl Pts',(72.9950033871039,244.596240433655,6.33206902621705)) ;
#74895=CARTESIAN_POINT('Ctrl Pts',(73.0619179397723,244.646313620026,6.39005390425698)) ;
#74896=CARTESIAN_POINT('Ctrl Pts',(73.1261589448907,244.706921292487,6.4710199832332)) ;
#74897=CARTESIAN_POINT('Ctrl Pts',(73.2094278923994,244.816428207189,6.63780422869352)) ;
#74898=CARTESIAN_POINT('Ctrl Pts',(73.2699618445942,244.972390194654,6.90890610769434)) ;
#74899=CARTESIAN_POINT('Ctrl Pts',(73.278485994941,245.091669363501,7.13558347959712)) ;
#74900=CARTESIAN_POINT('Ctrl Pts',(73.2744232698454,245.149559325897,7.24979207607676)) ;
#74901=CARTESIAN_POINT('Ctrl Pts',(72.0842730845649,244.828457427666,7.19960837676255)) ;
#74902=CARTESIAN_POINT('Ctrl Pts',(72.1180702032677,244.771056611335,7.08747419070363)) ;
#74903=CARTESIAN_POINT('Ctrl Pts',(72.2033093580407,244.664099445641,6.86385716177446)) ;
#74904=CARTESIAN_POINT('Ctrl Pts',(72.3604949046759,244.558655570097,6.59636562128617)) ;
#74905=CARTESIAN_POINT('Ctrl Pts',(72.5078996758972,244.511896865288,6.43117365814849)) ;
#74906=CARTESIAN_POINT('Ctrl Pts',(72.6059859036912,244.49845940005,6.35140690677207)) ;
#74907=CARTESIAN_POINT('Ctrl Pts',(72.7259813969145,244.495104456363,6.27640204319265)) ;
#74908=CARTESIAN_POINT('Ctrl Pts',(72.8807785181998,244.527201799561,6.24390313457582)) ;
#74909=CARTESIAN_POINT('Ctrl Pts',(73.0124726998353,244.598319318779,6.2943887303005)) ;
#74910=CARTESIAN_POINT('Ctrl Pts',(73.0868970256526,244.654911283162,6.35176416943413)) ;
#74911=CARTESIAN_POINT('Ctrl Pts',(73.1582015882457,244.723564062097,6.43185569767935)) ;
#74912=CARTESIAN_POINT('Ctrl Pts',(73.2500058742025,244.847883120417,6.59674825081069)) ;
#74913=CARTESIAN_POINT('Ctrl Pts',(73.3151566187034,245.025648513998,6.8643892827353)) ;
#74914=CARTESIAN_POINT('Ctrl Pts',(73.3213024844566,245.162012348452,7.0874772568569)) ;
#74915=CARTESIAN_POINT('Ctrl Pts',(73.3149057494537,245.228314219316,7.19960837676259)) ;
#74916=CARTESIAN_POINT('Ctrl Pts',(71.9910147655644,244.806016366157,7.17608503411331)) ;
#74917=CARTESIAN_POINT('Ctrl Pts',(72.0321944574529,244.746635057199,7.0621566209928)) ;
#74918=CARTESIAN_POINT('Ctrl Pts',(72.1325429398017,244.637187568385,6.83553351420321)) ;
#74919=CARTESIAN_POINT('Ctrl Pts',(72.3104327593928,244.531883870857,6.5653014585105)) ;
#74920=CARTESIAN_POINT('Ctrl Pts',(72.4746449644358,244.487247007328,6.39866074879488)) ;
#74921=CARTESIAN_POINT('Ctrl Pts',(72.5834312809955,244.475805815997,6.31823715694155)) ;
#74922=CARTESIAN_POINT('Ctrl Pts',(72.7162984783341,244.475322282895,6.24263987289687)) ;
#74923=CARTESIAN_POINT('Ctrl Pts',(72.8875918907321,244.512256825088,6.20989806420845)) ;
#74924=CARTESIAN_POINT('Ctrl Pts',(73.0345989364271,244.589179504376,6.26076617601792)) ;
#74925=CARTESIAN_POINT('Ctrl Pts',(73.1184652751015,244.649847982056,6.31859653587809)) ;
#74926=CARTESIAN_POINT('Ctrl Pts',(73.1995894461384,244.723175613832,6.39934685299362)) ;
#74927=CARTESIAN_POINT('Ctrl Pts',(73.3062406700047,244.855654460481,6.56568669597758)) ;
#74928=CARTESIAN_POINT('Ctrl Pts',(73.388218198327,245.045477794218,6.8360690634198)) ;
#74929=CARTESIAN_POINT('Ctrl Pts',(73.405132183067,245.192731555512,7.06215973620671)) ;
#74930=CARTESIAN_POINT('Ctrl Pts',(73.4035438393931,245.264974883745,7.17608503411334)) ;
#74931=CARTESIAN_POINT('Ctrl Pts',(71.9556834737297,244.786783924096,7.17267980084142)) ;
#74932=CARTESIAN_POINT('Ctrl Pts',(71.9994364250326,244.7276871246,7.05718689584929)) ;
#74933=CARTESIAN_POINT('Ctrl Pts',(72.105166158695,244.619271346283,6.82779542102222)) ;
#74934=CARTESIAN_POINT('Ctrl Pts',(72.290755802235,244.516291089754,6.55479145994173)) ;
#74935=CARTESIAN_POINT('Ctrl Pts',(72.4615143280827,244.473900464396,6.38659706769207)) ;
#74936=CARTESIAN_POINT('Ctrl Pts',(72.5745815094689,244.463950453933,6.30545098091439)) ;
#74937=CARTESIAN_POINT('Ctrl Pts',(72.7126879954014,244.465289886791,6.22919102178501)) ;
#74938=CARTESIAN_POINT('Ctrl Pts',(72.8909283600454,244.504548617211,6.19617131038086)) ;
#74939=CARTESIAN_POINT('Ctrl Pts',(73.0445730380394,244.58352939965,6.24747481449832)) ;
#74940=CARTESIAN_POINT('Ctrl Pts',(73.1325804113198,244.645452965562,6.30581330844265)) ;
#74941=CARTESIAN_POINT('Ctrl Pts',(73.2180392194167,244.720087566317,6.38728864987029)) ;
#74942=CARTESIAN_POINT('Ctrl Pts',(73.331313815252,244.854600590535,6.55517985646993)) ;
#74943=CARTESIAN_POINT('Ctrl Pts',(73.4208757682397,245.047065698635,6.82833599723182)) ;
#74944=CARTESIAN_POINT('Ctrl Pts',(73.4427713648375,245.196657079445,7.05719005384205)) ;
#74945=CARTESIAN_POINT('Ctrl Pts',(73.4434320007296,245.270182723559,7.17267980084145)) ;
#74946=CARTESIAN_POINT('Ctrl Pts',(73.4434320007296,245.270182723559,7.17267980084145)) ;
#74947=CARTESIAN_POINT('Ctrl Pts',(73.4431020130991,245.233456664063,7.11499267180461)) ;
#74948=CARTESIAN_POINT('Ctrl Pts',(73.4402029360074,245.196364845114,7.0574944676865)) ;
#74949=CARTESIAN_POINT('Ctrl Pts',(73.4344583668991,245.158974046861,7.00044813217449)) ;
#74950=CARTESIAN_POINT('Ctrl Pts',(73.430549504914,245.133531673876,6.96163125173052)) ;
#74951=CARTESIAN_POINT('Ctrl Pts',(73.4253236110167,245.107950944466,6.92302359436789)) ;
#74952=CARTESIAN_POINT('Ctrl Pts',(73.4187008698935,245.082253697312,6.88470696318928)) ;
#74953=CARTESIAN_POINT('Ctrl Pts',(73.4155906518556,245.070185576252,6.86671243868241)) ;
#74954=CARTESIAN_POINT('Ctrl Pts',(73.4121725669894,245.058091915308,6.84878227850999)) ;
#74955=CARTESIAN_POINT('Ctrl Pts',(73.4084372767916,245.045970522218,6.83091828323211)) ;
#74956=CARTESIAN_POINT('Ctrl Pts',(73.3850436077588,244.970055708869,6.71903824955231)) ;
#74957=CARTESIAN_POINT('Ctrl Pts',(73.3492173176614,244.893081205197,6.60979489059652)) ;
#74958=CARTESIAN_POINT('Ctrl Pts',(73.294132385133,244.816188540897,6.50943171095909)) ;
#74959=CARTESIAN_POINT('Ctrl Pts',(73.2710746632426,244.784002431421,6.46742119777713)) ;
#74960=CARTESIAN_POINT('Ctrl Pts',(73.2446445763898,244.751835121943,6.42697296071601)) ;
#74961=CARTESIAN_POINT('Ctrl Pts',(73.2136229784609,244.720113630821,6.38961257812027)) ;
#74962=CARTESIAN_POINT('Ctrl Pts',(73.2075751679563,244.713929372755,6.38232899089704)) ;
#74963=CARTESIAN_POINT('Ctrl Pts',(73.2013528423385,244.707762030666,6.37516271804997)) ;
#74964=CARTESIAN_POINT('Ctrl Pts',(73.1949469784241,244.701614748171,6.36812502208952)) ;
#74965=CARTESIAN_POINT('Ctrl Pts',(73.1836709346794,244.690793877285,6.35573678397329)) ;
#74966=CARTESIAN_POINT('Ctrl Pts',(73.1718261861905,244.68003516648,6.34374695713007)) ;
#74967=CARTESIAN_POINT('Ctrl Pts',(73.1593823140545,244.669394897422,6.3322774914791)) ;
#74968=CARTESIAN_POINT('Ctrl Pts',(73.1501555753554,244.661505473519,6.32377324445519)) ;
#74969=CARTESIAN_POINT('Ctrl Pts',(73.1405952222296,244.653677586905,6.31555124386587)) ;
#74970=CARTESIAN_POINT('Ctrl Pts',(73.1306902804345,244.645936066955,6.3076636555575)) ;
#74971=CARTESIAN_POINT('Ctrl Pts',(73.1074240776829,244.627751631699,6.2891361131851)) ;
#74972=CARTESIAN_POINT('Ctrl Pts',(73.0822567910222,244.61004723145,6.27245966803159)) ;
#74973=CARTESIAN_POINT('Ctrl Pts',(73.0549119312148,244.593134139718,6.25837186118317)) ;
#74974=CARTESIAN_POINT('Ctrl Pts',(73.0438936901924,244.5863192384,6.25269537015611)) ;
#74975=CARTESIAN_POINT('Ctrl Pts',(73.0325224261536,244.579632692525,6.24743866551629)) ;
#74976=CARTESIAN_POINT('Ctrl Pts',(73.0208477353986,244.573129233053,6.24267263511688)) ;
#74977=CARTESIAN_POINT('Ctrl Pts',(73.014675248033,244.569690810378,6.24015280285393)) ;
#74978=CARTESIAN_POINT('Ctrl Pts',(73.0084179521525,244.56630354916,6.23777009440928)) ;
#74979=CARTESIAN_POINT('Ctrl Pts',(73.0020832177036,244.562975403627,6.23553472416755)) ;
#74980=CARTESIAN_POINT('Ctrl Pts',(72.9955648125652,244.559550761108,6.23323454110739)) ;
#74981=CARTESIAN_POINT('Ctrl Pts',(72.9889570762782,244.556184795348,6.23108766580282)) ;
#74982=CARTESIAN_POINT('Ctrl Pts',(72.98226214601,244.552884038068,6.22910483023557)) ;
#74983=CARTESIAN_POINT('Ctrl Pts',(72.9678571946245,244.545782059967,6.22483851993699)) ;
#74984=CARTESIAN_POINT('Ctrl Pts',(72.9530544980498,244.538984925329,6.22133345057263)) ;
#74985=CARTESIAN_POINT('Ctrl Pts',(72.937916101209,244.532580800946,6.21871395687209)) ;
#74986=CARTESIAN_POINT('Ctrl Pts',(72.9316302795469,244.529921656507,6.21762628091671)) ;
#74987=CARTESIAN_POINT('Ctrl Pts',(72.9252856550904,244.527329944157,6.21669124187431)) ;
#74988=CARTESIAN_POINT('Ctrl Pts',(72.9188902808961,244.524813504551,6.21591837295059)) ;
#74989=CARTESIAN_POINT('Ctrl Pts',(72.9007439069117,244.517673304023,6.21372541783891)) ;
#74990=CARTESIAN_POINT('Ctrl Pts',(72.8821933431793,244.511142194532,6.21284099333179)) ;
#74991=CARTESIAN_POINT('Ctrl Pts',(72.8634811408771,244.505251424119,6.21317786085357)) ;
#74992=CARTESIAN_POINT('Ctrl Pts',(72.8463692443292,244.499864444422,6.21348591877695)) ;
#74993=CARTESIAN_POINT('Ctrl Pts',(72.8291180547982,244.495010433656,6.21481320707205)) ;
#74994=CARTESIAN_POINT('Ctrl Pts',(72.8118702212274,244.490694079075,6.21708372521223)) ;
#74995=CARTESIAN_POINT('Ctrl Pts',(72.7915336066829,244.485604741971,6.21976085286675)) ;
#74996=CARTESIAN_POINT('Ctrl Pts',(72.7711961915529,244.481260225182,6.22374801364797)) ;
#74997=CARTESIAN_POINT('Ctrl Pts',(72.7510661192296,244.477710567067,6.22899928973749)) ;
#74998=CARTESIAN_POINT('Ctrl Pts',(72.7440058314115,244.476465583565,6.23084108742252)) ;
#74999=CARTESIAN_POINT('Ctrl Pts',(72.7369714274797,244.475318607259,6.2328385443403)) ;
#75000=CARTESIAN_POINT('Ctrl Pts',(72.7299731476575,244.474272523511,6.23499013385452)) ;
#75001=CARTESIAN_POINT('Ctrl Pts',(72.7090389360436,244.471143334754,6.24142626263776)) ;
#75002=CARTESIAN_POINT('Ctrl Pts',(72.6883573215069,244.468786869276,6.24908069692733)) ;
#75003=CARTESIAN_POINT('Ctrl Pts',(72.6681923159947,244.467248684764,6.25787359444939)) ;
#75004=CARTESIAN_POINT('Ctrl Pts',(72.6438222406551,244.465389737965,6.26850010159001)) ;
#75005=CARTESIAN_POINT('Ctrl Pts',(72.6202065313713,244.464726020216,6.28079022660041)) ;
#75006=CARTESIAN_POINT('Ctrl Pts',(72.5973092509544,244.464976781267,6.29423639923435)) ;
#75007=CARTESIAN_POINT('Ctrl Pts',(72.5900990277946,244.465055744493,6.29847052239526)) ;
#75008=CARTESIAN_POINT('Ctrl Pts',(72.5829603890789,244.465225423066,6.30281908603248)) ;
#75009=CARTESIAN_POINT('Ctrl Pts',(72.575893129647,244.465477187611,6.30726577261015)) ;
#75010=CARTESIAN_POINT('Ctrl Pts',(72.5639041463512,244.465904283992,6.31480918482168)) ;
#75011=CARTESIAN_POINT('Ctrl Pts',(72.5521204122704,244.466567572729,6.32263505153982)) ;
#75012=CARTESIAN_POINT('Ctrl Pts',(72.5405625868693,244.467463254872,6.33072043562018)) ;
#75013=CARTESIAN_POINT('Ctrl Pts',(72.5236632480752,244.468772881507,6.34254252499356)) ;
#75014=CARTESIAN_POINT('Ctrl Pts',(72.5071998069331,244.470542167386,6.35489086909629)) ;
#75015=CARTESIAN_POINT('Ctrl Pts',(72.49118920689,244.472728629967,6.36767692557154)) ;
#75016=CARTESIAN_POINT('Ctrl Pts',(72.4398639222179,244.47973778728,6.40866526995973)) ;
#75017=CARTESIAN_POINT('Ctrl Pts',(72.3931914538475,244.491034261609,6.45415279537548)) ;
#75018=CARTESIAN_POINT('Ctrl Pts',(72.3500947237597,244.504952123835,6.50170615626623)) ;
#75019=CARTESIAN_POINT('Ctrl Pts',(72.3479010740007,244.505660551483,6.50412665124215)) ;
#75020=CARTESIAN_POINT('Ctrl Pts',(72.3457166726364,244.506375885972,6.50655267846174)) ;
#75021=CARTESIAN_POINT('Ctrl Pts',(72.3435413791296,244.507097907721,6.50898391584394)) ;
#75022=CARTESIAN_POINT('Ctrl Pts',(72.2939557630567,244.523556327311,6.56440374909368)) ;
#75023=CARTESIAN_POINT('Ctrl Pts',(72.2491073863615,244.543491811814,6.62253117127341)) ;
#75024=CARTESIAN_POINT('Ctrl Pts',(72.2081933830777,244.5660749154,6.68231650548116)) ;
#75025=CARTESIAN_POINT('Ctrl Pts',(72.1749957149923,244.58439887094,6.73082639261291)) ;
#75026=CARTESIAN_POINT('Ctrl Pts',(72.144386895211,244.604465119596,6.78042742681575)) ;
#75027=CARTESIAN_POINT('Ctrl Pts',(72.1159153532659,244.625820724971,6.83056031505395)) ;
#75028=CARTESIAN_POINT('Ctrl Pts',(72.108878159526,244.631099101981,6.84295145452781)) ;
#75029=CARTESIAN_POINT('Ctrl Pts',(72.1019714543362,244.636456219632,6.85537510631104)) ;
#75030=CARTESIAN_POINT('Ctrl Pts',(72.0951927450628,244.641889511684,6.86782833804242)) ;
#75031=CARTESIAN_POINT('Ctrl Pts',(72.0505748877656,244.677651754852,6.94979623102563)) ;
#75032=CARTESIAN_POINT('Ctrl Pts',(72.0115273534747,244.716808066892,7.03316537501444)) ;
#75033=CARTESIAN_POINT('Ctrl Pts',(71.9774750347497,244.758698720179,7.11710901687511)) ;
#75034=CARTESIAN_POINT('Ctrl Pts',(71.9699709268568,244.767930161495,7.13560767332584)) ;
#75035=CARTESIAN_POINT('Ctrl Pts',(71.9627092212568,244.777294296984,7.15413421780112)) ;
#75036=CARTESIAN_POINT('Ctrl Pts',(71.9556834737298,244.786783924096,7.17267980084129)) ;
#75037=CARTESIAN_POINT('Ctrl Pts',(72.1901462641291,244.751891562381,7.27867958884205)) ;
#75038=CARTESIAN_POINT('Ctrl Pts',(72.2226915456361,244.707440284483,7.16318668384993)) ;
#75039=CARTESIAN_POINT('Ctrl Pts',(72.3010345108137,244.62567313033,6.93379520902284)) ;
#75040=CARTESIAN_POINT('Ctrl Pts',(72.4376389789193,244.547258447274,6.66079124794237)) ;
#75041=CARTESIAN_POINT('Ctrl Pts',(72.5627005459071,244.514203826472,6.49259685569267)) ;
#75042=CARTESIAN_POINT('Ctrl Pts',(72.6452938287017,244.505871428575,6.411450768915)) ;
#75043=CARTESIAN_POINT('Ctrl Pts',(72.7460237857294,244.505796254997,6.33519080978562)) ;
#75044=CARTESIAN_POINT('Ctrl Pts',(72.8756195873876,244.533840692988,6.30217109838147)) ;
#75045=CARTESIAN_POINT('Ctrl Pts',(72.986994973301,244.591933082758,6.35347460249892)) ;
#75046=CARTESIAN_POINT('Ctrl Pts',(73.0507055731919,244.637746956413,6.41181309644325)) ;
#75047=CARTESIAN_POINT('Ctrl Pts',(73.1125055094761,244.693131160356,6.49328843787088)) ;
#75048=CARTESIAN_POINT('Ctrl Pts',(73.1942872183044,244.793268231079,6.66117964447055)) ;
#75049=CARTESIAN_POINT('Ctrl Pts',(73.2586724865194,244.937050873409,6.93433578523243)) ;
#75050=CARTESIAN_POINT('Ctrl Pts',(73.2740549596695,245.049050470208,7.1631898418427)) ;
#75051=CARTESIAN_POINT('Ctrl Pts',(73.2742568343815,245.10414043955,7.27867958884209)) ;
#75052=CARTESIAN_POINT('Origin',(73.474255491572,245.103407553477,16.0213203435596)) ;
#75053=CARTESIAN_POINT('',(73.2742568343815,245.10414043955,16.0254384350469)) ;
#75054=CARTESIAN_POINT('',(73.2742568343815,245.10414043955,16.0213203435596)) ;
#75055=CARTESIAN_POINT('Ctrl Pts',(73.2742568343815,245.10414043955,16.0254384350469)) ;
#75056=CARTESIAN_POINT('Ctrl Pts',(73.2743301777146,245.124155239482,16.0294645582753)) ;
#75057=CARTESIAN_POINT('Ctrl Pts',(73.2773992812257,245.143295198932,16.0362204083692)) ;
#75058=CARTESIAN_POINT('Ctrl Pts',(73.2896355981226,245.183957276819,16.056050217191)) ;
#75059=CARTESIAN_POINT('Ctrl Pts',(73.3002084167048,245.204241849721,16.070223718736)) ;
#75060=CARTESIAN_POINT('Ctrl Pts',(73.3282463715764,245.242541900774,16.1046945816763)) ;
#75061=CARTESIAN_POINT('Ctrl Pts',(73.3468662032201,245.259416049113,16.1258672215778)) ;
#75062=CARTESIAN_POINT('Ctrl Pts',(73.3883685066135,245.285800732098,16.1708720249666)) ;
#75063=CARTESIAN_POINT('Ctrl Pts',(73.4118063557929,245.294988472914,16.1951765216919)) ;
#75064=CARTESIAN_POINT('Ctrl Pts',(73.4365748219814,245.299827069804,16.2199877856716)) ;
#75065=CARTESIAN_POINT('Ctrl Pts',(73.4372405812222,245.29995361842,16.2206540664831)) ;
#75066=CARTESIAN_POINT('Ctrl Pts',(73.4379069626931,245.300076779458,16.2213203435596)) ;
#75067=CARTESIAN_POINT('Origin',(72.0287747312355,244.633742383918,16.0213203435596)) ;
#75068=CARTESIAN_POINT('',(72.1901462641291,244.751891562381,16.0254384350469)) ;
#75069=CARTESIAN_POINT('',(72.1901462641291,244.751891562381,16.0213203435596)) ;
#75070=CARTESIAN_POINT('Ctrl Pts',(71.9425820382072,244.814216259225,16.2213203435596)) ;
#75071=CARTESIAN_POINT('Ctrl Pts',(71.9431935443975,244.814508309059,16.2206540664685)) ;
#75072=CARTESIAN_POINT('Ctrl Pts',(71.9438065383602,244.814797252548,16.2199877856879)) ;
#75073=CARTESIAN_POINT('Ctrl Pts',(71.9632344714873,244.823834488918,16.1989219658621)) ;
#75074=CARTESIAN_POINT('Ctrl Pts',(71.9835241847008,244.829711338052,16.1784289743563)) ;
#75075=CARTESIAN_POINT('Ctrl Pts',(72.0247458013708,244.834727421522,16.1396302535195)) ;
#75076=CARTESIAN_POINT('Ctrl Pts',(72.0458338508477,244.834186521463,16.12105377447)) ;
#75077=CARTESIAN_POINT('Ctrl Pts',(72.0895325990311,244.825657771132,16.0855257633019)) ;
#75078=CARTESIAN_POINT('Ctrl Pts',(72.1124548100242,244.817186011065,16.0684876094896)) ;
#75079=CARTESIAN_POINT('Ctrl Pts',(72.1504375878132,244.793629310998,16.0440628922452)) ;
#75080=CARTESIAN_POINT('Ctrl Pts',(72.1659608719307,244.780773205401,16.0353723462245)) ;
#75081=CARTESIAN_POINT('Ctrl Pts',(72.1833422628339,244.760784770124,16.0279192770517)) ;
#75082=CARTESIAN_POINT('Ctrl Pts',(72.1868310246749,244.756419611409,16.0265673132457)) ;
#75083=CARTESIAN_POINT('Ctrl Pts',(72.1901462641293,244.751891562381,16.0254384350468)) ;
#75084=CARTESIAN_POINT('Origin',(74.5283628290597,239.4,16.2213203435596)) ;
#75085=CARTESIAN_POINT('',(73.2726525382015,245.062436901673,16.0213203435596)) ;
#75086=CARTESIAN_POINT('Ctrl Pts',(73.2742568343815,245.10414043955,16.0254384350468)) ;
#75087=CARTESIAN_POINT('Ctrl Pts',(73.2742163896029,245.093103387952,16.0232182514845)) ;
#75088=CARTESIAN_POINT('Ctrl Pts',(73.2738691507354,245.081871745349,16.0218983740811)) ;
#75089=CARTESIAN_POINT('Ctrl Pts',(73.2730305547208,245.06783972849,16.0213707571522)) ;
#75090=CARTESIAN_POINT('Ctrl Pts',(73.2728506031715,245.065136548611,16.0213203435596)) ;
#75091=CARTESIAN_POINT('Ctrl Pts',(73.2726525382014,245.062436901673,16.0213203435596)) ;
#75092=CARTESIAN_POINT('',(72.2159568915352,244.719095673148,16.0213203435596)) ;
#75093=CARTESIAN_POINT('Origin',(74.5283628290597,239.4,16.0213203435596)) ;
#75094=CARTESIAN_POINT('Ctrl Pts',(72.2159568915352,244.719095673148,16.0213203435596)) ;
#75095=CARTESIAN_POINT('Ctrl Pts',(72.2086763170662,244.727712258944,16.0213203435596)) ;
#75096=CARTESIAN_POINT('Ctrl Pts',(72.2016374368113,244.736538177641,16.0221950109068)) ;
#75097=CARTESIAN_POINT('Ctrl Pts',(72.1932909888623,244.747625968734,16.0244263118334)) ;
#75098=CARTESIAN_POINT('Ctrl Pts',(72.1917073899104,244.749759332063,16.0249068532759)) ;
#75099=CARTESIAN_POINT('Ctrl Pts',(72.1901462641291,244.751891562381,16.0254384350468)) ;
#75100=CARTESIAN_POINT('Origin',(71.0016513153049,244.25410196625,16.0213203435596)) ;
#75101=CARTESIAN_POINT('Origin',(71.0016513153049,244.25410196625,16.0213203435596)) ;
#75102=CARTESIAN_POINT('Origin',(69.67426086281,242.926711513755,16.0213203435596)) ;
#75103=CARTESIAN_POINT('Origin',(69.67426086281,242.926711513755,16.0213203435596)) ;
#75104=CARTESIAN_POINT('Origin',(68.8220237312887,241.25410196625,16.0213203435596)) ;
#75105=CARTESIAN_POINT('Origin',(68.8220237312887,241.25410196625,16.0213203435596)) ;
#75106=CARTESIAN_POINT('Origin',(68.5283628290597,239.4,16.0213203435596)) ;
#75107=CARTESIAN_POINT('Origin',(68.5283628290597,239.4,16.0213203435596)) ;
#75108=CARTESIAN_POINT('Origin',(68.8220237312888,237.54589803375,16.0213203435596)) ;
#75109=CARTESIAN_POINT('Origin',(68.8220237312888,237.54589803375,16.0213203435596)) ;
#75110=CARTESIAN_POINT('Origin',(69.6742608628099,235.873288486245,16.0213203435596)) ;
#75111=CARTESIAN_POINT('Origin',(69.6742608628099,235.873288486245,16.0213203435596)) ;
#75112=CARTESIAN_POINT('Origin',(71.0016513153048,234.54589803375,16.0213203435596)) ;
#75113=CARTESIAN_POINT('Origin',(71.0016513153048,234.54589803375,16.0213203435596)) ;
#75114=CARTESIAN_POINT('Origin',(72.67426086281,233.693660902229,16.0213203435596)) ;
#75115=CARTESIAN_POINT('Origin',(72.67426086281,233.693660902229,16.0213203435596)) ;
#75116=CARTESIAN_POINT('Origin',(74.5283628290597,233.4,16.0213203435596)) ;
#75117=CARTESIAN_POINT('Origin',(74.5283628290597,233.4,16.0213203435596)) ;
#75118=CARTESIAN_POINT('Origin',(76.3824647953094,233.693660902229,16.0213203435596)) ;
#75119=CARTESIAN_POINT('Origin',(76.3824647953094,233.693660902229,16.0213203435596)) ;
#75120=CARTESIAN_POINT('Origin',(78.0550743428145,234.54589803375,16.0213203435596)) ;
#75121=CARTESIAN_POINT('Origin',(78.0550743428145,234.54589803375,16.0213203435596)) ;
#75122=CARTESIAN_POINT('Origin',(79.3824647953094,235.873288486245,16.0213203435596)) ;
#75123=CARTESIAN_POINT('Origin',(79.3824647953094,235.873288486245,16.0213203435596)) ;
#75124=CARTESIAN_POINT('Origin',(80.2347019268307,237.54589803375,16.0213203435596)) ;
#75125=CARTESIAN_POINT('Origin',(80.2347019268307,237.54589803375,16.0213203435596)) ;
#75126=CARTESIAN_POINT('Origin',(80.5283628290597,239.4,16.0213203435596)) ;
#75127=CARTESIAN_POINT('Origin',(80.5283628290597,239.4,16.0213203435596)) ;
#75128=CARTESIAN_POINT('Origin',(80.2347019268306,241.25410196625,16.0213203435596)) ;
#75129=CARTESIAN_POINT('Origin',(80.2347019268306,241.25410196625,16.0213203435596)) ;
#75130=CARTESIAN_POINT('Origin',(79.3824647953094,242.926711513755,16.0213203435596)) ;
#75131=CARTESIAN_POINT('Origin',(79.3824647953094,242.926711513755,16.0213203435596)) ;
#75132=CARTESIAN_POINT('Origin',(78.0550743428145,244.25410196625,16.0213203435596)) ;
#75133=CARTESIAN_POINT('Origin',(78.0550743428145,244.25410196625,16.0213203435596)) ;
#75134=CARTESIAN_POINT('Origin',(76.3824647953094,245.106339097771,16.0213203435596)) ;
#75135=CARTESIAN_POINT('Origin',(76.3824647953094,245.106339097771,16.0213203435596)) ;
#75136=CARTESIAN_POINT('Origin',(74.5283628290597,245.4,16.0213203435596)) ;
#75137=CARTESIAN_POINT('Origin',(74.5283628290597,245.4,16.0213203435596)) ;
#75138=CARTESIAN_POINT('Origin',(72.67426086281,245.106339097771,16.0213203435596)) ;
#75139=CARTESIAN_POINT('Origin',(72.67426086281,245.106339097771,16.0213203435596)) ;
#75140=CARTESIAN_POINT('Origin',(74.5283628290597,239.4,6.62132034355964)) ;
#75141=CARTESIAN_POINT('',(69.2196126965601,239.4,6.115320555559)) ;
#75142=CARTESIAN_POINT('',(68.9033628290597,239.4,6.62132034355964)) ;
#75143=CARTESIAN_POINT('Origin',(74.5283628290597,239.4,6.115320555559)) ;
#75144=CARTESIAN_POINT('Origin',(76.0783628290596,240.95,6.22132034355964)) ;
#75145=CARTESIAN_POINT('',(75.3283628290596,240.95,6.02132034355964)) ;
#75146=CARTESIAN_POINT('Origin',(75.3283628290596,240.95,6.22132034355964)) ;
#75147=CARTESIAN_POINT('',(76.0783628290596,240.2,6.02132034355964)) ;
#75148=CARTESIAN_POINT('Origin',(76.0783628290596,240.95,6.02132034355964)) ;
#75149=CARTESIAN_POINT('Origin',(76.0783628290596,240.2,6.22132034355964)) ;
#75150=CARTESIAN_POINT('Origin',(74.5283628290597,239.4,6.02132034355964)) ;
#75151=CARTESIAN_POINT('',(69.3892123573611,239.4,6.02132034355964)) ;
#75152=CARTESIAN_POINT('Origin',(74.5283628290597,239.4,6.02132034355964)) ;
#75153=CARTESIAN_POINT('',(75.3283628290596,242.7,6.02132034355964)) ;
#75154=CARTESIAN_POINT('',(75.3283628290596,241.15,6.02132034355964)) ;
#75155=CARTESIAN_POINT('',(74.9283628290597,243.1,6.02132034355964)) ;
#75156=CARTESIAN_POINT('Origin',(74.9283628290597,242.7,6.02132034355964)) ;
#75157=CARTESIAN_POINT('',(74.1283628290597,243.1,6.02132034355964)) ;
#75158=CARTESIAN_POINT('',(74.2283628290596,243.1,6.02132034355964)) ;
#75159=CARTESIAN_POINT('',(73.7283628290597,242.7,6.02132034355964)) ;
#75160=CARTESIAN_POINT('Origin',(74.1283628290597,242.7,6.02132034355964)) ;
#75161=CARTESIAN_POINT('',(73.7283628290597,240.95,6.02132034355964)) ;
#75162=CARTESIAN_POINT('',(73.7283628290597,239.7,6.02132034355964)) ;
#75163=CARTESIAN_POINT('',(72.9783628290596,240.2,6.02132034355964)) ;
#75164=CARTESIAN_POINT('Origin',(72.9783628290596,240.95,6.02132034355964)) ;
#75165=CARTESIAN_POINT('',(71.2283628290598,240.2,6.02132034355964)) ;
#75166=CARTESIAN_POINT('',(72.7783628290597,240.2,6.02132034355964)) ;
#75167=CARTESIAN_POINT('',(70.8283628290598,239.8,6.02132034355964)) ;
#75168=CARTESIAN_POINT('Origin',(71.2283628290598,239.8,6.02132034355964)) ;
#75169=CARTESIAN_POINT('',(70.8283628290598,239.,6.02132034355964)) ;
#75170=CARTESIAN_POINT('',(70.8283628290598,239.1,6.02132034355964)) ;
#75171=CARTESIAN_POINT('',(71.2283628290597,238.6,6.02132034355964)) ;
#75172=CARTESIAN_POINT('Origin',(71.2283628290597,239.,6.02132034355964)) ;
#75173=CARTESIAN_POINT('',(72.9783628290596,238.6,6.02132034355964)) ;
#75174=CARTESIAN_POINT('',(74.2283628290596,238.6,6.02132034355964)) ;
#75175=CARTESIAN_POINT('',(73.7283628290597,237.85,6.02132034355964)) ;
#75176=CARTESIAN_POINT('Origin',(72.9783628290596,237.85,6.02132034355964)) ;
#75177=CARTESIAN_POINT('',(73.7283628290597,236.1,6.02132034355964)) ;
#75178=CARTESIAN_POINT('',(73.7283628290597,237.65,6.02132034355964)) ;
#75179=CARTESIAN_POINT('',(74.1283628290597,235.7,6.02132034355964)) ;
#75180=CARTESIAN_POINT('Origin',(74.1283628290597,236.1,6.02132034355964)) ;
#75181=CARTESIAN_POINT('',(74.9283628290597,235.7,6.02132034355964)) ;
#75182=CARTESIAN_POINT('',(74.8283628290597,235.7,6.02132034355964)) ;
#75183=CARTESIAN_POINT('',(75.3283628290596,236.1,6.02132034355964)) ;
#75184=CARTESIAN_POINT('Origin',(74.9283628290597,236.1,6.02132034355964)) ;
#75185=CARTESIAN_POINT('',(75.3283628290596,237.85,6.02132034355964)) ;
#75186=CARTESIAN_POINT('',(75.3283628290596,239.1,6.02132034355964)) ;
#75187=CARTESIAN_POINT('',(76.0783628290597,238.6,6.02132034355964)) ;
#75188=CARTESIAN_POINT('Origin',(76.0783628290597,237.85,6.02132034355964)) ;
#75189=CARTESIAN_POINT('',(77.8283628290598,238.6,6.02132034355964)) ;
#75190=CARTESIAN_POINT('',(76.2783628290597,238.6,6.02132034355964)) ;
#75191=CARTESIAN_POINT('',(78.2283628290598,239.,6.02132034355964)) ;
#75192=CARTESIAN_POINT('Origin',(77.8283628290598,239.,6.02132034355964)) ;
#75193=CARTESIAN_POINT('',(78.2283628290598,239.8,6.02132034355964)) ;
#75194=CARTESIAN_POINT('',(78.2283628290598,239.7,6.02132034355964)) ;
#75195=CARTESIAN_POINT('',(77.8283628290598,240.2,6.02132034355964)) ;
#75196=CARTESIAN_POINT('Origin',(77.8283628290598,239.8,6.02132034355964)) ;
#75197=CARTESIAN_POINT('',(74.8283628290597,240.2,6.02132034355964)) ;
#75198=CARTESIAN_POINT('Origin',(75.3283628290596,241.15,6.22132034355964)) ;
#75199=CARTESIAN_POINT('',(75.1283628290596,242.7,6.22132034355964)) ;
#75200=CARTESIAN_POINT('',(75.1283628290596,241.15,6.22132034355964)) ;
#75201=CARTESIAN_POINT('Origin',(75.3283628290596,242.7,6.22132034355964)) ;
#75202=CARTESIAN_POINT('Origin',(75.1283628290596,242.9,11.0213203435596)) ;
#75203=CARTESIAN_POINT('',(75.1283628290596,242.7,11.0213203435596)) ;
#75204=CARTESIAN_POINT('Origin',(76.0783628290597,237.85,6.22132034355964)) ;
#75205=CARTESIAN_POINT('Origin',(76.0783628290597,238.6,6.22132034355964)) ;
#75206=CARTESIAN_POINT('Origin',(75.3283628290597,237.85,6.22132034355964)) ;
#75207=CARTESIAN_POINT('Origin',(76.2783628290597,238.6,6.22132034355964)) ;
#75208=CARTESIAN_POINT('Origin',(77.8283628290598,238.6,6.22132034355964)) ;
#75209=CARTESIAN_POINT('Origin',(72.9783628290596,240.95,6.22132034355964)) ;
#75210=CARTESIAN_POINT('',(72.9783628290596,240.,6.22132034355964)) ;
#75211=CARTESIAN_POINT('Origin',(72.9783628290596,240.2,6.22132034355964)) ;
#75212=CARTESIAN_POINT('',(73.9283628290597,240.95,6.22132034355964)) ;
#75213=CARTESIAN_POINT('Origin',(73.7283628290596,240.95,6.22132034355964)) ;
#75214=CARTESIAN_POINT('Origin',(72.9783628290596,240.95,6.22132034355964)) ;
#75215=CARTESIAN_POINT('Origin',(72.9783628290596,240.95,11.0213203435596)) ;
#75216=CARTESIAN_POINT('',(72.9783628290596,240.,11.0213203435596)) ;
#75217=CARTESIAN_POINT('',(73.9283628290597,240.95,11.0213203435596)) ;
#75218=CARTESIAN_POINT('Origin',(72.7783628290597,240.2,6.22132034355964)) ;
#75219=CARTESIAN_POINT('',(71.2283628290598,240.,6.22132034355964)) ;
#75220=CARTESIAN_POINT('',(72.7783628290597,240.,6.22132034355964)) ;
#75221=CARTESIAN_POINT('Origin',(71.2283628290598,240.2,6.22132034355964)) ;
#75222=CARTESIAN_POINT('Origin',(71.0283628290598,240.,11.0213203435596)) ;
#75223=CARTESIAN_POINT('',(71.2283628290598,240.,11.0213203435596)) ;
#75224=CARTESIAN_POINT('Origin',(72.9783628290596,237.85,6.22132034355964)) ;
#75225=CARTESIAN_POINT('Origin',(73.7283628290596,237.85,6.22132034355964)) ;
#75226=CARTESIAN_POINT('',(72.9783628290596,238.8,6.22132034355964)) ;
#75227=CARTESIAN_POINT('Origin',(72.9783628290596,238.6,6.22132034355964)) ;
#75228=CARTESIAN_POINT('Origin',(72.9783628290596,237.85,6.22132034355964)) ;
#75229=CARTESIAN_POINT('Origin',(72.9783628290596,237.85,11.0213203435596)) ;
#75230=CARTESIAN_POINT('',(72.9783628290596,238.8,11.0213203435596)) ;
#75231=CARTESIAN_POINT('Origin',(73.7283628290597,237.65,6.22132034355964)) ;
#75232=CARTESIAN_POINT('Origin',(73.7283628290597,236.1,6.22132034355964)) ;
#75233=CARTESIAN_POINT('Origin',(74.5283628290597,239.4,6.22132034355964)) ;
#75234=CARTESIAN_POINT('Origin',(69.3892123573611,239.4,6.22132034355964)) ;
#75235=CARTESIAN_POINT('Origin',(77.8283628290598,239.,6.22132034355964)) ;
#75236=CARTESIAN_POINT('Origin',(78.2283628290598,239.,6.22132034355964)) ;
#75237=CARTESIAN_POINT('Origin',(77.8283628290598,239.8,6.22132034355964)) ;
#75238=CARTESIAN_POINT('Origin',(78.2283628290598,239.8,6.22132034355964)) ;
#75239=CARTESIAN_POINT('Origin',(77.8283628290598,240.2,6.22132034355964)) ;
#75240=CARTESIAN_POINT('Origin',(78.2283628290598,239.7,6.22132034355964)) ;
#75241=CARTESIAN_POINT('Origin',(74.9283628290597,236.1,6.22132034355964)) ;
#75242=CARTESIAN_POINT('Origin',(75.3283628290596,236.1,6.22132034355964)) ;
#75243=CARTESIAN_POINT('Origin',(74.9283628290597,235.7,6.22132034355964)) ;
#75244=CARTESIAN_POINT('Origin',(75.3283628290596,239.1,6.22132034355964)) ;
#75245=CARTESIAN_POINT('Origin',(74.8283628290597,240.2,6.22132034355964)) ;
#75246=CARTESIAN_POINT('Origin',(74.1283628290597,236.1,6.22132034355964)) ;
#75247=CARTESIAN_POINT('Origin',(74.1283628290597,235.7,6.22132034355964)) ;
#75248=CARTESIAN_POINT('Origin',(74.9283628290597,242.7,6.22132034355964)) ;
#75249=CARTESIAN_POINT('',(74.9283628290597,242.9,6.22132034355964)) ;
#75250=CARTESIAN_POINT('Origin',(74.9283628290597,242.7,6.22132034355964)) ;
#75251=CARTESIAN_POINT('Origin',(74.9283628290597,243.1,6.22132034355964)) ;
#75252=CARTESIAN_POINT('Origin',(74.9283628290597,242.7,11.0213203435596)) ;
#75253=CARTESIAN_POINT('',(74.9283628290597,242.9,11.0213203435596)) ;
#75254=CARTESIAN_POINT('Origin',(74.1283628290597,242.7,6.22132034355964)) ;
#75255=CARTESIAN_POINT('',(74.1283628290597,242.9,6.22132034355964)) ;
#75256=CARTESIAN_POINT('Origin',(74.1283628290597,243.1,6.22132034355964)) ;
#75257=CARTESIAN_POINT('',(73.9283628290597,242.7,6.22132034355964)) ;
#75258=CARTESIAN_POINT('Origin',(74.1283628290597,242.7,6.22132034355964)) ;
#75259=CARTESIAN_POINT('Origin',(73.7283628290597,242.7,6.22132034355964)) ;
#75260=CARTESIAN_POINT('Origin',(74.2283628290596,243.1,6.22132034355964)) ;
#75261=CARTESIAN_POINT('',(74.2283628290596,242.9,6.22132034355964)) ;
#75262=CARTESIAN_POINT('Origin',(74.1283628290597,242.7,11.0213203435596)) ;
#75263=CARTESIAN_POINT('',(73.9283628290597,242.7,11.0213203435596)) ;
#75264=CARTESIAN_POINT('',(74.1283628290597,242.9,11.0213203435596)) ;
#75265=CARTESIAN_POINT('Origin',(71.2283628290597,239.,6.22132034355964)) ;
#75266=CARTESIAN_POINT('',(71.0283628290597,239.,6.22132034355964)) ;
#75267=CARTESIAN_POINT('Origin',(70.8283628290598,239.,6.22132034355964)) ;
#75268=CARTESIAN_POINT('',(71.2283628290597,238.8,6.22132034355964)) ;
#75269=CARTESIAN_POINT('Origin',(71.2283628290597,239.,6.22132034355964)) ;
#75270=CARTESIAN_POINT('Origin',(71.2283628290597,238.6,6.22132034355964)) ;
#75271=CARTESIAN_POINT('Origin',(73.7283628290597,239.7,6.22132034355964)) ;
#75272=CARTESIAN_POINT('',(73.9283628290597,239.7,6.22132034355964)) ;
#75273=CARTESIAN_POINT('Origin',(71.2283628290598,239.8,6.22132034355964)) ;
#75274=CARTESIAN_POINT('',(71.0283628290598,239.8,6.22132034355964)) ;
#75275=CARTESIAN_POINT('Origin',(71.2283628290598,239.8,6.22132034355964)) ;
#75276=CARTESIAN_POINT('Origin',(70.8283628290598,239.8,6.22132034355964)) ;
#75277=CARTESIAN_POINT('Origin',(71.2283628290598,239.8,11.0213203435596)) ;
#75278=CARTESIAN_POINT('',(71.0283628290598,239.8,11.0213203435596)) ;
#75279=CARTESIAN_POINT('Origin',(70.8283628290598,239.1,6.22132034355964)) ;
#75280=CARTESIAN_POINT('',(71.0283628290597,239.1,6.22132034355964)) ;
#75281=CARTESIAN_POINT('Origin',(71.2283628290597,239.,11.0213203435596)) ;
#75282=CARTESIAN_POINT('',(71.2283628290597,238.8,11.0213203435596)) ;
#75283=CARTESIAN_POINT('',(71.0283628290597,239.,11.0213203435596)) ;
#75284=CARTESIAN_POINT('Origin',(74.2283628290596,238.6,6.22132034355964)) ;
#75285=CARTESIAN_POINT('',(74.2283628290596,238.8,6.22132034355964)) ;
#75286=CARTESIAN_POINT('Origin',(74.8283628290597,235.7,6.22132034355964)) ;
#75287=CARTESIAN_POINT('Origin',(76.2897596969969,233.978977857118,16.0213203435596)) ;
#75288=CARTESIAN_POINT('Origin',(77.8787387671268,234.788603132063,16.0213203435596)) ;
#75289=CARTESIAN_POINT('Origin',(79.1397596969969,236.049624061933,16.0213203435596)) ;
#75290=CARTESIAN_POINT('Origin',(79.9493849719421,237.638603132063,16.0213203435596)) ;
#75291=CARTESIAN_POINT('Origin',(80.2283628290596,239.4,16.0213203435596)) ;
#75292=CARTESIAN_POINT('Origin',(79.9493849719421,241.161396867937,16.0213203435596)) ;
#75293=CARTESIAN_POINT('Origin',(79.1397596969969,242.750375938067,16.0213203435596)) ;
#75294=CARTESIAN_POINT('Origin',(77.8787387671268,244.011396867937,16.0213203435596)) ;
#75295=CARTESIAN_POINT('Origin',(76.2897596969969,244.821022142882,16.0213203435596)) ;
#75296=CARTESIAN_POINT('Origin',(74.5283628290597,245.1,16.0213203435596)) ;
#75297=CARTESIAN_POINT('Origin',(72.7669659611225,244.821022142882,16.0213203435596)) ;
#75298=CARTESIAN_POINT('Origin',(71.1779868909926,244.011396867937,16.0213203435596)) ;
#75299=CARTESIAN_POINT('Origin',(69.9169659611225,242.750375938067,16.0213203435596)) ;
#75300=CARTESIAN_POINT('Origin',(69.1073406861773,241.161396867937,16.0213203435596)) ;
#75301=CARTESIAN_POINT('Origin',(68.8283628290597,239.4,16.0213203435596)) ;
#75302=CARTESIAN_POINT('Origin',(69.1073406861773,237.638603132063,16.0213203435596)) ;
#75303=CARTESIAN_POINT('Origin',(69.9169659611224,236.049624061933,16.0213203435596)) ;
#75304=CARTESIAN_POINT('Origin',(71.1779868909926,234.788603132063,16.0213203435596)) ;
#75305=CARTESIAN_POINT('Origin',(72.7669659611225,233.978977857118,16.0213203435596)) ;
#75306=CARTESIAN_POINT('Origin',(74.5283628290597,233.7,16.0213203435596)) ;
#75307=CARTESIAN_POINT('Origin',(73.9283628290597,240.,11.0213203435596)) ;
#75308=CARTESIAN_POINT('Origin',(71.0283628290597,238.8,11.0213203435596)) ;
#75309=CARTESIAN_POINT('Origin',(73.9283628290597,238.8,11.0213203435596)) ;
#75310=CARTESIAN_POINT('Origin',(73.9283628290597,242.9,11.0213203435596)) ;
#117126=UNCERTAINTY_MEASURE_WITH_UNIT(LENGTH_MEASURE(0.01),#117171,
'DISTANCE_ACCURACY_VALUE',
'Maximum model space distance between geometric entities at asserted c
onnectivities') ;
#117147=UNCERTAINTY_MEASURE_WITH_UNIT(LENGTH_MEASURE(0.01),#117171,
'DISTANCE_ACCURACY_VALUE',
'Maximum model space distance between geometric entities at asserted c
onnectivities') ;
#117149=(
GEOMETRIC_REPRESENTATION_CONTEXT(3)
GLOBAL_UNCERTAINTY_ASSIGNED_CONTEXT((#117126))
GLOBAL_UNIT_ASSIGNED_CONTEXT((#117171,#117173,#117174))
REPRESENTATION_CONTEXT('','3D')
) ;
#117170=(
GEOMETRIC_REPRESENTATION_CONTEXT(3)
GLOBAL_UNCERTAINTY_ASSIGNED_CONTEXT((#117147))
GLOBAL_UNIT_ASSIGNED_CONTEXT((#117171,#117173,#117174))
REPRESENTATION_CONTEXT('','3D')
) ;
#117171=(
LENGTH_UNIT()
NAMED_UNIT(*)
SI_UNIT(.MILLI.,.METRE.)
) ;
#117173=(
NAMED_UNIT(*)
PLANE_ANGLE_UNIT()
SI_UNIT($,.RADIAN.)
) ;
#117174=(
NAMED_UNIT(*)
SI_UNIT($,.STERADIAN.)
SOLID_ANGLE_UNIT()
) ;
#117176=SHAPE_DEFINITION_REPRESENTATION(#117198,#117241) ;
#117198=PRODUCT_DEFINITION_SHAPE('',$,#117264) ;
#117241=SHAPE_REPRESENTATION('',(#49311),#117149) ;
#117262=PRODUCT_DEFINITION_CONTEXT('part definition',#117330,'design') ;
#117264=PRODUCT_DEFINITION('Vertical_Knob','Vertical_Knob',#117286,#117262) ;
#117286=PRODUCT_DEFINITION_FORMATION('',$,#117333) ;
#117330=APPLICATION_CONTEXT(
'Core Data for Automotive Mechanical Design Process') ;
#117331=PRODUCT_CONTEXT('part definition',#117330,'mechanical') ;
#117333=PRODUCT('Vertical_Knob','Vertical_Knob',$,(#117331)) ;
#117355=PRESENTATION_STYLE_ASSIGNMENT((#117357)) ;
#117357=SURFACE_STYLE_USAGE(.BOTH.,#117359) ;
#117359=SURFACE_SIDE_STYLE('',(#117361)) ;
#117361=SURFACE_STYLE_FILL_AREA(#117363) ;
#117363=FILL_AREA_STYLE('Opaque(160,160,160)',(#117365)) ;
#117365=FILL_AREA_STYLE_COLOUR('Opaque(160,160,160)',#117367) ;
#117367=COLOUR_RGB('Opaque(160,160,160)', 0.09019608, 0.27058824, 0.51372549) ;
ENDSEC;
END-ISO-10303-21;
